ISO-10303-21;
HEADER;
FILE_DESCRIPTION (('STEP AP214'),
    '1' );
FILE_NAME ('Pocket Clip.step',
    '2026-10-06T14:00:01',
    ( '' ),
    ( '' ),
    'SwSTEP 2.0',
    'SolidWorks 2020',
    '' );
FILE_SCHEMA (( 'AUTOMOTIVE_DESIGN' ));
ENDSEC;

DATA;
#7=EDGE_CURVE ( 'NONE', #13124, #5233, #22627, .T. ) ;
#10=AXIS2_PLACEMENT_3D ( 'NONE', #12076, #19216, #28858 ) ;
#11=PLANE ( 'NONE',  #16571 ) ;
#12=FACE_OUTER_BOUND ( 'NONE', #24808, .T. ) ;
#14=B_SPLINE_CURVE_WITH_KNOTS ( 'NONE', 3,
 ( #5240, #644, #10304, #19973, #29610, #17605, #27249, #12178, #23901, #9510 ),
 .UNSPECIFIED., .F., .F.,
 ( 4, 2, 2, 2, 4 ),
 ( 0.000000000000000000, 0.0003925703575136129699, 0.0007851407150272259397, 0.001177711072540838910, 0.001570281430054451879 ),
 .UNSPECIFIED. ) ;
#33=ORIENTED_EDGE ( 'NONE', *, *, #2651, .T. ) ;
#41=CARTESIAN_POINT ( 'NONE',  ( 53.71392934491857574, 7.814769211952036443, -2.050000000000187228 ) ) ;
#53=DIRECTION ( 'NONE',  ( -1.000000000000000000, -0.000000000000000000, 3.491481338843133355E-15 ) ) ;
#57=CARTESIAN_POINT ( 'NONE',  ( 54.19028661868582475, 6.697846887293304796, 2.049999999999810640 ) ) ;
#58=CARTESIAN_POINT ( 'NONE',  ( 47.10000000920868501, -4.079797993893489405, 2.128382101831542528 ) ) ;
#59=ORIENTED_EDGE ( 'NONE', *, *, #31217, .T. ) ;
#64=CARTESIAN_POINT ( 'NONE',  ( 51.80000000000002558, -3.933368109459642437, 2.186004417992994497 ) ) ;
#69=EDGE_LOOP ( 'NONE', ( #13659, #24370, #7129, #8608 ) ) ;
#75=CARTESIAN_POINT ( 'NONE',  ( 29.99460041311888148, 6.535150002936795488, 2.049999999999441158 ) ) ;
#100=PLANE ( 'NONE',  #28662 ) ;
#105=CYLINDRICAL_SURFACE ( 'NONE', #5460, 4.099999999999992539 ) ;
#107=VERTEX_POINT ( 'NONE', #27203 ) ;
#111=EDGE_CURVE ( 'NONE', #4199, #30552, #22537, .T. ) ;
#116=CARTESIAN_POINT ( 'NONE',  ( 52.18319145150645255, 8.687974897284844289, -2.050000000000181455 ) ) ;
#119=EDGE_CURVE ( 'NONE', #27144, #25407, #10724, .T. ) ;
#125=VERTEX_POINT ( 'NONE', #18190 ) ;
#128=CARTESIAN_POINT ( 'NONE',  ( 53.73313364444125995, 5.556159244632989491, 1.667741514041239048 ) ) ;
#129=CARTESIAN_POINT ( 'NONE',  ( 53.99324657738113586, 6.679477176219531742, 1.975347020395713526 ) ) ;
#133=VERTEX_POINT ( 'NONE', #3916 ) ;
#137=CARTESIAN_POINT ( 'NONE',  ( 47.44814918337031884, -3.852602532216165887, -1.405026670785768816 ) ) ;
#142=LINE ( 'NONE', #17098, #13523 ) ;
#152=AXIS2_PLACEMENT_3D ( 'NONE', #25976, #4453, #2803 ) ;
#155=ADVANCED_FACE ( 'NONE', ( #20723 ), #5995, .F. ) ;
#156=CARTESIAN_POINT ( 'NONE',  ( 51.70000000000002416, 4.174380580618757719, 1.932497546739255556 ) ) ;
#157=ADVANCED_FACE ( 'NONE', ( #22927 ), #25441, .T. ) ;
#163=CARTESIAN_POINT ( 'NONE',  ( 22.04321716858594371, 7.679566743993215816, 1.424999999999923661 ) ) ;
#172=ORIENTED_EDGE ( 'NONE', *, *, #3641, .F. ) ;
#184=EDGE_LOOP ( 'NONE', ( #28553, #23035, #27159, #29370 ) ) ;
#186=CARTESIAN_POINT ( 'NONE',  ( 54.23679421920400756, 6.620234584472831862, -2.050000000000189004 ) ) ;
#196=DIRECTION ( 'NONE',  ( 3.491481338843133750E-15, 0.000000000000000000, 1.000000000000000000 ) ) ;
#199=CARTESIAN_POINT ( 'NONE',  ( 52.72006341977384380, 4.014035108600657153, -0.8473018902927296203 ) ) ;
#200=CARTESIAN_POINT ( 'NONE',  ( 48.00000000000002842, -4.387164041431067751, 1.383037119376590462 ) ) ;
#201=ORIENTED_EDGE ( 'NONE', *, *, #2247, .T. ) ;
#205=CARTESIAN_POINT ( 'NONE',  ( 29.29107486424064888, 6.659593085418571867, 1.424999999999898126 ) ) ;
#211=EDGE_CURVE ( 'NONE', #19416, #22328, #13432, .T. ) ;
#220=CARTESIAN_POINT ( 'NONE',  ( 27.52339381995009049, 5.460762561607864995, 2.049999999999904787 ) ) ;
#228=EDGE_CURVE ( 'NONE', #8009, #12847, #30638, .T. ) ;
#251=CARTESIAN_POINT ( 'NONE',  ( 31.90749320720395588, 7.645246318247174599, -2.050000000000176570 ) ) ;
#255=DIRECTION ( 'NONE',  ( -1.000000000000000000, -0.000000000000000000, 3.491481338843133355E-15 ) ) ;
#260=CARTESIAN_POINT ( 'NONE',  ( 53.91678946233204073, 6.821600947619984368, -1.787725782035514355 ) ) ;
#264=AXIS2_PLACEMENT_3D ( 'NONE', #11573, #21251, #6807 ) ;
#271=CARTESIAN_POINT ( 'NONE',  ( 53.91582462592152325, 6.672259099522118930, 0.8960560279709253173 ) ) ;
#281=DIRECTION ( 'NONE',  ( 0.9993908270190958731, -0.03489949670249358621, 0.000000000000000000 ) ) ;
#285=CARTESIAN_POINT ( 'NONE',  ( 51.80000048712027905, 3.919471135816211316, 2.045252759501752227 ) ) ;
#293=AXIS2_PLACEMENT_3D ( 'NONE', #30543, #21080, #28187 ) ;
#302=CIRCLE ( 'NONE', #5869, 2.625000000001610267 ) ;
#307=CARTESIAN_POINT ( 'NONE',  ( 51.25173832208872682, -3.873874536552759373, 1.343508358799209379 ) ) ;
#308=CARTESIAN_POINT ( 'NONE',  ( 22.44093457455321783, 6.836382162713700694, 1.424999999999920997 ) ) ;
#312=ORIENTED_EDGE ( 'NONE', *, *, #11950, .F. ) ;
#320=VERTEX_POINT ( 'NONE', #1312 ) ;
#323=AXIS2_PLACEMENT_3D ( 'NONE', #26001, #1950, #28541 ) ;
#329=EDGE_CURVE ( 'NONE', #6782, #11116, #30403, .T. ) ;
#348=DIRECTION ( 'NONE',  ( -1.000000000000000000, -0.000000000000000000, 3.491481338843133355E-15 ) ) ;
#357=EDGE_CURVE ( 'NONE', #13475, #23396, #17276, .T. ) ;
#361=CARTESIAN_POINT ( 'NONE',  ( 52.91788431598524056, 4.099929541424792490, -0.1776868343159781760 ) ) ;
#362=CARTESIAN_POINT ( 'NONE',  ( 47.10000000000002984, -4.020776289669855785, 2.234582293948413678 ) ) ;
#363=VERTEX_POINT ( 'NONE', #7618 ) ;
#377=CARTESIAN_POINT ( 'NONE',  ( 51.80000000000001847, 0.2793919678926817252, -0.9601771338026217073 ) ) ;
#381=CARTESIAN_POINT ( 'NONE',  ( 32.30803788440357494, 7.816246120667637243, 2.049999999999888356 ) ) ;
#390=CIRCLE ( 'NONE', #15052, 160.1997717543138720 ) ;
#402=EDGE_LOOP ( 'NONE', ( #25249, #26786, #6480, #5576 ) ) ;
#407=CIRCLE ( 'NONE', #8905, 0.1000000000000003386 ) ;
#409=ORIENTED_EDGE ( 'NONE', *, *, #20294, .F. ) ;
#411=ORIENTED_EDGE ( 'NONE', *, *, #1166, .F. ) ;
#413=DIRECTION ( 'NONE',  ( -1.000000000000000000, -0.000000000000000000, 3.491481338843133355E-15 ) ) ;
#416=CARTESIAN_POINT ( 'NONE',  ( 33.97298909694990243, 8.288184271123828495, -2.050000000000117506 ) ) ;
#422=CARTESIAN_POINT ( 'NONE',  ( 52.54946733419065197, 4.465216787881845839, -1.565330858589896845 ) ) ;
#433=CARTESIAN_POINT ( 'NONE',  ( 53.90733871594494531, 6.075395493854959028, -1.402257306246839752 ) ) ;
#464=CARTESIAN_POINT ( 'NONE',  ( 23.09424125814508955, 6.161968159343407692, 1.424999999999919664 ) ) ;
#471=CARTESIAN_POINT ( 'NONE',  ( 47.10000000000000853, -4.020776289669854009, -2.234582293948742748 ) ) ;
#472=DIRECTION ( 'NONE',  ( 0.6819983600624907050, -0.7313537016191778983, -2.168404344971033323E-15 ) ) ;
#485=AXIS2_PLACEMENT_3D ( 'NONE', #31169, #14065, #21059 ) ;
#497=AXIS2_PLACEMENT_3D ( 'NONE', #10217, #15753, #20048 ) ;
#499=CARTESIAN_POINT ( 'NONE',  ( 47.10000000000002274, 2.428612866367529932E-14, -1.644487710595116631E-13 ) ) ;
#509=CARTESIAN_POINT ( 'NONE',  ( 47.19811728011942620, -4.191430714671217750, -1.624095931900840117 ) ) ;
#516=ORIENTED_EDGE ( 'NONE', *, *, #10698, .T. ) ;
#530=CARTESIAN_POINT ( 'NONE',  ( 22.41225425283438355, 6.886225701514022468, 2.050000000000119726 ) ) ;
#536=DIRECTION ( 'NONE',  ( 0.000000000000000000, 0.000000000000000000, 1.000000000000000000 ) ) ;
#541=EDGE_CURVE ( 'NONE', #13128, #21850, #16800, .T. ) ;
#542=AXIS2_PLACEMENT_3D ( 'NONE', #25219, #6797, #30869 ) ;
#546=FACE_OUTER_BOUND ( 'NONE', #69, .T. ) ;
#549=SHAPE_REPRESENTATION ( 'Pocket Clip', ( #9018 ), #22713 ) ;
#550=ORIENTED_EDGE ( 'NONE', *, *, #4785, .F. ) ;
#554=FACE_OUTER_BOUND ( 'NONE', #22689, .T. ) ;
#557=CARTESIAN_POINT ( 'NONE',  ( 51.30885344615025190, -4.380199991373268986, -1.408811060053339226 ) ) ;
#561=CARTESIAN_POINT ( 'NONE',  ( 26.91641317417821000, 5.349067879199080444, -2.050000000000093969 ) ) ;
#566=EDGE_CURVE ( 'NONE', #9993, #18673, #27716, .T. ) ;
#570=CARTESIAN_POINT ( 'NONE',  ( 54.21471704787896329, 5.862036637490151136, -2.050000000000189004 ) ) ;
#571=CARTESIAN_POINT ( 'NONE',  ( 47.49336422635084887, -3.991980709735058142, -1.294710393269184134 ) ) ;
#578=DIRECTION ( 'NONE',  ( 3.491481338843133355E-15, -0.000000000000000000, 1.000000000000000000 ) ) ;
#579=ORIENTED_EDGE ( 'NONE', *, *, #7, .T. ) ;
#582=CARTESIAN_POINT ( 'NONE',  ( 54.19695643086576808, 6.698469119960920537, 2.049999999999810640 ) ) ;
#583=EDGE_LOOP ( 'NONE', ( #2042, #21747, #12985, #11896, #10364, #14795, #4740, #15981, #29108, #15326 ) ) ;
#586=CARTESIAN_POINT ( 'NONE',  ( 52.61915120152465875, 4.492597126270361230, 1.565330858589529806 ) ) ;
#588=CARTESIAN_POINT ( 'NONE',  ( 51.25960411873057154, -4.349885043120370831, 1.496908008647323207 ) ) ;
#594=CARTESIAN_POINT ( 'NONE',  ( 52.84329436925435886, 4.147588588921422570, 2.046816584343155387 ) ) ;
#609=DIRECTION ( 'NONE',  ( 1.000000000000000000, 0.000000000000000000, -3.491481338843133750E-15 ) ) ;
#610=EDGE_CURVE ( 'NONE', #737, #19244, #24862, .T. ) ;
#615=CARTESIAN_POINT ( 'NONE',  ( 25.07992259980452943, 5.430687345545501366, 2.049999999999912781 ) ) ;
#638=B_SPLINE_CURVE_WITH_KNOTS ( 'NONE', 3,
 ( #156, #24228, #5203, #14564 ),
 .UNSPECIFIED., .F., .F.,
 ( 4, 4 ),
 ( 0.000000000000000000, 0.0001000467755295619533 ),
 .UNSPECIFIED. ) ;
#644=CARTESIAN_POINT ( 'NONE',  ( 50.93273774044249791, -4.031600731908414836, 1.173113608511496153 ) ) ;
#646=EDGE_CURVE ( 'NONE', #4290, #26664, #11219, .T. ) ;
#647=CARTESIAN_POINT ( 'NONE',  ( 23.27131915274573615, 6.595123925190214287, -1.425000000000080869 ) ) ;
#658=CARTESIAN_POINT ( 'NONE',  ( 51.70000000000001705, 3.851905453475298113, -1.404572667215154835 ) ) ;
#659=CARTESIAN_POINT ( 'NONE',  ( 47.86824454757851299, -4.417905783403702991, 1.285520530454691057 ) ) ;
#660=ORIENTED_EDGE ( 'NONE', *, *, #4616, .F. ) ;
#665=ORIENTED_EDGE ( 'NONE', *, *, #19945, .T. ) ;
#669=CARTESIAN_POINT ( 'NONE',  ( 34.41826917700200994, 8.206708519135760938, 1.949999999999880274 ) ) ;
#673=DIRECTION ( 'NONE',  ( 1.000000000000000000, 0.000000000000000000, -3.491481338843133355E-15 ) ) ;
#705=CARTESIAN_POINT ( 'NONE',  ( 53.91566580141704890, 6.672244292255800069, -1.816235364411796116 ) ) ;
#710=CARTESIAN_POINT ( 'NONE',  ( 25.99900894223747017, 5.212247164669804533, -2.050000000000091305 ) ) ;
#712=DIRECTION ( 'NONE',  ( 1.000000000000000000, -0.000000000000000000, -3.491481338843133355E-15 ) ) ;
#714=CARTESIAN_POINT ( 'NONE',  ( 47.53097527630302466, -3.881932310064107217, 1.329369065054880394 ) ) ;
#718=CARTESIAN_POINT ( 'NONE',  ( 54.12895949791516159, 5.523355893849346110, -2.050000000000188560 ) ) ;
#720=CARTESIAN_POINT ( 'NONE',  ( 47.38545878925128818, -3.877603133524967660, -1.337216932410631554 ) ) ;
#728=CARTESIAN_POINT ( 'NONE',  ( 50.87477060347373481, 8.633605004118187765, -2.050000000000176570 ) ) ;
#729=ORIENTED_EDGE ( 'NONE', *, *, #12353, .T. ) ;
#730=VECTOR ( 'NONE', #6705, 1000.000000000000000 ) ;
#734=CARTESIAN_POINT ( 'NONE',  ( 54.37322678328315106, 5.989334493575450225, 2.026383240762962057 ) ) ;
#735=ORIENTED_EDGE ( 'NONE', *, *, #357, .T. ) ;
#737=VERTEX_POINT ( 'NONE', #5196 ) ;
#742=CARTESIAN_POINT ( 'NONE',  ( 51.59056972799722018, -4.226153977860459321, 1.819915812912550335 ) ) ;
#743=CARTESIAN_POINT ( 'NONE',  ( 51.58885679141839375, -3.753732476607584800, -1.652583012570544074 ) ) ;
#744=EDGE_LOOP ( 'NONE', ( #9293, #4130, #2550, #9244, #30717, #18089, #30568, #28296 ) ) ;
#748=CARTESIAN_POINT ( 'NONE',  ( 52.07305031865988809, 3.932152079777906817, 2.045338552409953881 ) ) ;
#800=CARTESIAN_POINT ( 'NONE',  ( 53.90177594311669651, 7.547472342232321552, -2.050000000000187672 ) ) ;
#811=CARTESIAN_POINT ( 'NONE',  ( 51.87765138016309407, 8.698644590117595499, 2.049999999999819522 ) ) ;
#834=CARTESIAN_POINT ( 'NONE',  ( 26.52792526470753387, 5.214288841967440469, 1.949999999999907585 ) ) ;
#843=CARTESIAN_POINT ( 'NONE',  ( 23.07431837327364832, 6.199584068344338839, 2.049999999999582379 ) ) ;
#844=ORIENTED_EDGE ( 'NONE', *, *, #5546, .F. ) ;
#845=CIRCLE ( 'NONE', #15996, 4.500000000000037303 ) ;
#854=CYLINDRICAL_SURFACE ( 'NONE', #8814, 0.09999999999999886757 ) ;
#863=CARTESIAN_POINT ( 'NONE',  ( 54.16616206058712635, 6.839261630856932506, -2.050000000000188560 ) ) ;
#878=ORIENTED_EDGE ( 'NONE', *, *, #12811, .F. ) ;
#880=CARTESIAN_POINT ( 'NONE',  ( 53.90436476239020180, 5.768992244161037952, -1.948923759896386665 ) ) ;
#885=CARTESIAN_POINT ( 'NONE',  ( 30.73039769179424141, 7.037486595895787289, -2.049999999999975842 ) ) ;
#893=CARTESIAN_POINT ( 'NONE',  ( 47.02489528704867894, -3.758556366959797668, 1.867213167016393394 ) ) ;
#894=CARTESIAN_POINT ( 'NONE',  ( 47.20291695880406735, -3.814011388176768769, -1.508225752246980633 ) ) ;
#897=AXIS2_PLACEMENT_3D ( 'NONE', #25108, #28108, #8177 ) ;
#901=FACE_OUTER_BOUND ( 'NONE', #12065, .T. ) ;
#912=CARTESIAN_POINT ( 'NONE',  ( 54.18857573620737611, 5.673640356790727424, 2.049999999999811529 ) ) ;
#944=EDGE_CURVE ( 'NONE', #1060, #23376, #21759, .T. ) ;
#946=LINE ( 'NONE', #17881, #20702 ) ;
#947=CARTESIAN_POINT ( 'NONE',  ( 30.91780351980854746, 7.261267790723114679, 2.049999999999891465 ) ) ;
#948=ORIENTED_EDGE ( 'NONE', *, *, #23612, .F. ) ;
#953=DIRECTION ( 'NONE',  ( -1.000000000000000000, -0.000000000000000000, 3.491481338843133355E-15 ) ) ;
#959=CARTESIAN_POINT ( 'NONE',  ( 29.69543387591359362, 6.938696499881336521, 1.424999999999895683 ) ) ;
#972=CARTESIAN_POINT ( 'NONE',  ( 52.88620718028469980, 4.625382794676526466, -1.578939844535521386 ) ) ;
#980=CARTESIAN_POINT ( 'NONE',  ( 52.86869685578782452, 4.158893372528646104, -2.046892089072104959 ) ) ;
#991=CARTESIAN_POINT ( 'NONE',  ( 54.17703590114060574, 6.867671797591380134, 2.049999999999811084 ) ) ;
#1003=CIRCLE ( 'NONE', #9086, 4.600000000000036948 ) ;
#1006=CARTESIAN_POINT ( 'NONE',  ( 23.93127868632236144, 5.811091648295740875, 2.049999999999915445 ) ) ;
#1023=CARTESIAN_POINT ( 'NONE',  ( 52.14998464476281725, 8.689016205149746597, -2.050000000000180567 ) ) ;
#1026=CARTESIAN_POINT ( 'NONE',  ( 53.61896909490565832, 5.359691232772922476, 1.649479992712508336 ) ) ;
#1033=CARTESIAN_POINT ( 'NONE',  ( 47.49423211416725366, -4.280519502657941899, 1.378181460053769625 ) ) ;
#1034=ORIENTED_EDGE ( 'NONE', *, *, #1460, .T. ) ;
#1036=CARTESIAN_POINT ( 'NONE',  ( 50.80000000000001137, -4.387164041431065087, -1.383037119376935298 ) ) ;
#1038=CARTESIAN_POINT ( 'NONE',  ( 51.74168341169266938, 3.850633047928920139, -1.433002550189482083 ) ) ;
#1046=CARTESIAN_POINT ( 'NONE',  ( 22.04321716858593661, 7.679566743993218481, -1.550000000000076206 ) ) ;
#1047=CARTESIAN_POINT ( 'NONE',  ( 47.00300903693474908, -3.614067288483654661, -1.940243272268905361 ) ) ;
#1052=CARTESIAN_POINT ( 'NONE',  ( 50.91890276716776498, -4.387164036186654847, 1.383037136012494672 ) ) ;
#1056=CARTESIAN_POINT ( 'NONE',  ( 51.80000000000001137, 6.475000000000062705, -1.950000000000180256 ) ) ;
#1059=CARTESIAN_POINT ( 'NONE',  ( 54.30613021257498474, 6.708647431342469325, 2.049999999999810196 ) ) ;
#1060=VERTEX_POINT ( 'NONE', #31298 ) ;
#1089=DIRECTION ( 'NONE',  ( -0.9993908270190953180, 0.03489949670251091263, 4.336808689942080056E-15 ) ) ;
#1092=CARTESIAN_POINT ( 'NONE',  ( 32.25145567989078188, 7.901888653700006593, 2.049999999999887468 ) ) ;
#1099=EDGE_CURVE ( 'NONE', #23396, #4604, #14785, .T. ) ;
#1111=FACE_OUTER_BOUND ( 'NONE', #18843, .T. ) ;
#1117=CARTESIAN_POINT ( 'NONE',  ( 51.38935952926939876, 3.882318105937780928, -2.050000000000178790 ) ) ;
#1122=CARTESIAN_POINT ( 'NONE',  ( 29.69543387591358652, 6.938696499881336521, -1.425000000000103517 ) ) ;
#1130=CIRCLE ( 'NONE', #30969, 0.09999999999999856226 ) ;
#1136=CARTESIAN_POINT ( 'NONE',  ( 54.18071634157382022, 6.868323337799980166, 2.049999999999812861 ) ) ;
#1145=CARTESIAN_POINT ( 'NONE',  ( 32.25672990471646528, 7.797045638327628758, 1.949999999999888267 ) ) ;
#1163=DIRECTION ( 'NONE',  ( 0.9480661539417378769, -0.3180732113053867383, -3.310155284476359054E-15 ) ) ;
#1166=EDGE_CURVE ( 'NONE', #10094, #30563, #15180, .T. ) ;
#1170=EDGE_CURVE ( 'NONE', #7259, #9698, #12636, .T. ) ;
#1183=DIRECTION ( 'NONE',  ( -1.000000000000000000, 0.000000000000000000, 3.491481338843133750E-15 ) ) ;
#1191=DIRECTION ( 'NONE',  ( 0.000000000000000000, -1.000000000000000000, 0.000000000000000000 ) ) ;
#1197=PLANE ( 'NONE',  #14485 ) ;
#1199=CARTESIAN_POINT ( 'NONE',  ( 54.16745733320535550, 5.680725514543202515, 2.049999999999808420 ) ) ;
#1204=CARTESIAN_POINT ( 'NONE',  ( 51.46757676178953034, 4.376162276235350035, 1.549999999999820410 ) ) ;
#1207=CARTESIAN_POINT ( 'NONE',  ( 51.79700381482543747, -3.613796805335215190, -1.940711795749421986 ) ) ;
#1223=AXIS2_PLACEMENT_3D ( 'NONE', #16763, #29089, #9936 ) ;
#1226=ADVANCED_FACE ( 'NONE', ( #16230 ), #21317, .T. ) ;
#1231=CARTESIAN_POINT ( 'NONE',  ( 47.00000000000001421, -3.933368109459638884, -2.186004417993339111 ) ) ;
#1232=CARTESIAN_POINT ( 'NONE',  ( 26.60100329382704487, 5.318777344783313765, 2.049999999999906564 ) ) ;
#1236=FACE_OUTER_BOUND ( 'NONE', #6825, .T. ) ;
#1237=ORIENTED_EDGE ( 'NONE', *, *, #12586, .T. ) ;
#1238=PRODUCT_DEFINITION_CONTEXT ( 'detailed design', #4728, 'design' ) ;
#1242=DIRECTION ( 'NONE',  ( -0.9993908270190957621, 0.03489949670250098307, 3.491481338843133355E-15 ) ) ;
#1247=CARTESIAN_POINT ( 'NONE',  ( 50.93264724376069097, -4.319730106884872356, -1.256953381662414770 ) ) ;
#1258=CARTESIAN_POINT ( 'NONE',  ( 51.75611399313424243, 4.330462468336024884, -1.550000000000180123 ) ) ;
#1263=CARTESIAN_POINT ( 'NONE',  ( 22.72662675107778796, 7.272876594663846284, -1.425000000000078870 ) ) ;
#1265=CARTESIAN_POINT ( 'NONE',  ( 52.99757510872610311, 4.225639836365437496, -2.047297191224516144 ) ) ;
#1279=CARTESIAN_POINT ( 'NONE',  ( 51.65293807187810415, 3.825852911387368493, 2.049999999999816414 ) ) ;
#1291=CARTESIAN_POINT ( 'NONE',  ( 22.57514569326381348, 6.661564121306509101, 1.949999999999920908 ) ) ;
#1312=CARTESIAN_POINT ( 'NONE',  ( 51.89161117884413699, 9.098400920926795976, -1.950000000000180256 ) ) ;
#1338=CARTESIAN_POINT ( 'NONE',  ( 51.80000000000002558, -4.003661535119149129, 1.269131321891737274 ) ) ;
#1339=ORIENTED_EDGE ( 'NONE', *, *, #18345, .T. ) ;
#1343=CARTESIAN_POINT ( 'NONE',  ( 47.76154518333414956, -3.901365292554825892, 1.261477279111806515 ) ) ;
#1345=AXIS2_PLACEMENT_3D ( 'NONE', #1733, #16321, #25967 ) ;
#1354=CARTESIAN_POINT ( 'NONE',  ( 51.60802515543293367, -4.291220349889137253, 1.660930850246465695 ) ) ;
#1355=CIRCLE ( 'NONE', #16537, 4.099999999999992539 ) ;
#1357=CARTESIAN_POINT ( 'NONE',  ( 51.87416143049283335, 8.598705507415685290, -2.050000000000180123 ) ) ;
#1360=DIRECTION ( 'NONE',  ( -3.489354422748178582E-15, 1.218509414717996338E-16, -1.000000000000000000 ) ) ;
#1366=CARTESIAN_POINT ( 'NONE',  ( 51.35619921172967395, -3.851485842263135506, 1.408112718337741764 ) ) ;
#1368=CARTESIAN_POINT ( 'NONE',  ( 51.38935952926941297, 3.882318105937780928, 2.049999999999820410 ) ) ;
#1374=CARTESIAN_POINT ( 'NONE',  ( 29.19131116422931527, 6.114831865242810416, -2.050000000000101963 ) ) ;
#1375=AXIS2_PLACEMENT_3D ( 'NONE', #7074, #21188, #4680 ) ;
#1378=ORIENTED_EDGE ( 'NONE', *, *, #3383, .T. ) ;
#1387=DIRECTION ( 'NONE',  ( 0.9993908270190956511, -0.03489949670250089980, -3.469446951951485842E-15 ) ) ;
#1391=B_SPLINE_CURVE_WITH_KNOTS ( 'NONE', 3,
 ( #3206, #10503, #669, #27577, #2902, #5597, #22237, #3533, #29478, #7793, #1145, #10330, #17463, #24747, #10797, #5435, #3058, #12700, #22380, #20001, #29643, #7969, #24890, #22531, #834, #18109, #9057, #3826, #25366, #3986, #6360, #30417, #18406, #1291, #1599, #25682, #28045, #1754, #20792, #13629 ),
 .UNSPECIFIED., .F., .F.,
 ( 4, 2, 2, 2, 2, 2, 2, 2, 2, 2, 2, 2, 2, 2, 2, 2, 2, 2, 2, 4 ),
 ( -6.000000000463940585E-08, 0.0002197707893516534494, 0.0004396015787033115299, 0.0008792631574066276908, 0.001758586314813259145, 0.002637909472219890274, 0.003077571050923215163, 0.003517232629626540052, 0.004396555787033208477, 0.005275878944439876470, 0.007034525259253204647, 0.007913848416659874374, 0.008793171574066544968, 0.009672494731473213828, 0.01055181788887988442, 0.01143114104628655328, 0.01231046420369322388, 0.01318978736109989273, 0.01362944893980322890, 0.01406911051850656159 ),
 .UNSPECIFIED. ) ;
#1392=ADVANCED_FACE ( 'NONE', ( #28889 ), #8285, .T. ) ;
#1403=DIRECTION ( 'NONE',  ( -1.000000000000000000, 0.000000000000000000, 3.491481338843133355E-15 ) ) ;
#1411=CARTESIAN_POINT ( 'NONE',  ( 30.89639353480225026, 7.705332860780324644, 1.424999999999891687 ) ) ;
#1412=DIRECTION ( 'NONE',  ( -1.000000000000000000, -0.000000000000000000, 3.491481338843133355E-15 ) ) ;
#1427=DIRECTION ( 'NONE',  ( -0.9993908270190957621, 0.03489949670250106634, 3.490838185622846777E-15 ) ) ;
#1438=DIRECTION ( 'NONE',  ( -3.489354422748178188E-15, 1.218509414717996091E-16, -1.000000000000000000 ) ) ;
#1442=CARTESIAN_POINT ( 'NONE',  ( 51.29845177546387447, 3.894758067259834533, 2.049999999999820410 ) ) ;
#1445=B_SPLINE_CURVE_WITH_KNOTS ( 'NONE', 3,
 ( #3476, #20424, #22473, #3151, #8364, #17882, #25459, #10598, #7899, #15502, #8214, #12643, #25314, #17575, #615, #10742, #25158, #1232, #29580, #20275, #13116, #27220, #27851, #22806, #8067, #5533, #947, #6161, #30049, #10276, #3308, #1092, #10437, #10895, #15810, #18047 ),
 .UNSPECIFIED., .F., .F.,
 ( 4, 2, 2, 2, 2, 2, 2, 2, 2, 2, 2, 2, 2, 2, 2, 2, 2, 4 ),
 ( 0.000000000000000000, 0.0004577609249772582344, 0.0009155218499545164689, 0.001373282774931774758, 0.001831043699909032938, 0.002746565549863547780, 0.003662087399818062840, 0.004577609249772577465, 0.005493131099727092959, 0.006408652949681607584, 0.007324174799636122210, 0.009155218499545142788, 0.01007074034949965481, 0.01098626219945416857, 0.01144402312443142111, 0.01190178404940867192, 0.01281730589936317527, 0.01464834959927219932 ),
 .UNSPECIFIED. ) ;
#1446=DIRECTION ( 'NONE',  ( -3.489354422748178582E-15, 1.218509414717996338E-16, -1.000000000000000000 ) ) ;
#1460=EDGE_CURVE ( 'NONE', #23119, #21532, #3754, .T. ) ;
#1463=CARTESIAN_POINT ( 'NONE',  ( 31.18344400622543233, 7.296549944477582095, -1.425000000000107958 ) ) ;
#1466=CARTESIAN_POINT ( 'NONE',  ( 51.80000000000001847, 6.982261990806648555E-14, -1.796574372350448449E-13 ) ) ;
#1467=CARTESIAN_POINT ( 'NONE',  ( 51.80000000000001847, 6.982261990806648555E-14, -1.796574372350448449E-13 ) ) ;
#1469=LINE ( 'NONE', #18587, #22573 ) ;
#1482=AXIS2_PLACEMENT_3D ( 'NONE', #11066, #27699, #1242 ) ;
#1495=CARTESIAN_POINT ( 'NONE',  ( 22.41225425035812435, 6.886225699534504585, -1.950000000000111644 ) ) ;
#1499=ORIENTED_EDGE ( 'NONE', *, *, #14118, .F. ) ;
#1514=CYLINDRICAL_SURFACE ( 'NONE', #25070, 0.1000000000000000472 ) ;
#1516=CARTESIAN_POINT ( 'NONE',  ( 54.33851261602290350, 5.996233363966824825, -2.046523645606439956 ) ) ;
#1518=CARTESIAN_POINT ( 'NONE',  ( 51.80000000000003979, -3.550773357292059007, 2.049880134335640758 ) ) ;
#1519=AXIS2_PLACEMENT_3D ( 'NONE', #7836, #1183, #10841 ) ;
#1521=CARTESIAN_POINT ( 'NONE',  ( 54.16188382698978643, 6.950389949135505674, 2.049999999999811084 ) ) ;
#1526=EDGE_CURVE ( 'NONE', #7829, #23041, #4725, .T. ) ;
#1544=DIRECTION ( 'NONE',  ( -0.9993908270190956511, 0.03489949670250096919, 3.491481338843132961E-15 ) ) ;
#1552=CARTESIAN_POINT ( 'NONE',  ( 51.87765138016309407, 8.698644590117595499, 2.049999999999819522 ) ) ;
#1568=CARTESIAN_POINT ( 'NONE',  ( 53.29713869289653871, 4.966949757952739297, -1.611981027863837790 ) ) ;
#1576=CARTESIAN_POINT ( 'NONE',  ( 21.97322666366010324, 8.076925076899300393, -1.950000000000076117 ) ) ;
#1580=CARTESIAN_POINT ( 'NONE',  ( 47.54430904983911432, -4.350592967663754251, -1.494824413850514011 ) ) ;
#1583=ORIENTED_EDGE ( 'NONE', *, *, #24855, .T. ) ;
#1590=CARTESIAN_POINT ( 'NONE',  ( 54.21235476094170735, 5.862613896911504696, 2.049999999999810640 ) ) ;
#1596=B_SPLINE_CURVE_WITH_KNOTS ( 'NONE', 3,
 ( #27344, #15465, #24658, #10401, #29721, #24954, #10862, #3450 ),
 .UNSPECIFIED., .F., .F.,
 ( 4, 2, 2, 4 ),
 ( 0.000000000000000000, 5.497193010381665759E-05, 0.0001099438602076330306, 0.0002198877204152543789 ),
 .UNSPECIFIED. ) ;
#1599=CARTESIAN_POINT ( 'NONE',  ( 22.38053502801890104, 6.905764555043880648, 1.949999999999922018 ) ) ;
#1605=CIRCLE ( 'NONE', #23373, 0.1000000000000000472 ) ;
#1616=FACE_OUTER_BOUND ( 'NONE', #7253, .T. ) ;
#1621=DIRECTION ( 'NONE',  ( 3.491481338843133355E-15, 0.000000000000000000, 1.000000000000000000 ) ) ;
#1623=( NAMED_UNIT ( * ) SI_UNIT ( $, .STERADIAN. ) SOLID_ANGLE_UNIT ( ) );
#1624=EDGE_CURVE ( 'NONE', #320, #12157, #2991, .T. ) ;
#1631=CARTESIAN_POINT ( 'NONE',  ( 51.58839176096986989, -4.227734780419154070, -1.816236823409610679 ) ) ;
#1634=DIRECTION ( 'NONE',  ( 0.000000000000000000, 0.000000000000000000, -1.000000000000000000 ) ) ;
#1636=CARTESIAN_POINT ( 'NONE',  ( 24.76493886329395977, 5.404133871416555657, -1.950000000000151390 ) ) ;
#1637=AXIS2_PLACEMENT_3D ( 'NONE', #28074, #3564, #25711 ) ;
#1642=ADVANCED_FACE ( 'NONE', ( #22317 ), #27005, .T. ) ;
#1651=CARTESIAN_POINT ( 'NONE',  ( 51.52218784613614844, -4.266866293145943345, 1.720819027621672381 ) ) ;
#1665=CARTESIAN_POINT ( 'NONE',  ( 53.90340377275681760, 6.895264694547793560, 2.049999999999684963 ) ) ;
#1678=DIRECTION ( 'NONE',  ( 9.754918421198722508E-16, 0.9601771338024398528, 0.2793919678926571337 ) ) ;
#1679=ORIENTED_EDGE ( 'NONE', *, *, #5046, .F. ) ;
#1693=CARTESIAN_POINT ( 'NONE',  ( 54.34016439512038943, 6.711820450561376994, -2.050000000000188116 ) ) ;
#1712=CARTESIAN_POINT ( 'NONE',  ( 50.31971926781695004, 8.252744006147214151, 2.049999999999824407 ) ) ;
#1733=CARTESIAN_POINT ( 'NONE',  ( 51.80000000000001847, 2.428612866367529932E-14, -1.808587333520743709E-13 ) ) ;
#1736=DIRECTION ( 'NONE',  ( 0.9993908270190956511, -0.03489949670250096919, -3.491481338843132961E-15 ) ) ;
#1754=CARTESIAN_POINT ( 'NONE',  ( 22.01652470039608289, 7.767688062055312592, 1.949999999999924016 ) ) ;
#1756=ORIENTED_EDGE ( 'NONE', *, *, #1170, .F. ) ;
#1768=CARTESIAN_POINT ( 'NONE',  ( 51.70000000000002416, 2.428612866367529932E-14, -1.805095852181900386E-13 ) ) ;
#1796=DIRECTION ( 'NONE',  ( 0.000000000000000000, 0.000000000000000000, -1.000000000000000000 ) ) ;
#1812=CARTESIAN_POINT ( 'NONE',  ( 50.80000000000001847, -3.936726248589971444, -1.145507068360071434 ) ) ;
#1819=LINE ( 'NONE', #30472, #24589 ) ;
#1824=CARTESIAN_POINT ( 'NONE',  ( 51.80000000000001137, -4.003661535119149129, -1.269131321892099207 ) ) ;
#1829=EDGE_CURVE ( 'NONE', #7143, #11640, #11722, .T. ) ;
#1833=CARTESIAN_POINT ( 'NONE',  ( 51.74555621289474061, 3.825902093565871631, 2.049999999999819522 ) ) ;
#1846=CARTESIAN_POINT ( 'NONE',  ( 53.42585677208777639, 7.844055467211287436, 1.880068497670932537 ) ) ;
#1852=VECTOR ( 'NONE', #28973, 1000.000000000000000 ) ;
#1870=CARTESIAN_POINT ( 'NONE',  ( 54.41366571437519184, 6.718673005292170153, -1.976179938780096013 ) ) ;
#1880=CARTESIAN_POINT ( 'NONE',  ( 51.67753520601183936, -4.133513435957371307, -2.021478398489999329 ) ) ;
#1887=CARTESIAN_POINT ( 'NONE',  ( 51.80000000000001137, -3.995259070520241540, -2.068697874512001267 ) ) ;
#1888=CARTESIAN_POINT ( 'NONE',  ( 47.07708546080149858, 8.766223091587903582, 1.549999999999835953 ) ) ;
#1918=FACE_OUTER_BOUND ( 'NONE', #16878, .T. ) ;
#1927=ORIENTED_EDGE ( 'NONE', *, *, #30575, .T. ) ;
#1930=EDGE_CURVE ( 'NONE', #12841, #15664, #7354, .T. ) ;
#1947=CARTESIAN_POINT ( 'NONE',  ( 48.00000000000001421, -4.416814815491191482, -1.285203052306389981 ) ) ;
#1948=DIRECTION ( 'NONE',  ( -0.6819983600625022513, 0.7313537016191670181, 2.468850131082277965E-15 ) ) ;
#1950=DIRECTION ( 'NONE',  ( -1.000000000000000000, -0.000000000000000000, 3.491481338843133355E-15 ) ) ;
#1954=CARTESIAN_POINT ( 'NONE',  ( 52.78861517463008823, 8.494192748968428575, 2.049999999999816858 ) ) ;
#1960=DIRECTION ( 'NONE',  ( 3.491481338843133355E-15, -0.000000000000000000, 1.000000000000000000 ) ) ;
#1996=CARTESIAN_POINT ( 'NONE',  ( 53.66376481541393417, 4.683274397263343047, 2.049999999999812861 ) ) ;
#2000=ORIENTED_EDGE ( 'NONE', *, *, #3617, .F. ) ;
#2004=FACE_OUTER_BOUND ( 'NONE', #18517, .T. ) ;
#2006=VERTEX_POINT ( 'NONE', #29820 ) ;
#2010=CARTESIAN_POINT ( 'NONE',  ( 53.78583825613542757, 7.269801125715066092, 1.827185152435081283 ) ) ;
#2013=CARTESIAN_POINT ( 'NONE',  ( 47.54047041873123902, -4.349936135048430685, 1.496764967786690326 ) ) ;
#2031=DIRECTION ( 'NONE',  ( 0.04332611568076707997, -0.9990609829735204173, 0.000000000000000000 ) ) ;
#2036=CARTESIAN_POINT ( 'NONE',  ( 53.91574522233626965, 6.672251602764244893, -1.774295313897662485 ) ) ;
#2042=ORIENTED_EDGE ( 'NONE', *, *, #646, .T. ) ;
#2049=CARTESIAN_POINT ( 'NONE',  ( 31.58270314793947620, 7.514175884156568230, 1.424999999999890132 ) ) ;
#2053=CARTESIAN_POINT ( 'NONE',  ( 51.80000000000002558, -3.637377585518695611, 2.099877210782855830 ) ) ;
#2063=CARTESIAN_POINT ( 'NONE',  ( 47.00000000000000711, -3.994423162662119609, -2.070282222600184685 ) ) ;
#2068=CARTESIAN_POINT ( 'NONE',  ( 54.26434950415730896, 6.004763229855418771, -2.050000000000188560 ) ) ;
#2070=CARTESIAN_POINT ( 'NONE',  ( 47.10000000000002274, 2.428612866367529932E-14, -1.644487710595116631E-13 ) ) ;
#2086=ORIENTED_EDGE ( 'NONE', *, *, #25090, .T. ) ;
#2091=AXIS2_PLACEMENT_3D ( 'NONE', #30693, #30853, #6778 ) ;
#2096=CARTESIAN_POINT ( 'NONE',  ( 47.10000000000002274, 6.982261990806648555E-14, -1.632474749424821370E-13 ) ) ;
#2106=CARTESIAN_POINT ( 'NONE',  ( 54.20407241913904528, 5.668441268431575253, -2.050000000000189004 ) ) ;
#2118=CARTESIAN_POINT ( 'NONE',  ( 51.80056040574818610, 4.600011524547849895, -0.2639097402654416724 ) ) ;
#2132=ADVANCED_BREP_SHAPE_REPRESENTATION ( '', ( #25333, #9018 ), #22713 ) ;
#2147=CARTESIAN_POINT ( 'NONE',  ( 54.23701917430469877, 5.946187982713466269, 2.049999999999810640 ) ) ;
#2148=AXIS2_PLACEMENT_3D ( 'NONE', #14226, #29110, #24216 ) ;
#2152=ORIENTED_EDGE ( 'NONE', *, *, #24073, .T. ) ;
#2154=ORIENTED_EDGE ( 'NONE', *, *, #14114, .T. ) ;
#2176=CARTESIAN_POINT ( 'NONE',  ( 53.81464057712625504, 5.799094425976106137, 0.8364386040616162976 ) ) ;
#2185=DIRECTION ( 'NONE',  ( 3.489354422748178582E-15, -1.218509414717996338E-16, 1.000000000000000000 ) ) ;
#2186=EDGE_CURVE ( 'NONE', #22413, #3208, #15560, .T. ) ;
#2235=EDGE_CURVE ( 'NONE', #22264, #27880, #25361, .T. ) ;
#2247=EDGE_CURVE ( 'NONE', #28320, #20006, #21853, .T. ) ;
#2248=EDGE_CURVE ( 'NONE', #9056, #12796, #6654, .T. ) ;
#2259=CARTESIAN_POINT ( 'NONE',  ( 54.40859250694163052, 6.718200028317722783, -1.988253509196054036 ) ) ;
#2267=B_SPLINE_CURVE_WITH_KNOTS ( 'NONE', 3,
 ( #9388, #7175, #4477, #21599, #14128, #11759, #23803, #16515 ),
 .UNSPECIFIED., .F., .F.,
 ( 4, 2, 2, 4 ),
 ( 0.000000000000000000, 0.0001089356377969812170, 0.0001634034566954674752, 0.0002178712755939534894 ),
 .UNSPECIFIED. ) ;
#2272=CARTESIAN_POINT ( 'NONE',  ( 51.83526099861352776, 4.481294105856048482, -1.046211687970766580 ) ) ;
#2280=CARTESIAN_POINT ( 'NONE',  ( 31.37624803221882175, 7.388935654832296862, 1.949999999999890710 ) ) ;
#2292=CARTESIAN_POINT ( 'NONE',  ( 50.87477060347629987, 8.633605004120575188, -1.550000000000176792 ) ) ;
#2294=EDGE_CURVE ( 'NONE', #10074, #9283, #26165, .T. ) ;
#2304=CARTESIAN_POINT ( 'NONE',  ( 53.90445947017991557, 7.548890922513427526, 2.049999999999810196 ) ) ;
#2307=DIRECTION ( 'NONE',  ( -0.8787808829753843698, -0.4772254810013855097, 3.008227586482355247E-15 ) ) ;
#2313=CARTESIAN_POINT ( 'NONE',  ( 22.09275828236362571, 6.785783592403104691, 1.949999999999922018 ) ) ;
#2319=CARTESIAN_POINT ( 'NONE',  ( 53.88560544134391961, 6.996383340473027346, 1.802989201814990894 ) ) ;
#2323=CARTESIAN_POINT ( 'NONE',  ( 47.20956584626475916, -4.226158602834445333, 1.819860353018571297 ) ) ;
#2330=DIRECTION ( 'NONE',  ( 0.000000000000000000, 0.000000000000000000, -1.000000000000000000 ) ) ;
#2351=TOROIDAL_SURFACE ( 'NONE', #20062, 160.5997717543497743, 0.1000000000000000056 ) ;
#2367=DIRECTION ( 'NONE',  ( 0.000000000000000000, -1.000000000000000000, 0.000000000000000000 ) ) ;
#2368=VECTOR ( 'NONE', #12525, 1000.000000000000000 ) ;
#2375=CARTESIAN_POINT ( 'NONE',  ( 51.88812122917229175, 8.998461838226505805, -1.950000000000180256 ) ) ;
#2386=CARTESIAN_POINT ( 'NONE',  ( 24.34823467037697498, 5.521868380698618850, 1.424999999999915445 ) ) ;
#2408=FILL_AREA_STYLE ('',( #29154 ) ) ;
#2414=CARTESIAN_POINT ( 'NONE',  ( 53.90445947017990136, 7.548890922513427526, -2.050000000000186784 ) ) ;
#2415=DIRECTION ( 'NONE',  ( 3.489354422748178582E-15, -1.218509414717996338E-16, 1.000000000000000000 ) ) ;
#2433=EDGE_CURVE ( 'NONE', #25954, #30783, #4549, .T. ) ;
#2434=CARTESIAN_POINT ( 'NONE',  ( 54.31978947732369534, 6.362875530773669297, -2.050000000000190781 ) ) ;
#2438=CARTESIAN_POINT ( 'NONE',  ( 22.72662675107779506, 7.272876594663846284, 1.424999999999921219 ) ) ;
#2440=ORIENTED_EDGE ( 'NONE', *, *, #18349, .T. ) ;
#2452=CARTESIAN_POINT ( 'NONE',  ( 29.24156346100637549, 6.028130203020907629, 2.050000000000804512 ) ) ;
#2469=CIRCLE ( 'NONE', #20182, 0.09999999999999942268 ) ;
#2472=AXIS2_PLACEMENT_3D ( 'NONE', #17817, #5768, #15421 ) ;
#2494=CARTESIAN_POINT ( 'NONE',  ( 52.72267294271966165, 4.003822062839299534, -2.050000000000183675 ) ) ;
#2501=VECTOR ( 'NONE', #3103, 1000.000000000000000 ) ;
#2520=CARTESIAN_POINT ( 'NONE',  ( 50.87477060347373481, 8.633605004118187765, -2.050000000000176570 ) ) ;
#2539=DIRECTION ( 'NONE',  ( 0.03489949670185131525, 0.9993908270191184107, 0.000000000000000000 ) ) ;
#2541=AXIS2_PLACEMENT_3D ( 'NONE', #26876, #7865, #281 ) ;
#2543=CARTESIAN_POINT ( 'NONE',  ( 53.37676683120072596, 7.899656915230087506, -1.885229198846103404 ) ) ;
#2547=CARTESIAN_POINT ( 'NONE',  ( 51.70000000000003126, -3.550773357292059007, 2.049880134335640758 ) ) ;
#2548=CARTESIAN_POINT ( 'NONE',  ( 26.18134456910377494, 5.211034382732834480, 1.424999999999908562 ) ) ;
#2550=ORIENTED_EDGE ( 'NONE', *, *, #14624, .T. ) ;
#2563=DIRECTION ( 'NONE',  ( -1.000000000000000000, -0.000000000000000000, 3.491481338843133355E-15 ) ) ;
#2577=CARTESIAN_POINT ( 'NONE',  ( 31.35411506832756601, 7.935106539446550755, -1.425000000000109068 ) ) ;
#2580=CARTESIAN_POINT ( 'NONE',  ( 51.70000000000002416, 2.428612866367529932E-14, -1.805095852181900386E-13 ) ) ;
#2590=CARTESIAN_POINT ( 'NONE',  ( 52.50881341635840727, 3.945078575635807550, 1.125510014975697803 ) ) ;
#2595=CARTESIAN_POINT ( 'NONE',  ( 26.19155409318043937, 5.638511060912940742, 1.424999999999908784 ) ) ;
#2598=DIRECTION ( 'NONE',  ( -1.000000000000000000, -0.000000000000000000, 3.491481338843133355E-15 ) ) ;
#2606=CARTESIAN_POINT ( 'NONE',  ( 30.73039769179423786, 7.037486595896031538, 2.050000000000022915 ) ) ;
#2620=CARTESIAN_POINT ( 'NONE',  ( 53.78456803694547972, 5.661108390837235937, 2.049999999999812417 ) ) ;
#2621=ORIENTED_EDGE ( 'NONE', *, *, #6295, .T. ) ;
#2627=DIRECTION ( 'NONE',  ( 0.03489949670185131525, 0.9993908270191184107, 0.000000000000000000 ) ) ;
#2629=ORIENTED_EDGE ( 'NONE', *, *, #16126, .T. ) ;
#2631=CARTESIAN_POINT ( 'NONE',  ( 22.07280086217093640, 8.086143481909148889, -2.050000000000076650 ) ) ;
#2636=FACE_OUTER_BOUND ( 'NONE', #23492, .T. ) ;
#2644=CARTESIAN_POINT ( 'NONE',  ( 53.60009913848111296, 4.619321414059949227, -2.050000000000186784 ) ) ;
#2645=CARTESIAN_POINT ( 'NONE',  ( 22.07280086217093640, 8.086143481909152442, -1.950000000000076339 ) ) ;
#2651=EDGE_CURVE ( 'NONE', #11471, #3677, #1003, .T. ) ;
#2655=EDGE_CURVE ( 'NONE', #18673, #13278, #9522, .T. ) ;
#2665=CARTESIAN_POINT ( 'NONE',  ( 51.70000000000003126, -4.079448311123456961, 2.129011300494053849 ) ) ;
#2666=CARTESIAN_POINT ( 'NONE',  ( 51.70000000000003126, -3.637377585518695611, 2.099877210782855830 ) ) ;
#2674=CARTESIAN_POINT ( 'NONE',  ( 51.80000000000001137, 3.850000000000016520, -1.678541033159632434 ) ) ;
#2683=ADVANCED_FACE ( 'NONE', ( #19013 ), #14972, .F. ) ;
#2685=CARTESIAN_POINT ( 'NONE',  ( 30.88580673845696722, 7.128392828669079861, -1.950000000000106315 ) ) ;
#2687=CYLINDRICAL_SURFACE ( 'NONE', #21556, 4.099999999999992539 ) ;
#2690=CARTESIAN_POINT ( 'NONE',  ( 51.80000000000002558, 4.350000000000017408, 1.550321101314541927 ) ) ;
#2711=EDGE_CURVE ( 'NONE', #12883, #7683, #19205, .T. ) ;
#2714=CARTESIAN_POINT ( 'NONE',  ( 53.66827364943466705, 4.678978782231800082, -2.050000000000186784 ) ) ;
#2728=CARTESIAN_POINT ( 'NONE',  ( 51.99335957375618023, 4.356869014081647506, -1.476207528374383848 ) ) ;
#2729=CARTESIAN_POINT ( 'NONE',  ( 51.77508801986071063, 3.850110376304356929, 1.503046890130784519 ) ) ;
#2732=CARTESIAN_POINT ( 'NONE',  ( 47.02556836852575373, -4.052038242240619148, 1.950335525115682644 ) ) ;
#2733=ORIENTED_EDGE ( 'NONE', *, *, #25922, .T. ) ;
#2743=CARTESIAN_POINT ( 'NONE',  ( 51.94457537908208167, 4.389362525834665796, 1.376356216334040372 ) ) ;
#2762=CARTESIAN_POINT ( 'NONE',  ( 52.45567523936536958, 8.517307475678970619, 1.943109374214545770 ) ) ;
#2774=CARTESIAN_POINT ( 'NONE',  ( 53.94302949310494455, 6.378738071910782459, -1.816235364411796116 ) ) ;
#2776=CARTESIAN_POINT ( 'NONE',  ( 29.25706191173315673, 5.994885333997870269, -1.950000000000101652 ) ) ;
#2781=CARTESIAN_POINT ( 'NONE',  ( 51.89798357584853505, 4.350000000000017408, 1.495827530165568575 ) ) ;
#2786=CARTESIAN_POINT ( 'NONE',  ( 53.82520270936414875, 4.899646637710924679, -2.050000000000188116 ) ) ;
#2796=CARTESIAN_POINT ( 'NONE',  ( 54.18130252701728722, 6.361998095200566361, 2.049999999999792877 ) ) ;
#2803=DIRECTION ( 'NONE',  ( 0.000000000000000000, 0.8660422822663634834, 0.4999707644721521627 ) ) ;
#2810=CARTESIAN_POINT ( 'NONE',  ( 53.74996364474760924, 4.800585817144076728, 2.049999999999812417 ) ) ;
#2828=CARTESIAN_POINT ( 'NONE',  ( 28.59102362472352965, 5.695743087063649845, -1.950000000000098321 ) ) ;
#2830=EDGE_CURVE ( 'NONE', #20869, #3677, #30002, .T. ) ;
#2836=CARTESIAN_POINT ( 'NONE',  ( 31.18344400622541812, 7.296549944477567884, 1.424999999999891243 ) ) ;
#2845=FACE_OUTER_BOUND ( 'NONE', #3900, .T. ) ;
#2853=CARTESIAN_POINT ( 'NONE',  ( 51.80000000000001137, 4.350000000000017408, -1.495827530165608321 ) ) ;
#2854=ORIENTED_EDGE ( 'NONE', *, *, #3100, .T. ) ;
#2870=CARTESIAN_POINT ( 'NONE',  ( 52.11563210330034224, 3.836792880204552336, -2.050000000000181455 ) ) ;
#2874=CIRCLE ( 'NONE', #24613, 0.1000000000000000472 ) ;
#2882=EDGE_LOOP ( 'NONE', ( #21093, #25984, #3642, #25836 ) ) ;
#2887=DIRECTION ( 'NONE',  ( -0.9480661539417394312, 0.3180732113053816867, 0.000000000000000000 ) ) ;
#2888=CARTESIAN_POINT ( 'NONE',  ( 47.54437363841991271, -4.350642226022881864, 1.494686490729194572 ) ) ;
#2902=CARTESIAN_POINT ( 'NONE',  ( 34.19605798823444331, 8.191999290087634833, 1.949999999999880940 ) ) ;
#2909=FACE_OUTER_BOUND ( 'NONE', #16028, .T. ) ;
#2927=CARTESIAN_POINT ( 'NONE',  ( 41.48619405472010868, -151.3359592902261852, 1.549999999999835953 ) ) ;
#2928=CARTESIAN_POINT ( 'NONE',  ( 52.16611735465140498, 8.588510181886395145, 1.949999998429079895 ) ) ;
#2932=ORIENTED_EDGE ( 'NONE', *, *, #610, .F. ) ;
#2936=FACE_OUTER_BOUND ( 'NONE', #18568, .T. ) ;
#2939=ORIENTED_EDGE ( 'NONE', *, *, #22956, .F. ) ;
#2940=CARTESIAN_POINT ( 'NONE',  ( 54.15683185445048764, 5.684290329229592764, -2.050000000000188560 ) ) ;
#2943=CARTESIAN_POINT ( 'NONE',  ( 22.09275828236361150, 6.785783592403105580, -1.950000000000076783 ) ) ;
#2945=CARTESIAN_POINT ( 'NONE',  ( 31.77414890219379373, 7.582826004857478708, -1.950000000000077671 ) ) ;
#2947=DIRECTION ( 'NONE',  ( 3.491481338843133355E-15, 0.000000000000000000, 1.000000000000000000 ) ) ;
#2952=CARTESIAN_POINT ( 'NONE',  ( 53.05417955289645704, 8.376364939874980209, -2.050000000000184563 ) ) ;
#2953=DIRECTION ( 'NONE',  ( 3.016910393003118404E-15, 1.776356839400249479E-15, 1.000000000000000000 ) ) ;
#2965=CARTESIAN_POINT ( 'NONE',  ( 54.35699702479112716, 6.713389762748565914, 2.043118800226060294 ) ) ;
#2966=EDGE_LOOP ( 'NONE', ( #7230, #4325, #17494, #23908, #15032, #23931, #24621, #3742, #16342, #6386, #7783, #411, #1237, #24829, #29363, #13803 ) ) ;
#2973=CARTESIAN_POINT ( 'NONE',  ( 22.04321716858594371, 7.679566743993215816, 1.424999999999923661 ) ) ;
#2974=CARTESIAN_POINT ( 'NONE',  ( 27.72148966843209550, 5.417328426838181166, 1.424999999999903233 ) ) ;
#2975=EDGE_CURVE ( 'NONE', #11640, #26805, #3884, .T. ) ;
#2988=LINE ( 'NONE', #10262, #6885 ) ;
#2990=PRODUCT_DEFINITION_SHAPE ( 'NONE', 'NONE',  #27331 ) ;
#2991=LINE ( 'NONE', #26890, #21480 ) ;
#2997=DIRECTION ( 'NONE',  ( 3.384826294588897856E-15, 0.000000000000000000, 1.000000000000000000 ) ) ;
#3013=CARTESIAN_POINT ( 'NONE',  ( 47.19776093000137962, -3.901712759401290143, 1.540267080487876861 ) ) ;
#3025=CARTESIAN_POINT ( 'NONE',  ( 52.80835374156198014, 4.037528258991556207, -2.050000000000183675 ) ) ;
#3039=EDGE_CURVE ( 'NONE', #28320, #17715, #15129, .T. ) ;
#3045=CARTESIAN_POINT ( 'NONE',  ( 51.87760527554365808, 3.845134623358581472, 1.423141017617783444 ) ) ;
#3058=CARTESIAN_POINT ( 'NONE',  ( 30.65165540517411813, 6.989120292443193883, 1.949999999999893152 ) ) ;
#3063=CARTESIAN_POINT ( 'NONE',  ( 23.33428888190691453, 6.022557145544392476, 1.949999999999984190 ) ) ;
#3066=CARTESIAN_POINT ( 'NONE',  ( 54.13382992866385024, 5.521407779354435164, -2.050000000000187672 ) ) ;
#3068=CARTESIAN_POINT ( 'NONE',  ( 51.70000000000003126, -4.020776289669855785, 2.234582293948397691 ) ) ;
#3078=CARTESIAN_POINT ( 'NONE',  ( 52.41172327503544182, 8.636713207008101634, -2.050000000000181455 ) ) ;
#3079=ORIENTED_EDGE ( 'NONE', *, *, #6579, .T. ) ;
#3085=DIRECTION ( 'NONE',  ( 0.000000000000000000, 0.2793919678926571892, -0.9601771338024398528 ) ) ;
#3089=CARTESIAN_POINT ( 'NONE',  ( 54.07867252728983942, 6.687441468603865680, -2.033313965204277540 ) ) ;
#3093=CARTESIAN_POINT ( 'NONE',  ( 26.92903764425373581, 5.249711979700405706, -2.050000000000161915 ) ) ;
#3099=CARTESIAN_POINT ( 'NONE',  ( 53.93929004300591856, 7.474130129650688126, -2.050000000000187228 ) ) ;
#3100=EDGE_CURVE ( 'NONE', #20522, #3896, #4349, .T. ) ;
#3101=CARTESIAN_POINT ( 'NONE',  ( 47.86868016046713592, -3.937842567657670489, -1.145831922971770611 ) ) ;
#3103=DIRECTION ( 'NONE',  ( -1.000000000000000000, -0.000000000000000000, 3.491481338843133355E-15 ) ) ;
#3115=CARTESIAN_POINT ( 'NONE',  ( 54.27563121892215747, 6.003154427583493380, 2.049999999999808420 ) ) ;
#3132=PLANE ( 'NONE',  #8991 ) ;
#3134=DIRECTION ( 'NONE',  ( -1.000000000000000000, 0.000000000000000000, 3.491481338843133355E-15 ) ) ;
#3151=CARTESIAN_POINT ( 'NONE',  ( 22.20323573143550178, 7.488806638634509127, 2.049999999999922107 ) ) ;
#3181=DIRECTION ( 'NONE',  ( 1.000000000000000000, 0.000000000000000000, -3.491481338843133355E-15 ) ) ;
#3188=FACE_OUTER_BOUND ( 'NONE', #26019, .T. ) ;
#3194=CARTESIAN_POINT ( 'NONE',  ( 47.44420282665343080, -4.328226263800974749, 1.560066312054830151 ) ) ;
#3201=EDGE_CURVE ( 'NONE', #3677, #20124, #24572, .T. ) ;
#3206=CARTESIAN_POINT ( 'NONE',  ( 34.56702326949726256, 8.213851659285209550, 1.949999999999879385 ) ) ;
#3208=VERTEX_POINT ( 'NONE', #13307 ) ;
#3214=CARTESIAN_POINT ( 'NONE',  ( 24.21299357973638067, 5.692280404211449429, 2.049999999999915001 ) ) ;
#3215=ORIENTED_EDGE ( 'NONE', *, *, #27783, .F. ) ;
#3217=B_SPLINE_CURVE_WITH_KNOTS ( 'NONE', 3,
 ( #3981, #7155, #13936, #23935 ),
 .UNSPECIFIED., .F., .F.,
 ( 4, 4 ),
 ( 0.1946945739040590595, 0.4911851874284507424 ),
 .UNSPECIFIED. ) ;
#3227=CARTESIAN_POINT ( 'NONE',  ( 51.80000000000003979, 2.428612866367529932E-14, 4.199999999999811884 ) ) ;
#3230=EDGE_CURVE ( 'NONE', #23119, #11471, #5677, .T. ) ;
#3245=CARTESIAN_POINT ( 'NONE',  ( 50.80000000000001847, -4.417905791132255899, -1.285520503972919615 ) ) ;
#3249=CARTESIAN_POINT ( 'NONE',  ( 31.50816695980852700, 7.454773700473188214, -2.050000000000237854 ) ) ;
#3271=CARTESIAN_POINT ( 'NONE',  ( 51.70000000000002416, 2.428612866367529932E-14, -1.805095852181900386E-13 ) ) ;
#3272=CARTESIAN_POINT ( 'NONE',  ( 54.28362898602030384, 5.641750290588808170, 1.990863471608376845 ) ) ;
#3278=LINE ( 'NONE', #12924, #23405 ) ;
#3279=CARTESIAN_POINT ( 'NONE',  ( 51.36025231009421788, -4.327031471043523148, 1.563408443048849072 ) ) ;
#3280=CARTESIAN_POINT ( 'NONE',  ( 51.77510471295143901, -3.758556366959755035, -1.867213167016891218 ) ) ;
#3287=CARTESIAN_POINT ( 'NONE',  ( 53.96142581635486124, 5.170113101904351360, 2.049999999999811529 ) ) ;
#3308=CARTESIAN_POINT ( 'NONE',  ( 31.84510612492130122, 7.726745150394289219, 2.049999999999887468 ) ) ;
#3322=CARTESIAN_POINT ( 'NONE',  ( 27.62808879389202588, 5.849836810644521989, 1.424999999999903011 ) ) ;
#3338=CARTESIAN_POINT ( 'NONE',  ( 51.80000000000001137, 8.700707106781294442, -2.050000000000180123 ) ) ;
#3349=CARTESIAN_POINT ( 'NONE',  ( 52.07304482952998370, 3.932152442337120579, -2.045338529774464398 ) ) ;
#3360=CARTESIAN_POINT ( 'NONE',  ( 51.87416143049284045, 8.598705507415683513, 2.049999999999819522 ) ) ;
#3380=CARTESIAN_POINT ( 'NONE',  ( 22.10122560051324569, 7.779108733371196571, 2.049999999999922551 ) ) ;
#3383=EDGE_CURVE ( 'NONE', #16857, #7964, #4085, .T. ) ;
#3405=ORIENTED_EDGE ( 'NONE', *, *, #17202, .T. ) ;
#3411=DIRECTION ( 'NONE',  ( 3.384826294588897856E-15, 0.000000000000000000, 1.000000000000000000 ) ) ;
#3415=EDGE_CURVE ( 'NONE', #2006, #26664, #24196, .T. ) ;
#3416=ORIENTED_EDGE ( 'NONE', *, *, #119, .T. ) ;
#3420=CARTESIAN_POINT ( 'NONE',  ( 51.74859327566192491, 3.850496488340269696, -1.443897952417738439 ) ) ;
#3422=CARTESIAN_POINT ( 'NONE',  ( 22.79271333219223550, 6.591595603790847413, -2.050000000000079758 ) ) ;
#3429=CARTESIAN_POINT ( 'NONE',  ( 47.38487367463270061, -3.877460150898551561, 1.337636034593590484 ) ) ;
#3430=CARTESIAN_POINT ( 'NONE',  ( 47.10000000000000853, -3.550773357292059007, -2.049880134335985815 ) ) ;
#3435=CARTESIAN_POINT ( 'NONE',  ( 51.30892234234251248, -4.380148595134231826, 1.408962902656405891 ) ) ;
#3436=EDGE_CURVE ( 'NONE', #12157, #30563, #302, .T. ) ;
#3443=CARTESIAN_POINT ( 'NONE',  ( 54.22840347875643374, 6.361164334018160282, 2.049999999999810640 ) ) ;
#3447=AXIS2_PLACEMENT_3D ( 'NONE', #29247, #7845, #5019 ) ;
#3450=CARTESIAN_POINT ( 'NONE',  ( 51.80000048029783244, 4.021162535479849254, 2.019963026417355589 ) ) ;
#3453=CYLINDRICAL_SURFACE ( 'NONE', #24127, 2.125000000000048850 ) ;
#3476=CARTESIAN_POINT ( 'NONE',  ( 22.07280086217095061, 8.086143481909148889, 2.049999999999922995 ) ) ;
#3497=CARTESIAN_POINT ( 'NONE',  ( 53.81457038983117513, 5.799118250651475570, -1.689328355159275041 ) ) ;
#3500=CARTESIAN_POINT ( 'NONE',  ( 53.89553379148907197, 6.017104844469305824, -1.708828125785526675 ) ) ;
#3508=FACE_OUTER_BOUND ( 'NONE', #29871, .T. ) ;
#3518=CARTESIAN_POINT ( 'NONE',  ( 51.80000000000001847, 2.428612866367529932E-14, -1.808587333520743709E-13 ) ) ;
#3520=ORIENTED_EDGE ( 'NONE', *, *, #566, .T. ) ;
#3521=CARTESIAN_POINT ( 'NONE',  ( 52.48739568812350598, 8.621481665389278959, 2.049999999999817302 ) ) ;
#3525=VECTOR ( 'NONE', #13585, 1000.000000000000000 ) ;
#3533=CARTESIAN_POINT ( 'NONE',  ( 33.39017613691037667, 8.099518147537066781, 1.949999999999883382 ) ) ;
#3547=DIRECTION ( 'NONE',  ( 1.000000000000000000, 0.000000000000000000, -3.491481338843133355E-15 ) ) ;
#3564=DIRECTION ( 'NONE',  ( 3.491481338843133355E-15, -0.000000000000000000, 1.000000000000000000 ) ) ;
#3580=AXIS2_PLACEMENT_3D ( 'NONE', #9514, #2367, #14708 ) ;
#3581=EDGE_CURVE ( 'NONE', #25173, #20006, #30037, .T. ) ;
#3589=CARTESIAN_POINT ( 'NONE',  ( 54.29903166994490959, 6.002871265136678680, 2.049999999999811529 ) ) ;
#3591=EDGE_CURVE ( 'NONE', #17195, #20006, #12005, .T. ) ;
#3592=CARTESIAN_POINT ( 'NONE',  ( 51.69999999178978101, -3.608818513796484773, 1.949335135736226299 ) ) ;
#3594=FACE_OUTER_BOUND ( 'NONE', #30267, .T. ) ;
#3596=CARTESIAN_POINT ( 'NONE',  ( 51.80000000000001137, 4.175664755576646847, -1.929721184274108436 ) ) ;
#3604=DIRECTION ( 'NONE',  ( -0.9993908270190956511, 0.03489949670250096919, 3.491481338843132961E-15 ) ) ;
#3617=EDGE_CURVE ( 'NONE', #10094, #29651, #30529, .T. ) ;
#3631=VERTEX_POINT ( 'NONE', #19614 ) ;
#3633=AXIS2_PLACEMENT_3D ( 'NONE', #8691, #3956, #30242 ) ;
#3636=DIRECTION ( 'NONE',  ( -0.9993908270190957621, 0.03489949670250106634, 3.490838185622846777E-15 ) ) ;
#3641=EDGE_CURVE ( 'NONE', #4765, #17711, #21687, .T. ) ;
#3642=ORIENTED_EDGE ( 'NONE', *, *, #566, .F. ) ;
#3644=CARTESIAN_POINT ( 'NONE',  ( 53.25508263676793064, 8.249290793645352338, -2.050000000000185452 ) ) ;
#3663=CARTESIAN_POINT ( 'NONE',  ( 51.87770073550464645, 8.700057942179276083, 2.049999999999819522 ) ) ;
#3670=DIRECTION ( 'NONE',  ( 4.275831445896958607E-31, 1.000000000000000000, 1.224646799147353207E-16 ) ) ;
#3677=VERTEX_POINT ( 'NONE', #13654 ) ;
#3684=EDGE_CURVE ( 'NONE', #12841, #8007, #3758, .T. ) ;
#3686=DIRECTION ( 'NONE',  ( -0.7313537016191670181, -0.6819983600625023623, 2.468850131082252722E-15 ) ) ;
#3693=ORIENTED_EDGE ( 'NONE', *, *, #3581, .F. ) ;
#3704=ORIENTED_EDGE ( 'NONE', *, *, #16126, .F. ) ;
#3705=CARTESIAN_POINT ( 'NONE',  ( 51.60751284041730713, -4.291463206565929944, -1.660299764304736359 ) ) ;
#3710=CARTESIAN_POINT ( 'NONE',  ( 22.09542497983174414, 7.445411299648926118, -2.050000000000211209 ) ) ;
#3716=CARTESIAN_POINT ( 'NONE',  ( 47.73617949479463363, -3.930543434675368264, 1.171429914303333764 ) ) ;
#3720=CARTESIAN_POINT ( 'NONE',  ( 54.15675781068899397, 5.684314874070254042, -2.050000000000189004 ) ) ;
#3729=CARTESIAN_POINT ( 'NONE',  ( 54.15683185445048764, 5.684290329229592764, -2.050000000000188560 ) ) ;
#3733=CARTESIAN_POINT ( 'NONE',  ( 53.89553379148921408, 6.017104844469294278, 2.049999999999811973 ) ) ;
#3739=CARTESIAN_POINT ( 'NONE',  ( 31.46405049521009545, 7.544521452532235273, -2.050000000000109956 ) ) ;
#3742=ORIENTED_EDGE ( 'NONE', *, *, #4272, .T. ) ;
#3746=VERTEX_POINT ( 'NONE', #17693 ) ;
#3754=CIRCLE ( 'NONE', #5797, 0.1000000000000000472 ) ;
#3758=B_SPLINE_CURVE_WITH_KNOTS ( 'NONE', 3,
 ( #29393, #6233, #24803, #23336 ),
 .UNSPECIFIED., .F., .F.,
 ( 4, 4 ),
 ( 0.000000000000000000, 1.000000000000000000 ),
 .UNSPECIFIED. ) ;
#3760=CARTESIAN_POINT ( 'NONE',  ( 53.61178450975653220, 7.592125988483584997, -1.856626124458810256 ) ) ;
#3766=ORIENTED_EDGE ( 'NONE', *, *, #3617, .T. ) ;
#3772=EDGE_LOOP ( 'NONE', ( #12572, #6493, #29764, #21015 ) ) ;
#3774=CARTESIAN_POINT ( 'NONE',  ( 53.91574522235882228, 6.672251602522421443, 1.774295301432037286 ) ) ;
#3793=ORIENTED_EDGE ( 'NONE', *, *, #10433, .F. ) ;
#3794=CARTESIAN_POINT ( 'NONE',  ( 52.10582242447213019, 8.700707108360601794, -2.050000000000181455 ) ) ;
#3814=CARTESIAN_POINT ( 'NONE',  ( 53.75952070206893296, 7.747157889885662563, 2.049999999999812417 ) ) ;
#3820=FACE_OUTER_BOUND ( 'NONE', #13623, .T. ) ;
#3822=EDGE_CURVE ( 'NONE', #6667, #22071, #6549, .T. ) ;
#3824=CARTESIAN_POINT ( 'NONE',  ( 47.75910361055753839, -4.379721596991718258, -1.407221449367546784 ) ) ;
#3826=CARTESIAN_POINT ( 'NONE',  ( 24.99011192183064978, 5.348094263731223208, 1.949999999999912248 ) ) ;
#3835=CARTESIAN_POINT ( 'NONE',  ( 24.79176202108331850, 5.385922622694285344, -1.425000000000086198 ) ) ;
#3843=CYLINDRICAL_SURFACE ( 'NONE', #28057, 4.600000000000036948 ) ;
#3854=ORIENTED_EDGE ( 'NONE', *, *, #23079, .F. ) ;
#3857=( NAMED_UNIT ( * ) PLANE_ANGLE_UNIT ( ) SI_UNIT ( $, .RADIAN. ) );
#3862=DIRECTION ( 'NONE',  ( -0.9993908270191184107, 0.03489949670185085034, 3.491481338843133355E-15 ) ) ;
#3880=CARTESIAN_POINT ( 'NONE',  ( 53.21917409580245817, 8.083376426877231680, -1.902110155464870944 ) ) ;
#3884=LINE ( 'NONE', #1812, #14636 ) ;
#3888=EDGE_CURVE ( 'NONE', #27612, #11116, #23804, .T. ) ;
#3889=AXIS2_PLACEMENT_3D ( 'NONE', #12820, #3181, #8698 ) ;
#3896=VERTEX_POINT ( 'NONE', #14904 ) ;
#3897=CARTESIAN_POINT ( 'NONE',  ( 53.96125931204732495, 5.169815675097246377, -2.050000000000188116 ) ) ;
#3899=CARTESIAN_POINT ( 'NONE',  ( 51.80000000000003268, -3.637377585518695611, 2.099877210782855830 ) ) ;
#3900=EDGE_LOOP ( 'NONE', ( #17794, #8347, #23386, #6319 ) ) ;
#3901=CARTESIAN_POINT ( 'NONE',  ( 51.38825337055899922, 3.875334094704443899, 2.049999999999820410 ) ) ;
#3905=AXIS2_PLACEMENT_3D ( 'NONE', #8379, #20754, #17896 ) ;
#3907=EDGE_LOOP ( 'NONE', ( #15999, #23196, #12657, #24000, #5776, #33 ) ) ;
#3908=CARTESIAN_POINT ( 'NONE',  ( 24.79155133983196180, 5.500688705494902742, -2.050000000000086420 ) ) ;
#3916=CARTESIAN_POINT ( 'NONE',  ( 47.00000000000002842, -3.637377585518695611, 2.099877210782872261 ) ) ;
#3917=ORIENTED_EDGE ( 'NONE', *, *, #14628, .F. ) ;
#3934=CARTESIAN_POINT ( 'NONE',  ( 53.29168147589466997, 4.961551560356480373, 1.611466093477803785 ) ) ;
#3938=ORIENTED_EDGE ( 'NONE', *, *, #1166, .T. ) ;
#3939=CARTESIAN_POINT ( 'NONE',  ( 51.87416143049284756, 8.598705507415681737, 1.976179938779733858 ) ) ;
#3945=FACE_OUTER_BOUND ( 'NONE', #22403, .T. ) ;
#3946=CARTESIAN_POINT ( 'NONE',  ( 51.30576788583277903, -4.280519502657941899, -1.378181460054113794 ) ) ;
#3950=DIRECTION ( 'NONE',  ( -3.489354422748178582E-15, 1.218509414717996338E-16, -1.000000000000000000 ) ) ;
#3956=DIRECTION ( 'NONE',  ( 3.489354422748178582E-15, -1.218509414717996338E-16, 1.000000000000000000 ) ) ;
#3959=CARTESIAN_POINT ( 'NONE',  ( 50.85906935218978475, 8.675599908283860628, 2.049999999999822631 ) ) ;
#3960=EDGE_CURVE ( 'NONE', #9996, #3746, #16638, .T. ) ;
#3963=EDGE_CURVE ( 'NONE', #10732, #21532, #8309, .T. ) ;
#3966=CARTESIAN_POINT ( 'NONE',  ( 50.35762544161294585, 8.151359338959888845, -2.050000000000174794 ) ) ;
#3977=CARTESIAN_POINT ( 'NONE',  ( 53.82285890661303540, 4.901445667019300068, 2.049999999999811973 ) ) ;
#3981=CARTESIAN_POINT ( 'NONE',  ( 51.80000048712027905, 3.919471135816211316, 2.045252759501752227 ) ) ;
#3983=CARTESIAN_POINT ( 'NONE',  ( 48.00000000000001421, -4.387164041431065975, -1.383037119376926194 ) ) ;
#3985=ORIENTED_EDGE ( 'NONE', *, *, #4616, .T. ) ;
#3986=CARTESIAN_POINT ( 'NONE',  ( 24.11041436609877309, 5.625678654145607638, 1.949999999999915801 ) ) ;
#3990=ORIENTED_EDGE ( 'NONE', *, *, #30078, .T. ) ;
#3997=CARTESIAN_POINT ( 'NONE',  ( 51.80000000000002558, 4.175664755576631748, 1.929721184273780255 ) ) ;
#4039=DIRECTION ( 'NONE',  ( 1.000000000000000000, 0.000000000000000000, -3.491481338843133355E-15 ) ) ;
#4054=EDGE_LOOP ( 'NONE', ( #4675, #20937, #29221, #22519 ) ) ;
#4057=CARTESIAN_POINT ( 'NONE',  ( 52.61915120152473690, 4.492597126270304386, 2.049999999999816414 ) ) ;
#4066=ORIENTED_EDGE ( 'NONE', *, *, #12586, .F. ) ;
#4074=VECTOR ( 'NONE', #19323, 1000.000000000000000 ) ;
#4085=LINE ( 'NONE', #4234, #28127 ) ;
#4092=DIRECTION ( 'NONE',  ( 0.9990609829735203062, 0.04332611568077059105, -3.480798531547777782E-15 ) ) ;
#4101=DIRECTION ( 'NONE',  ( -1.000000000000000000, -0.000000000000000000, 3.491481338843133355E-15 ) ) ;
#4104=DIRECTION ( 'NONE',  ( -3.489354422748178582E-15, 1.218509414717996338E-16, -1.000000000000000000 ) ) ;
#4109=DIRECTION ( 'NONE',  ( 0.000000000000000000, 0.000000000000000000, 1.000000000000000000 ) ) ;
#4115=CARTESIAN_POINT ( 'NONE',  ( 50.80000000000002558, -4.387164041431067751, 1.383037119376580693 ) ) ;
#4130=ORIENTED_EDGE ( 'NONE', *, *, #25940, .T. ) ;
#4136=DIRECTION ( 'NONE',  ( -0.9993908270190957621, 0.03489949670250100389, 3.491481338843133355E-15 ) ) ;
#4145=EDGE_LOOP ( 'NONE', ( #29364, #13838, #21005, #17635, #3854 ) ) ;
#4152=CARTESIAN_POINT ( 'NONE',  ( 47.05963571244991783, 8.266527678078146479, 1.949999999999835865 ) ) ;
#4155=DIRECTION ( 'NONE',  ( -9.754918421198724481E-16, -0.9601771338024399638, -0.2793919678926571892 ) ) ;
#4156=PLANE ( 'NONE',  #30583 ) ;
#4182=VERTEX_POINT ( 'NONE', #6663 ) ;
#4196=DIRECTION ( 'NONE',  ( 3.489354422748178582E-15, -1.218509414717996338E-16, 1.000000000000000000 ) ) ;
#4199=VERTEX_POINT ( 'NONE', #23620 ) ;
#4203=CARTESIAN_POINT ( 'NONE',  ( 50.93131983953347941, -3.937842567657669157, 1.145831922971412675 ) ) ;
#4206=CARTESIAN_POINT ( 'NONE',  ( 51.74548155811471162, 3.822334312940638412, 2.049999999999816414 ) ) ;
#4217=EDGE_CURVE ( 'NONE', #5230, #29912, #9561, .T. ) ;
#4232=LINE ( 'NONE', #13149, #7429 ) ;
#4234=CARTESIAN_POINT ( 'NONE',  ( 34.56702326949724835, 8.213851659285209550, -2.050000000000119726 ) ) ;
#4238=ORIENTED_EDGE ( 'NONE', *, *, #17518, .T. ) ;
#4241=CARTESIAN_POINT ( 'NONE',  ( 51.87416143049284756, 8.598705507415683513, 1.949999999999818767 ) ) ;
#4250=ORIENTED_EDGE ( 'NONE', *, *, #944, .F. ) ;
#4253=DIRECTION ( 'NONE',  ( -0.9993908270190957621, 0.03489949670250094838, 3.492791461889839594E-15 ) ) ;
#4269=CARTESIAN_POINT ( 'NONE',  ( 51.80000048712015115, 3.919471099442191520, -2.045252491637605807 ) ) ;
#4272=EDGE_CURVE ( 'NONE', #5179, #26160, #23549, .T. ) ;
#4281=ORIENTED_EDGE ( 'NONE', *, *, #1624, .T. ) ;
#4284=FACE_OUTER_BOUND ( 'NONE', #8959, .T. ) ;
#4290=VERTEX_POINT ( 'NONE', #14256 ) ;
#4309=AXIS2_PLACEMENT_3D ( 'NONE', #25885, #4039, #21640 ) ;
#4311=ADVANCED_FACE ( 'NONE', ( #21563 ), #30733, .F. ) ;
#4315=CARTESIAN_POINT ( 'NONE',  ( 50.97819963584588976, 8.730054137149846127, -1.950000000000177147 ) ) ;
#4317=CARTESIAN_POINT ( 'NONE',  ( 54.04571512766927555, 5.333082506721908977, 2.049999999999811529 ) ) ;
#4325=ORIENTED_EDGE ( 'NONE', *, *, #20002, .F. ) ;
#4349=CIRCLE ( 'NONE', #20559, 0.1000000000000002554 ) ;
#4353=CARTESIAN_POINT ( 'NONE',  ( 51.80000000000002558, 3.850000000000016520, 1.949999999999818767 ) ) ;
#4357=CYLINDRICAL_SURFACE ( 'NONE', #21889, 159.6997717543496833 ) ;
#4363=LINE ( 'NONE', #16576, #5237 ) ;
#4366=CARTESIAN_POINT ( 'NONE',  ( 51.46757676178952323, 4.376162276235349147, 2.049999999999819966 ) ) ;
#4368=DIRECTION ( 'NONE',  ( -1.000000000000000000, -0.000000000000000000, 3.491481338843133355E-15 ) ) ;
#4372=CARTESIAN_POINT ( 'NONE',  ( 22.68585293163317473, 6.704127117150638249, -2.050000000000078870 ) ) ;
#4390=EDGE_CURVE ( 'NONE', #11041, #29912, #14450, .T. ) ;
#4417=DIRECTION ( 'NONE',  ( 1.000000000000000000, 0.000000000000000000, -3.491481338843133355E-15 ) ) ;
#4420=CARTESIAN_POINT ( 'NONE',  ( 53.81457038983117513, 5.799118250651475570, -1.689328355159275041 ) ) ;
#4424=DIRECTION ( 'NONE',  ( -0.7313537016191670181, -0.6819983600625022513, 2.468850131082252327E-15 ) ) ;
#4453=DIRECTION ( 'NONE',  ( -3.023770467182126270E-15, 0.4999707644721522182, -0.8660422822663637055 ) ) ;
#4454=DIRECTION ( 'NONE',  ( 0.9993908270190956511, -0.03489949670250202390, -3.491481338843132961E-15 ) ) ;
#4474=CARTESIAN_POINT ( 'NONE',  ( 51.80000000000001847, 6.982261990806648555E-14, -1.796574372350448449E-13 ) ) ;
#4477=CARTESIAN_POINT ( 'NONE',  ( 51.79118295937481520, 4.088185644532909002, -1.991056910035179817 ) ) ;
#4486=ORIENTED_EDGE ( 'NONE', *, *, #23258, .F. ) ;
#4489=CARTESIAN_POINT ( 'NONE',  ( 54.30613356357999777, 6.708647743757887305, -2.050000000000188560 ) ) ;
#4492=CARTESIAN_POINT ( 'NONE',  ( 31.20024169370289613, 7.859880413227774199, 1.424999999999891687 ) ) ;
#4495=ORIENTED_EDGE ( 'NONE', *, *, #18598, .F. ) ;
#4505=CARTESIAN_POINT ( 'NONE',  ( 31.33102771648083618, 7.478136438692525090, 2.049999999999890132 ) ) ;
#4511=DIRECTION ( 'NONE',  ( -0.03489949670185131525, -0.9993908270191184107, 0.000000000000000000 ) ) ;
#4531=CARTESIAN_POINT ( 'NONE',  ( 50.83686442967772479, 8.734989671305513070, -2.050000000000176570 ) ) ;
#4538=CARTESIAN_POINT ( 'NONE',  ( 41.48619405471883681, -151.3359592902621955, -1.950000000000163380 ) ) ;
#4549=CIRCLE ( 'NONE', #10, 0.1000000000000001443 ) ;
#4560=ORIENTED_EDGE ( 'NONE', *, *, #31125, .F. ) ;
#4561=DIRECTION ( 'NONE',  ( 3.489354422748178582E-15, -1.218509414717996338E-16, 1.000000000000000000 ) ) ;
#4562=CARTESIAN_POINT ( 'NONE',  ( 53.17422497822705196, 4.853022681123431603, 1.601063398553745021 ) ) ;
#4563=CARTESIAN_POINT ( 'NONE',  ( 53.82818506963806016, 5.794550291359760408, 1.819877325055229145 ) ) ;
#4568=CARTESIAN_POINT ( 'NONE',  ( 51.59043415373528063, -4.226158602834444444, -1.819860353018915911 ) ) ;
#4576=ORIENTED_EDGE ( 'NONE', *, *, #541, .T. ) ;
#4604=VERTEX_POINT ( 'NONE', #20280 ) ;
#4607=ORIENTED_EDGE ( 'NONE', *, *, #11156, .T. ) ;
#4616=EDGE_CURVE ( 'NONE', #737, #5233, #2469, .T. ) ;
#4629=DIRECTION ( 'NONE',  ( 3.304235192336781034E-15, 0.000000000000000000, 1.000000000000000000 ) ) ;
#4636=CARTESIAN_POINT ( 'NONE',  ( 54.27131183106372703, 6.003201256477255221, -2.050000000000188116 ) ) ;
#4637=EDGE_CURVE ( 'NONE', #7143, #23119, #23419, .T. ) ;
#4652=LINE ( 'NONE', #26497, #5545 ) ;
#4656=DIRECTION ( 'NONE',  ( -0.1208805777273481014, 0.9926670569371698338, 0.000000000000000000 ) ) ;
#4658=CARTESIAN_POINT ( 'NONE',  ( 33.39233489564711732, 8.222108905996257988, 2.049999999999883027 ) ) ;
#4675=ORIENTED_EDGE ( 'NONE', *, *, #7674, .T. ) ;
#4677=CARTESIAN_POINT ( 'NONE',  ( 53.13232117966331458, 4.211086031869615276, 2.049999999999814637 ) ) ;
#4680=DIRECTION ( 'NONE',  ( 0.000000000000000000, 0.000000000000000000, -1.000000000000000000 ) ) ;
#4693=EDGE_CURVE ( 'NONE', #18665, #12339, #19804, .T. ) ;
#4698=LINE ( 'NONE', #26247, #18101 ) ;
#4703=CARTESIAN_POINT ( 'NONE',  ( 47.07708546080149858, 8.766223091587681537, -1.550000000000163469 ) ) ;
#4712=DIRECTION ( 'NONE',  ( 3.489354422748178582E-15, -1.218509414717996338E-16, 1.000000000000000000 ) ) ;
#4725=LINE ( 'NONE', #6973, #10828 ) ;
#4728=APPLICATION_CONTEXT ( 'automotive_design' ) ;
#4731=CARTESIAN_POINT ( 'NONE',  ( 51.80000000000002558, -3.933368109459642437, 2.186004417992994497 ) ) ;
#4732=ADVANCED_FACE ( 'NONE', ( #25936 ), #18357, .T. ) ;
#4734=FACE_OUTER_BOUND ( 'NONE', #744, .T. ) ;
#4740=ORIENTED_EDGE ( 'NONE', *, *, #8840, .T. ) ;
#4741=EDGE_CURVE ( 'NONE', #8527, #27612, #24662, .T. ) ;
#4747=DIRECTION ( 'NONE',  ( -1.000000000000000000, -0.000000000000000000, 3.491481338843133355E-15 ) ) ;
#4754=ORIENTED_EDGE ( 'NONE', *, *, #20002, .T. ) ;
#4758=ORIENTED_EDGE ( 'NONE', *, *, #27975, .F. ) ;
#4760=ORIENTED_EDGE ( 'NONE', *, *, #5241, .T. ) ;
#4765=VERTEX_POINT ( 'NONE', #19307 ) ;
#4777=CIRCLE ( 'NONE', #27534, 4.099999999999992539 ) ;
#4785=EDGE_CURVE ( 'NONE', #28051, #107, #1596, .T. ) ;
#4796=CARTESIAN_POINT ( 'NONE',  ( 28.63101374161908552, 6.274379892050021112, 1.424999999999900346 ) ) ;
#4799=VERTEX_POINT ( 'NONE', #7862 ) ;
#4802=CARTESIAN_POINT ( 'NONE',  ( 52.05052023551990459, 4.366200217884951940, 1.447862837342193565 ) ) ;
#4804=ORIENTED_EDGE ( 'NONE', *, *, #10429, .F. ) ;
#4808=CARTESIAN_POINT ( 'NONE',  ( 31.46392738815476164, 7.544460793879348870, 2.049999999999889688 ) ) ;
#4812=CARTESIAN_POINT ( 'NONE',  ( 53.76063741390512973, 7.747904304409473752, -2.050000000000187228 ) ) ;
#4820=VECTOR ( 'NONE', #21388, 1000.000000000000000 ) ;
#4849=CARTESIAN_POINT ( 'NONE',  ( 52.08333333333335702, 4.368973594129894167, 1.439468559502539824 ) ) ;
#4855=ADVANCED_FACE ( 'NONE', ( #3594 ), #27334, .T. ) ;
#4868=CARTESIAN_POINT ( 'NONE',  ( 53.90826136769680943, 6.078611636103663507, 1.730551604087905204 ) ) ;
#4872=ORIENTED_EDGE ( 'NONE', *, *, #25274, .F. ) ;
#4875=CARTESIAN_POINT ( 'NONE',  ( 51.35976194839694386, -4.327157167232345003, -1.563052875988793611 ) ) ;
#4889=CARTESIAN_POINT ( 'NONE',  ( 51.80000000000003268, 6.982261990806648555E-14, 4.599999999999857536 ) ) ;
#4891=TOROIDAL_SURFACE ( 'NONE', #12974, 4.199999999999993072, 0.1000000000000000056 ) ;
#4899=CARTESIAN_POINT ( 'NONE',  ( 23.02167883289836681, 6.240626183124143189, -1.950000000000080558 ) ) ;
#4904=CARTESIAN_POINT ( 'NONE',  ( 53.35463186488154008, 7.923732722238535864, -1.887452792520897704 ) ) ;
#4908=CARTESIAN_POINT ( 'NONE',  ( 51.35185081662972095, -3.852602532216165887, 1.405026670785422871 ) ) ;
#4909=CARTESIAN_POINT ( 'NONE',  ( 22.20257169554298216, 7.242789023567402396, 1.424999999999922995 ) ) ;
#4933=SURFACE_SIDE_STYLE ('',( #5392 ) ) ;
#4939=CARTESIAN_POINT ( 'NONE',  ( 52.98705886115021002, 8.418976914897422503, -2.050000000000184563 ) ) ;
#4976=CARTESIAN_POINT ( 'NONE',  ( 31.37624803156852948, 7.388935656075745761, 2.049999999999763567 ) ) ;
#4991=CARTESIAN_POINT ( 'NONE',  ( 53.49139514279634966, 5.155866831720416599, 2.049999999999812861 ) ) ;
#4992=ORIENTED_EDGE ( 'NONE', *, *, #29132, .F. ) ;
#5005=CARTESIAN_POINT ( 'NONE',  ( 33.05069135236684019, 8.148093138862860130, -1.950000000000114531 ) ) ;
#5007=CARTESIAN_POINT ( 'NONE',  ( 32.57869118518439677, 7.908463454149920580, -2.050000000000176570 ) ) ;
#5010=LINE ( 'NONE', #14668, #5066 ) ;
#5012=B_SPLINE_CURVE_WITH_KNOTS ( 'NONE', 3,
 ( #19136, #28457, #28776, #2323, #23400, #13861, #2013, #6760, #16420, #21356 ),
 .UNSPECIFIED., .F., .F.,
 ( 4, 2, 2, 2, 4 ),
 ( 0.000000000000000000, 0.0003601004132760236712, 0.0007202008265520473424, 0.001080301239828071122, 0.001440401653104094685 ),
 .UNSPECIFIED. ) ;
#5014=CARTESIAN_POINT ( 'NONE',  ( 52.82099478266073334, 4.588601447596447613, -1.578939844535521386 ) ) ;
#5017=AXIS2_PLACEMENT_3D ( 'NONE', #25625, #953, #20746 ) ;
#5019=DIRECTION ( 'NONE',  ( 3.384826294588897856E-15, -8.881784197001252323E-16, 1.000000000000000000 ) ) ;
#5022=B_SPLINE_CURVE_WITH_KNOTS ( 'NONE', 3,
 ( #24847, #9404, #19957, #22193, #3013, #7914, #14873, #19073, #12504, #12655 ),
 .UNSPECIFIED., .F., .F.,
 ( 4, 2, 2, 2, 4 ),
 ( 0.000000000000000000, 0.0003926182454497119476, 0.0007852364908994238953, 0.001177854736349135843, 0.001570472981798847791 ),
 .UNSPECIFIED. ) ;
#5027=FACE_OUTER_BOUND ( 'NONE', #2966, .T. ) ;
#5039=LINE ( 'NONE', #4889, #4820 ) ;
#5046=EDGE_CURVE ( 'NONE', #4604, #3896, #4777, .T. ) ;
#5057=ADVANCED_FACE ( 'NONE', ( #22407 ), #22733, .T. ) ;
#5060=CARTESIAN_POINT ( 'NONE',  ( 32.22975847903030910, 7.786540417375088730, -1.950000000000110756 ) ) ;
#5066=VECTOR ( 'NONE', #712, 1000.000000000000000 ) ;
#5071=PLANE ( 'NONE',  #5217 ) ;
#5073=CARTESIAN_POINT ( 'NONE',  ( 51.80000000000001137, 4.349412134559255350, -1.696806954411249402 ) ) ;
#5075=CYLINDRICAL_SURFACE ( 'NONE', #11601, 1.000000000000000000 ) ;
#5087=ORIENTED_EDGE ( 'NONE', *, *, #11156, .F. ) ;
#5090=ORIENTED_EDGE ( 'NONE', *, *, #20294, .T. ) ;
#5092=EDGE_CURVE ( 'NONE', #21532, #11640, #5771, .T. ) ;
#5094=CARTESIAN_POINT ( 'NONE',  ( 54.16568811108923143, 5.603438171869654205, -2.050000000000187672 ) ) ;
#5110=DIRECTION ( 'NONE',  ( -3.489354422748178188E-15, 1.218509414717996091E-16, -1.000000000000000000 ) ) ;
#5121=CARTESIAN_POINT ( 'NONE',  ( 52.06777441456687683, 4.366880381858252669, 1.445821729970449221 ) ) ;
#5123=ORIENTED_EDGE ( 'NONE', *, *, #6295, .F. ) ;
#5126=CARTESIAN_POINT ( 'NONE',  ( 30.98482657477578428, 7.184130536712136639, 2.050000000000149925 ) ) ;
#5129=EDGE_CURVE ( 'NONE', #21850, #23309, #6556, .T. ) ;
#5140=CARTESIAN_POINT ( 'NONE',  ( 53.91678946233205494, 6.821600947619984368, 1.787725782035106459 ) ) ;
#5152=ORIENTED_EDGE ( 'NONE', *, *, #610, .T. ) ;
#5154=VERTEX_POINT ( 'NONE', #8609 ) ;
#5155=CARTESIAN_POINT ( 'NONE',  ( 21.97322666366011035, 8.076925076899403422, 1.949999999999922906 ) ) ;
#5157=CARTESIAN_POINT ( 'NONE',  ( 33.40812713800432476, 8.122903761241905940, -1.949999999999987965 ) ) ;
#5162=DIRECTION ( 'NONE',  ( 3.491481338843133750E-15, 0.000000000000000000, 1.000000000000000000 ) ) ;
#5165=CARTESIAN_POINT ( 'NONE',  ( 51.68129744679067272, 4.333300462216210569, -2.050000000000496758 ) ) ;
#5178=CARTESIAN_POINT ( 'NONE',  ( 53.91582462592150193, 6.672259099522118042, -0.8960560664367791528 ) ) ;
#5179=VERTEX_POINT ( 'NONE', #13804 ) ;
#5181=ORIENTED_EDGE ( 'NONE', *, *, #15824, .F. ) ;
#5182=EDGE_CURVE ( 'NONE', #22859, #29340, #23489, .T. ) ;
#5187=ORIENTED_EDGE ( 'NONE', *, *, #8547, .F. ) ;
#5196=CARTESIAN_POINT ( 'NONE',  ( 34.56269065792917417, 8.313757757582560970, 2.049999999999879474 ) ) ;
#5203=CARTESIAN_POINT ( 'NONE',  ( 51.76665129121498410, 4.175715153428418702, 1.929612129901060902 ) ) ;
#5217=AXIS2_PLACEMENT_3D ( 'NONE', #22019, #19652, #23776 ) ;
#5230=VERTEX_POINT ( 'NONE', #2853 ) ;
#5233=VERTEX_POINT ( 'NONE', #7038 ) ;
#5235=CARTESIAN_POINT ( 'NONE',  ( 51.80000000000001137, 8.701414213562481237, -2.050000000000180123 ) ) ;
#5237=VECTOR ( 'NONE', #12127, 1000.000000000000000 ) ;
#5240=CARTESIAN_POINT ( 'NONE',  ( 50.80000000000002558, -4.031600731908413948, 1.173113608511496375 ) ) ;
#5241=EDGE_CURVE ( 'NONE', #133, #9283, #5022, .T. ) ;
#5262=ORIENTED_EDGE ( 'NONE', *, *, #14118, .T. ) ;
#5272=CARTESIAN_POINT ( 'NONE',  ( 25.99900894223004855, 5.212247165294382256, 1.949999999999974198 ) ) ;
#5274=LINE ( 'NONE', #17643, #21361 ) ;
#5284=CARTESIAN_POINT ( 'NONE',  ( 53.87827693845219557, 5.944250707180090743, 1.708828125785182728 ) ) ;
#5297=CARTESIAN_POINT ( 'NONE',  ( 53.90826135247864670, 6.078611590743634885, -1.730551853729838774 ) ) ;
#5300=ORIENTED_EDGE ( 'NONE', *, *, #2711, .T. ) ;
#5301=CARTESIAN_POINT ( 'NONE',  ( 29.19109589769589164, 6.114704649263054570, -2.050000000000100631 ) ) ;
#5308=CARTESIAN_POINT ( 'NONE',  ( 51.97945110550969616, 4.337541896208930048, -1.549654688285467596 ) ) ;
#5310=DIRECTION ( 'NONE',  ( 0.000000000000000000, 0.000000000000000000, 1.000000000000000000 ) ) ;
#5320=CARTESIAN_POINT ( 'NONE',  ( 54.24287105605030490, 6.361183780992974768, 2.049999999999811529 ) ) ;
#5326=AXIS2_PLACEMENT_3D ( 'NONE', #28085, #6565, #13097 ) ;
#5329=CARTESIAN_POINT ( 'NONE',  ( 51.52519442949588324, -4.265347051556910962, 1.724604836179060019 ) ) ;
#5331=ORIENTED_EDGE ( 'NONE', *, *, #22449, .F. ) ;
#5333=DIRECTION ( 'NONE',  ( 3.304235192336781034E-15, 0.000000000000000000, 1.000000000000000000 ) ) ;
#5352=ADVANCED_FACE ( 'NONE', ( #9250 ), #13886, .F. ) ;
#5366=CARTESIAN_POINT ( 'NONE',  ( 29.45665666413592376, 6.177494273110388789, 1.424999999999897904 ) ) ;
#5392=SURFACE_STYLE_FILL_AREA ( #2408 ) ;
#5405=AXIS2_PLACEMENT_3D ( 'NONE', #6731, #20535, #30168 ) ;
#5407=AXIS2_PLACEMENT_3D ( 'NONE', #8283, #22551, #12867 ) ;
#5420=CARTESIAN_POINT ( 'NONE',  ( 52.05786831706192430, 3.857808750919801355, 1.390516658560897234 ) ) ;
#5421=CARTESIAN_POINT ( 'NONE',  ( 47.12301153005437016, -4.134673935618278229, 2.019140663349721976 ) ) ;
#5426=CIRCLE ( 'NONE', #17571, 4.600000000000036948 ) ;
#5435=CARTESIAN_POINT ( 'NONE',  ( 30.91033855991008039, 7.142409676556906284, 1.949999999999890710 ) ) ;
#5439=DIRECTION ( 'NONE',  ( -9.754918421198724481E-16, -0.9601771338024399638, -0.2793919678926571892 ) ) ;
#5445=CARTESIAN_POINT ( 'NONE',  ( 25.68808851946594984, 5.234409800456067963, 2.049999999999911005 ) ) ;
#5448=CARTESIAN_POINT ( 'NONE',  ( 53.60445531103937356, 4.614871059762981176, -2.050000000000186784 ) ) ;
#5453=TOROIDAL_SURFACE ( 'NONE', #30718, 4.500000000000037303, 0.1000000000000000056 ) ;
#5458=CARTESIAN_POINT ( 'NONE',  ( 51.70000000000003837, 6.982261990806648555E-14, 4.599999999999857536 ) ) ;
#5460=AXIS2_PLACEMENT_3D ( 'NONE', #22120, #413, #17206 ) ;
#5462=CARTESIAN_POINT ( 'NONE',  ( 51.87765138016307986, 8.698644590117595499, -2.050000000000180123 ) ) ;
#5463=ORIENTED_EDGE ( 'NONE', *, *, #3201, .F. ) ;
#5478=CARTESIAN_POINT ( 'NONE',  ( 26.61920844897797167, 5.219578739559237235, -2.050000000000091305 ) ) ;
#5483=CARTESIAN_POINT ( 'NONE',  ( 53.05367528747407135, 8.375580747031634132, -2.050000000000184563 ) ) ;
#5484=FACE_OUTER_BOUND ( 'NONE', #7077, .T. ) ;
#5497=CARTESIAN_POINT ( 'NONE',  ( 54.38981447126021607, 6.361385918223966485, 2.043118800226060294 ) ) ;
#5501=CARTESIAN_POINT ( 'NONE',  ( 53.81176349924870550, 5.730864617276226980, 1.682988280464426722 ) ) ;
#5507=ADVANCED_FACE ( 'NONE', ( #3945 ), #21382, .F. ) ;
#5509=ORIENTED_EDGE ( 'NONE', *, *, #24581, .F. ) ;
#5533=CARTESIAN_POINT ( 'NONE',  ( 30.66094943579030385, 7.112308407316297654, 2.049999999999892797 ) ) ;
#5535=AXIS2_PLACEMENT_3D ( 'NONE', #19536, #22064, #17301 ) ;
#5539=B_SPLINE_CURVE_WITH_KNOTS ( 'NONE', 3,
 ( #29076, #2319, #2010, #16595, #14509, #23548, #1846, #16417, #24183, #11522, #21199, #12143, #14031, #6758, #30829, #9148, #21354, #11824, #30981 ),
 .UNSPECIFIED., .F., .F.,
 ( 4, 2, 2, 2, 1, 2, 2, 2, 2, 4 ),
 ( 0.5315346799924233201, 0.6486510099942875973, 0.7072091749952189588, 0.7364882574956834738, 0.7438080281207990474, 0.7474679134333586106, 0.7511277987459183958, 0.7657673399961579808, 0.8828836699980789904, 1.000000000000000000 ),
 .UNSPECIFIED. ) ;
#5545=VECTOR ( 'NONE', #26815, 1000.000000000000114 ) ;
#5546=EDGE_CURVE ( 'NONE', #30852, #28320, #21529, .T. ) ;
#5551=EDGE_CURVE ( 'NONE', #19284, #9698, #16624, .T. ) ;
#5553=ADVANCED_FACE ( 'NONE', ( #28331 ), #23275, .T. ) ;
#5563=CARTESIAN_POINT ( 'NONE',  ( 53.81176349924876945, 5.730864617276189676, -2.050000000000250289 ) ) ;
#5567=TOROIDAL_SURFACE ( 'NONE', #22791, 4.199999999999993072, 0.1000000000000000056 ) ;
#5576=ORIENTED_EDGE ( 'NONE', *, *, #6988, .F. ) ;
#5580=CARTESIAN_POINT ( 'NONE',  ( 47.12430284249615653, -4.150085526745831643, -1.728112049830362151 ) ) ;
#5583=CARTESIAN_POINT ( 'NONE',  ( 47.73576178058490171, -4.410640387331298484, 1.311048612304915428 ) ) ;
#5597=CARTESIAN_POINT ( 'NONE',  ( 33.97474581211285027, 8.173393014830729442, 1.949999999999881606 ) ) ;
#5600=DIRECTION ( 'NONE',  ( 3.304235192336781034E-15, 0.000000000000000000, 1.000000000000000000 ) ) ;
#5601=CARTESIAN_POINT ( 'NONE',  ( 51.80000000000001137, 3.954022803064791702, -2.040489002254654682 ) ) ;
#5602=CARTESIAN_POINT ( 'NONE',  ( 22.72181155399538355, 6.520914524688622649, 1.949999999999919575 ) ) ;
#5616=CARTESIAN_POINT ( 'NONE',  ( 54.12924440478096244, 6.977429999421167039, -2.050000000000188116 ) ) ;
#5628=CARTESIAN_POINT ( 'NONE',  ( 53.93368044017396556, 6.673923803580072978, -1.889921144916990592 ) ) ;
#5631=ORIENTED_EDGE ( 'NONE', *, *, #13596, .T. ) ;
#5632=CARTESIAN_POINT ( 'NONE',  ( 31.37624803221847358, 7.388935654832122779, -1.950000000000108091 ) ) ;
#5634=CARTESIAN_POINT ( 'NONE',  ( 54.36607077795603971, 6.714235712056784600, 2.039222690360789958 ) ) ;
#5637=CARTESIAN_POINT ( 'NONE',  ( 52.02306152107793480, 3.830941655646746824, -2.050000000000181455 ) ) ;
#5638=CARTESIAN_POINT ( 'NONE',  ( 47.12288048077186176, -3.662677325876132706, -1.845585774149762326 ) ) ;
#5650=CARTESIAN_POINT ( 'NONE',  ( 54.33836613259588688, 6.362881108852070255, 2.049999999999810196 ) ) ;
#5660=B_SPLINE_CURVE_WITH_KNOTS ( 'NONE', 3,
 ( #8560, #15372, #27731, #11094 ),
 .UNSPECIFIED., .F., .F.,
 ( 4, 4 ),
 ( 0.000000000000000000, 0.0001000467755295633628 ),
 .UNSPECIFIED. ) ;
#5661=EDGE_CURVE ( 'NONE', #8932, #15558, #21121, .T. ) ;
#5668=CARTESIAN_POINT ( 'NONE',  ( 48.00000000000002132, -4.319730106884873244, 1.256953381662069269 ) ) ;
#5677=B_SPLINE_CURVE_WITH_KNOTS ( 'NONE', 3,
 ( #20641, #6208, #3824, #15563, #23167, #11108, #25211, #8720, #28041, #22529 ),
 .UNSPECIFIED., .F., .F.,
 ( 4, 2, 2, 2, 4 ),
 ( 0.000000000000000000, 0.0003600849014046848253, 0.0007201698028093696507, 0.001080254704214054368, 0.001440339605618739301 ),
 .UNSPECIFIED. ) ;
#5709=CARTESIAN_POINT ( 'NONE',  ( 53.53640187423184216, 5.215699251213393062, -2.050000000000122835 ) ) ;
#5719=DIRECTION ( 'NONE',  ( -6.842565855738836309E-15, 0.4857787595540328796, -0.8740818021021518058 ) ) ;
#5720=CARTESIAN_POINT ( 'NONE',  ( 52.34995357322210907, 3.980947253423499532, -2.045629398349763317 ) ) ;
#5727=PLANE ( 'NONE',  #21750 ) ;
#5744=ORIENTED_EDGE ( 'NONE', *, *, #25274, .T. ) ;
#5749=CARTESIAN_POINT ( 'NONE',  ( 24.76493886322414539, 5.404133871203915973, 2.049999999999914557 ) ) ;
#5768=DIRECTION ( 'NONE',  ( -0.9993908270190957621, 0.03489949670250097613, 3.491481338843133355E-15 ) ) ;
#5771=LINE ( 'NONE', #15596, #8326 ) ;
#5776=ORIENTED_EDGE ( 'NONE', *, *, #3230, .T. ) ;
#5781=ORIENTED_EDGE ( 'NONE', *, *, #3591, .T. ) ;
#5791=CARTESIAN_POINT ( 'NONE',  ( 47.12349245989109647, -3.859221392886552859, 1.645001822843298545 ) ) ;
#5792=CARTESIAN_POINT ( 'NONE',  ( 47.00000000000000711, -3.637377585518695611, -2.099877210783200887 ) ) ;
#5796=CARTESIAN_POINT ( 'NONE',  ( 51.41814105943718971, -4.256263374916419373, 1.450017276182312465 ) ) ;
#5797=AXIS2_PLACEMENT_3D ( 'NONE', #31018, #14384, #4109 ) ;
#5806=CARTESIAN_POINT ( 'NONE',  ( 54.40536566420629327, 5.987876313947340989, -1.625000000000180744 ) ) ;
#5813=FACE_OUTER_BOUND ( 'NONE', #19036, .T. ) ;
#5839=CARTESIAN_POINT ( 'NONE',  ( 53.78583212225908738, 7.269814517959708233, -1.827186616692397791 ) ) ;
#5865=CARTESIAN_POINT ( 'NONE',  ( 53.12796055743056911, 4.814990154991031446, -1.597383859324410516 ) ) ;
#5868=EDGE_LOOP ( 'NONE', ( #5181, #13164, #28939, #735, #7233, #19154 ) ) ;
#5869=AXIS2_PLACEMENT_3D ( 'NONE', #21369, #27987, #11361 ) ;
#5871=CARTESIAN_POINT ( 'NONE',  ( 53.53640187423192032, 5.215699251213354870, -1.635615235160539749 ) ) ;
#5876=DIRECTION ( 'NONE',  ( 3.491481338843133750E-15, 0.000000000000000000, 1.000000000000000000 ) ) ;
#5887=AXIS2_PLACEMENT_3D ( 'NONE', #9567, #11445, #4629 ) ;
#5892=DIRECTION ( 'NONE',  ( -1.000000000000000000, -0.000000000000000000, 3.491481338843133355E-15 ) ) ;
#5893=DIRECTION ( 'NONE',  ( 3.016910393003118404E-15, 0.000000000000000000, 1.000000000000000000 ) ) ;
#5895=CARTESIAN_POINT ( 'NONE',  ( 53.05250010753326251, 4.165967808473761025, 2.049999999999814637 ) ) ;
#5896=CARTESIAN_POINT ( 'NONE',  ( 22.32336313483204648, 6.618105965108087574, -1.550000000000077316 ) ) ;
#5932=CARTESIAN_POINT ( 'NONE',  ( 52.91430282107062766, 8.434692232659099176, -2.050000000000183231 ) ) ;
#5940=AXIS2_PLACEMENT_3D ( 'NONE', #30248, #20306, #29935 ) ;
#5951=CARTESIAN_POINT ( 'NONE',  ( 51.80000000000001137, 3.850000000000016520, -1.678541033159632434 ) ) ;
#5954=CARTESIAN_POINT ( 'NONE',  ( 21.97322666366011390, 8.076925076899296840, -1.950000000000075895 ) ) ;
#5959=CARTESIAN_POINT ( 'NONE',  ( 54.31409749668479492, 6.709390224138187975, 2.049999999999810640 ) ) ;
#5964=CARTESIAN_POINT ( 'NONE',  ( 52.45567523936535537, 8.517307475678972395, -1.943109374214847973 ) ) ;
#5973=DIRECTION ( 'NONE',  ( -1.000000000000000000, 9.912705577004238501E-16, 3.469446951951483476E-15 ) ) ;
#5977=AXIS2_PLACEMENT_3D ( 'NONE', #26353, #18923, #4656 ) ;
#5979=CARTESIAN_POINT ( 'NONE',  ( 54.31535817511873176, 6.000144074150753681, 2.049999999999810196 ) ) ;
#5989=ORIENTED_EDGE ( 'NONE', *, *, #4693, .T. ) ;
#5995=PLANE ( 'NONE',  #17992 ) ;
#6018=EDGE_CURVE ( 'NONE', #12847, #26028, #18331, .T. ) ;
#6034=CARTESIAN_POINT ( 'NONE',  ( 52.04555679422406200, 4.350000000000022737, -1.551140652419768617 ) ) ;
#6038=CARTESIAN_POINT ( 'NONE',  ( 53.71202192472756565, 7.447163568589272309, -1.837855077339860976 ) ) ;
#6043=CIRCLE ( 'NONE', #30298, 4.099999999999992539 ) ;
#6044=CARTESIAN_POINT ( 'NONE',  ( 22.58314801556725371, 7.622751244490530986, -1.425000000000078870 ) ) ;
#6058=CARTESIAN_POINT ( 'NONE',  ( 53.05417955289647125, 8.376364939874980209, 2.049999999999815081 ) ) ;
#6072=ORIENTED_EDGE ( 'NONE', *, *, #4390, .T. ) ;
#6083=CARTESIAN_POINT ( 'NONE',  ( 51.80000000000001847, 6.982261990806648555E-14, -1.796574372350448449E-13 ) ) ;
#6105=CARTESIAN_POINT ( 'NONE',  ( 25.68808851946277727, 5.234409800456325534, -2.050000000000087752 ) ) ;
#6107=DIRECTION ( 'NONE',  ( 0.000000000000000000, 0.000000000000000000, 1.000000000000000000 ) ) ;
#6113=CARTESIAN_POINT ( 'NONE',  ( 47.73505020348671479, -4.023708852620726972, 1.198807875231203468 ) ) ;
#6119=CARTESIAN_POINT ( 'NONE',  ( 50.80000000000002558, -4.387164041431065087, 1.383037119376580248 ) ) ;
#6122=CARTESIAN_POINT ( 'NONE',  ( 47.06312566212017146, 8.366466760780054912, 2.049999999999835953 ) ) ;
#6123=ADVANCED_FACE ( 'NONE', ( #2004 ), #30725, .T. ) ;
#6126=CARTESIAN_POINT ( 'NONE',  ( 54.26434950415730896, 6.004763229855418771, -2.050000000000188560 ) ) ;
#6129=EDGE_LOOP ( 'NONE', ( #18712, #16849, #22487, #4758 ) ) ;
#6134=ORIENTED_EDGE ( 'NONE', *, *, #11950, .T. ) ;
#6135=CARTESIAN_POINT ( 'NONE',  ( 33.39238368996267070, 8.222114305082241614, -2.050000000000116618 ) ) ;
#6159=DIRECTION ( 'NONE',  ( 3.489354422748178582E-15, -1.218509414717996338E-16, 1.000000000000000000 ) ) ;
#6161=CARTESIAN_POINT ( 'NONE',  ( 31.31144479506063760, 7.468183200860340598, 2.049999999999891021 ) ) ;
#6168=DIRECTION ( 'NONE',  ( 0.000000000000000000, 0.8660422822663634834, -0.4999707644721521627 ) ) ;
#6172=AXIS2_PLACEMENT_3D ( 'NONE', #13897, #3950, #28336 ) ;
#6174=CARTESIAN_POINT ( 'NONE',  ( 28.63101374161907842, 6.274379892050022001, -1.425000000000099742 ) ) ;
#6180=CARTESIAN_POINT ( 'NONE',  ( 52.59308447829369726, 4.500429781219338565, -1.566000285930613023 ) ) ;
#6182=ORIENTED_EDGE ( 'NONE', *, *, #21423, .F. ) ;
#6183=ADVANCED_FACE ( 'NONE', ( #9459 ), #21525, .F. ) ;
#6186=CARTESIAN_POINT ( 'NONE',  ( 52.10572631149717182, 8.700000001568275465, -2.050000000000181455 ) ) ;
#6190=DIRECTION ( 'NONE',  ( -3.489354422748178582E-15, 1.218509414717996338E-16, -1.000000000000000000 ) ) ;
#6194=( BOUNDED_SURFACE ( )  B_SPLINE_SURFACE ( 3, 2, ( 
 ( #1036, #3245, #12886 ),
 ( #22575, #7684, #14954 ),
 ( #7828, #24623, #27462 ),
 ( #22271, #557, #10215 ),
 ( #19883, #29514, #17503 ),
 ( #27158, #3705, #30305 ),
 ( #1631, #15889, #25548 ),
 ( #23348, #10835, #8469 ),
 ( #23203, #13810, #20822 ),
 ( #30451, #25400, #18146 ) ),
 .UNSPECIFIED., .F., .F., .F. ) 
 B_SPLINE_SURFACE_WITH_KNOTS ( ( 4, 2, 2, 2, 4 ),
 ( 3, 3 ),
 ( -4.878909776184769953E-18, 0.0003534454412679794333, 0.0007068908825359637455, 0.001060336323803948112, 0.001413781765071932478 ),
 ( 0.000000000000000000, 1.000000000000000000 ),
 .UNSPECIFIED. ) 
 GEOMETRIC_REPRESENTATION_ITEM ( )  RATIONAL_B_SPLINE_SURFACE ( (
 ( 1.000000000000000000, 0.6992058987801016423, 1.000000000000000000),
 ( 1.000000000000000000, 0.6992660572530883245, 1.000000000000000000),
 ( 1.000000000000000000, 0.6974033530225959288, 1.000000000000000000),
 ( 1.000000000000000000, 0.6920435876578637791, 1.000000000000000000),
 ( 1.000000000000000000, 0.6885661196046906074, 1.000000000000000000),
 ( 1.000000000000000000, 0.6845372766840260859, 1.000000000000000000),
 ( 1.000000000000000000, 0.6841195446886403353, 1.000000000000000000),
 ( 1.000000000000000000, 0.6902705495948038283, 1.000000000000000000),
 ( 1.000000000000000000, 0.6968978290748681914, 1.000000000000000000),
 ( 1.000000000000000000, 0.7071067811865727748, 1.000000000000000000) ) ) 
 REPRESENTATION_ITEM ( '' )  SURFACE ( )  );
#6202=CARTESIAN_POINT ( 'NONE',  ( 52.18319145150646676, 8.687974897284844289, 2.049999999999818190 ) ) ;
#6208=CARTESIAN_POINT ( 'NONE',  ( 47.87911513861941870, -4.387164041431065975, -1.383037119376925972 ) ) ;
#6219=ADVANCED_FACE ( 'NONE', ( #21816 ), #105, .F. ) ;
#6233=CARTESIAN_POINT ( 'NONE',  ( 53.90826771765248537, 6.078164526406591328, -1.689602626210267466 ) ) ;
#6240=AXIS2_PLACEMENT_3D ( 'NONE', #15812, #25461, #1403 ) ;
#6251=CARTESIAN_POINT ( 'NONE',  ( 23.88937650878775543, 5.720041404659518491, -2.050000000000081979 ) ) ;
#6264=CARTESIAN_POINT ( 'NONE',  ( 51.80000000000003268, -3.994423162662135152, 2.070282222599607813 ) ) ;
#6265=AXIS2_PLACEMENT_3D ( 'NONE', #9048, #16177, #13461 ) ;
#6268=EDGE_CURVE ( 'NONE', #133, #7683, #19127, .T. ) ;
#6271=CARTESIAN_POINT ( 'NONE',  ( 54.27670628353131121, 6.362024822791419787, -2.050000000000186340 ) ) ;
#6273=CARTESIAN_POINT ( 'NONE',  ( 51.79699096306529782, -3.614067288481912499, 1.940243272267534902 ) ) ;
#6275=CARTESIAN_POINT ( 'NONE',  ( 52.41186875581716720, 8.643425072357743488, 2.049999999999817302 ) ) ;
#6280=CARTESIAN_POINT ( 'NONE',  ( 26.91677043723410989, 5.349113832900135534, -2.050000000000093525 ) ) ;
#6282=VERTEX_POINT ( 'NONE', #26533 ) ;
#6295=EDGE_CURVE ( 'NONE', #4182, #23309, #8796, .T. ) ;
#6315=CARTESIAN_POINT ( 'NONE',  ( 53.91582462592152325, 6.672259099522126036, -1.484311132272649436 ) ) ;
#6319=ORIENTED_EDGE ( 'NONE', *, *, #23410, .F. ) ;
#6326=CARTESIAN_POINT ( 'NONE',  ( 22.32354329814791782, 7.018810584857204660, 1.949999999999922240 ) ) ;
#6346=LINE ( 'NONE', #16005, #29810 ) ;
#6349=ORIENTED_EDGE ( 'NONE', *, *, #9159, .T. ) ;
#6350=CARTESIAN_POINT ( 'NONE',  ( 53.04927178323141845, 4.171861402708406885, 2.049999999999814637 ) ) ;
#6354=ADVANCED_FACE ( 'NONE', ( #12739 ), #27809, .T. ) ;
#6359=EDGE_LOOP ( 'NONE', ( #28626, #729, #24440, #4760 ) ) ;
#6360=CARTESIAN_POINT ( 'NONE',  ( 23.82615635345663563, 5.749986595043423243, 1.949999999999916689 ) ) ;
#6371=CARTESIAN_POINT ( 'NONE',  ( 26.41339658680652391, 5.213169555504945762, -1.425000000000092637 ) ) ;
#6386=ORIENTED_EDGE ( 'NONE', *, *, #3415, .F. ) ;
#6391=EDGE_CURVE ( 'NONE', #24892, #20124, #12630, .T. ) ;
#6404=AXIS2_PLACEMENT_3D ( 'NONE', #22902, #8020, #5310 ) ;
#6409=CARTESIAN_POINT ( 'NONE',  ( 24.76493886322366222, 5.404133871204292561, -2.050000000000152589 ) ) ;
#6419=AXIS2_PLACEMENT_3D ( 'NONE', #28950, #4101, #13740 ) ;
#6420=CARTESIAN_POINT ( 'NONE',  ( 47.12894858146291455, -3.772456960769013712, 1.610749547355264433 ) ) ;
#6421=DIRECTION ( 'NONE',  ( -1.000000000000000000, 0.000000000000000000, 3.491481338843133355E-15 ) ) ;
#6427=FACE_OUTER_BOUND ( 'NONE', #18244, .T. ) ;
#6437=ORIENTED_EDGE ( 'NONE', *, *, #22825, .F. ) ;
#6441=CARTESIAN_POINT ( 'NONE',  ( 53.90340377275678918, 6.895264694548083995, 1.787725782035106459 ) ) ;
#6444=CARTESIAN_POINT ( 'NONE',  ( 50.93192783270057333, -3.937842570012147547, -1.145831914963376219 ) ) ;
#6447=CARTESIAN_POINT ( 'NONE',  ( 25.08846173237438748, 5.428824289251027224, -2.050000000000087308 ) ) ;
#6454=CARTESIAN_POINT ( 'NONE',  ( 51.87765138016307986, 8.698644590117595499, -2.050000000000180123 ) ) ;
#6466=AXIS2_PLACEMENT_3D ( 'NONE', #21868, #22171, #22007 ) ;
#6472=CARTESIAN_POINT ( 'NONE',  ( 52.59308920433354473, 4.500431172231105670, 1.566000610716282271 ) ) ;
#6480=ORIENTED_EDGE ( 'NONE', *, *, #14822, .F. ) ;
#6481=CARTESIAN_POINT ( 'NONE',  ( 53.91582462592150193, 6.672259099522118042, -0.8960560664367791528 ) ) ;
#6490=CARTESIAN_POINT ( 'NONE',  ( 51.80000000000001137, 4.350000000000017408, -1.550321101314903194 ) ) ;
#6493=ORIENTED_EDGE ( 'NONE', *, *, #7831, .T. ) ;
#6504=CARTESIAN_POINT ( 'NONE',  ( 47.44367304408061869, -4.328087698693956931, -1.560456010858677356 ) ) ;
#6513=CARTESIAN_POINT ( 'NONE',  ( 22.54717926605044198, 7.740376438784147162, -1.425000000000078204 ) ) ;
#6518=CARTESIAN_POINT ( 'NONE',  ( 52.16611735465127708, 8.588510181879298599, 2.049999999999818190 ) ) ;
#6537=EDGE_CURVE ( 'NONE', #30937, #125, #19082, .T. ) ;
#6542=DIRECTION ( 'NONE',  ( -0.9993908270190956511, 0.03489949670250202390, 3.491481338843132961E-15 ) ) ;
#6549=LINE ( 'NONE', #4315, #11807 ) ;
#6556=LINE ( 'NONE', #20672, #16938 ) ;
#6565=DIRECTION ( 'NONE',  ( -1.000000000000000000, -0.000000000000000000, 3.491481338843133355E-15 ) ) ;
#6579=EDGE_CURVE ( 'NONE', #9403, #6667, #4652, .T. ) ;
#6582=EDGE_CURVE ( 'NONE', #1060, #16210, #21260, .T. ) ;
#6594=CARTESIAN_POINT ( 'NONE',  ( 51.67089510066356439, -3.772469189071185003, 1.610667359469496240 ) ) ;
#6596=CARTESIAN_POINT ( 'NONE',  ( 52.09213388422766400, 8.600000000000108002, 1.949999998429079895 ) ) ;
#6601=CARTESIAN_POINT ( 'NONE',  ( 31.33115571983777770, 7.478201237066244289, -2.050000000000108180 ) ) ;
#6647=VERTEX_POINT ( 'NONE', #27115 ) ;
#6654=CIRCLE ( 'NONE', #9198, 0.1000000000000002970 ) ;
#6663=CARTESIAN_POINT ( 'NONE',  ( 51.70000000000001705, 3.851905453475298113, -1.404572667215154835 ) ) ;
#6667=VERTEX_POINT ( 'NONE', #22856 ) ;
#6697=EDGE_CURVE ( 'NONE', #5233, #20006, #1391, .T. ) ;
#6705=DIRECTION ( 'NONE',  ( -3.489354422748178582E-15, 1.218509414717996338E-16, -1.000000000000000000 ) ) ;
#6713=CARTESIAN_POINT ( 'NONE',  ( 54.19030381964616083, 6.697848500921247172, -2.050000000000189004 ) ) ;
#6731=CARTESIAN_POINT ( 'NONE',  ( 41.48619405472010868, -151.3359592902261852, 1.424999999999836175 ) ) ;
#6743=CARTESIAN_POINT ( 'NONE',  ( 54.16075265905998748, 5.605215124043997577, 2.049999999999811084 ) ) ;
#6746=CARTESIAN_POINT ( 'NONE',  ( 51.35673058052184103, -3.851351755029094104, -1.408485093545058575 ) ) ;
#6758=CARTESIAN_POINT ( 'NONE',  ( 53.29836137858970346, 7.982254241276255158, 1.892848342821848995 ) ) ;
#6760=CARTESIAN_POINT ( 'NONE',  ( 47.76052902567371916, -4.379874851678566827, 1.406750166670421631 ) ) ;
#6778=DIRECTION ( 'NONE',  ( 0.9993908270190958731, -0.03489949670249358621, -4.336808689942082423E-15 ) ) ;
#6782=VERTEX_POINT ( 'NONE', #25765 ) ;
#6797=DIRECTION ( 'NONE',  ( -1.000000000000000000, 0.000000000000000000, 3.491481338843133750E-15 ) ) ;
#6804=CARTESIAN_POINT ( 'NONE',  ( 47.00000000000002132, 6.982261990806648555E-14, -1.628983268085978048E-13 ) ) ;
#6807=DIRECTION ( 'NONE',  ( -0.9993908270190958731, 0.03489949670250096919, 3.491595022110081325E-15 ) ) ;
#6809=CARTESIAN_POINT ( 'NONE',  ( 47.02041791374344371, -4.146195171497997656, -1.996297985640646644 ) ) ;
#6819=ORIENTED_EDGE ( 'NONE', *, *, #27991, .T. ) ;
#6825=EDGE_LOOP ( 'NONE', ( #17014, #8090, #2733 ) ) ;
#6853=EDGE_LOOP ( 'NONE', ( #7710, #24653, #9877, #11549 ) ) ;
#6856=CARTESIAN_POINT ( 'NONE',  ( 53.56883702301119143, 7.945158945316190824, 2.049999999999813305 ) ) ;
#6859=CARTESIAN_POINT ( 'NONE',  ( 53.96142581635486124, 5.170113101904351360, 2.049999999999811529 ) ) ;
#6865=CARTESIAN_POINT ( 'NONE',  ( 22.58314801556729634, 7.622751244490449274, 1.424999999999920997 ) ) ;
#6870=AXIS2_PLACEMENT_3D ( 'NONE', #20880, #21366, #30993 ) ;
#6872=ORIENTED_EDGE ( 'NONE', *, *, #18887, .T. ) ;
#6879=CARTESIAN_POINT ( 'NONE',  ( 31.86617018594176898, 7.736336509539437856, 2.049999999999888800 ) ) ;
#6885=VECTOR ( 'NONE', #19636, 1000.000000000000114 ) ;
#6892=DIRECTION ( 'NONE',  ( 0.000000000000000000, 0.000000000000000000, -1.000000000000000000 ) ) ;
#6903=EDGE_LOOP ( 'NONE', ( #18949, #6072, #12690 ) ) ;
#6908=EDGE_CURVE ( 'NONE', #6782, #8527, #5539, .T. ) ;
#6915=CARTESIAN_POINT ( 'NONE',  ( 51.70000000000002416, 2.428612866367529932E-14, -1.805095852181900386E-13 ) ) ;
#6917=ADVANCED_FACE ( 'NONE', ( #19133 ), #5567, .T. ) ;
#6919=CARTESIAN_POINT ( 'NONE',  ( 22.20365324802978435, 7.487628413149166384, -2.050000000000077538 ) ) ;
#6926=ORIENTED_EDGE ( 'NONE', *, *, #1170, .T. ) ;
#6948=CARTESIAN_POINT ( 'NONE',  ( 52.04553598140720538, 4.350000000000022737, 1.551140582956726632 ) ) ;
#6972=PLANE ( 'NONE',  #16215 ) ;
#6973=CARTESIAN_POINT ( 'NONE',  ( 51.80000000000002558, 6.475000000000062705, 2.049999999999819522 ) ) ;
#6986=CARTESIAN_POINT ( 'NONE',  ( 54.31409749668478071, 6.709390224138188863, -2.050000000000189004 ) ) ;
#6988=EDGE_CURVE ( 'NONE', #9283, #30937, #5010, .T. ) ;
#6989=CARTESIAN_POINT ( 'NONE',  ( 48.00000000000001421, -4.417905791132255899, -1.285520503972909623 ) ) ;
#7034=CARTESIAN_POINT ( 'NONE',  ( 54.44213315155518274, 6.358439074249562672, -1.988253509196054036 ) ) ;
#7038=CARTESIAN_POINT ( 'NONE',  ( 34.56702326949726256, 8.213851659285209550, 1.949999999999879385 ) ) ;
#7046=CIRCLE ( 'NONE', #2472, 0.1000000000000000472 ) ;
#7050=LINE ( 'NONE', #24140, #14561 ) ;
#7057=ORIENTED_EDGE ( 'NONE', *, *, #29281, .T. ) ;
#7071=ORIENTED_EDGE ( 'NONE', *, *, #23641, .T. ) ;
#7074=CARTESIAN_POINT ( 'NONE',  ( 22.07280086217093640, 8.086143481909152442, -1.950000000000076339 ) ) ;
#7077=EDGE_LOOP ( 'NONE', ( #26156, #6349, #312, #948, #13259 ) ) ;
#7080=CARTESIAN_POINT ( 'NONE',  ( 47.00000000000002842, -4.137422847598536180, 2.245380186108497433 ) ) ;
#7104=CARTESIAN_POINT ( 'NONE',  ( 53.91582462592158720, 6.672259099522137582, -2.142504121165067499E-08 ) ) ;
#7115=TOROIDAL_SURFACE ( 'NONE', #12150, 4.199999999999993072, 0.1000000000000000056 ) ;
#7126=DIRECTION ( 'NONE',  ( -3.491481338843133355E-15, 0.000000000000000000, -1.000000000000000000 ) ) ;
#7129=ORIENTED_EDGE ( 'NONE', *, *, #3888, .F. ) ;
#7140=CARTESIAN_POINT ( 'NONE',  ( 47.37826908275614812, -4.356630359622855053, -1.481809601934080511 ) ) ;
#7143=VERTEX_POINT ( 'NONE', #27467 ) ;
#7155=CARTESIAN_POINT ( 'NONE',  ( 51.80000000000002558, 3.954024819382278455, 2.040489646992247774 ) ) ;
#7166=ORIENTED_EDGE ( 'NONE', *, *, #6391, .F. ) ;
#7169=CARTESIAN_POINT ( 'NONE',  ( 54.16322038507460235, 5.604326647956827223, -2.050000000000188116 ) ) ;
#7175=CARTESIAN_POINT ( 'NONE',  ( 51.80000003860129709, 4.055787512326642918, -2.007379997706556285 ) ) ;
#7184=CARTESIAN_POINT ( 'NONE',  ( 54.24492254264022506, 6.702941018009704877, -2.050000000000186340 ) ) ;
#7186=CARTESIAN_POINT ( 'NONE',  ( 51.80000000000002558, 6.475000000000062705, 1.949999999999818767 ) ) ;
#7201=CARTESIAN_POINT ( 'NONE',  ( 34.56269065792917417, 8.313757757582560970, 2.049999999999879030 ) ) ;
#7213=CARTESIAN_POINT ( 'NONE',  ( 53.91678946233206915, 6.821600947619693933, 2.049999999999684963 ) ) ;
#7220=CARTESIAN_POINT ( 'NONE',  ( 52.10591853744708857, 8.701414215152928122, 2.049999999999818190 ) ) ;
#7230=ORIENTED_EDGE ( 'NONE', *, *, #1930, .T. ) ;
#7233=ORIENTED_EDGE ( 'NONE', *, *, #1099, .T. ) ;
#7246=CARTESIAN_POINT ( 'NONE',  ( 53.81464057712626214, 5.799094425976102585, 1.402257142663977829 ) ) ;
#7252=CARTESIAN_POINT ( 'NONE',  ( 47.10000000000000853, -3.550773357292059451, -2.049880134335985815 ) ) ;
#7253=EDGE_LOOP ( 'NONE', ( #2000, #3938, #27313, #18763 ) ) ;
#7259=VERTEX_POINT ( 'NONE', #22745 ) ;
#7272=CARTESIAN_POINT ( 'NONE',  ( 47.54402780054770261, -3.873145847240279771, -1.345634385052774329 ) ) ;
#7276=CARTESIAN_POINT ( 'NONE',  ( 27.27497440150130714, 5.311319583820425017, -1.950000000000095657 ) ) ;
#7279=CARTESIAN_POINT ( 'NONE',  ( 53.29837957427783124, 7.982236199023435397, -1.892846475469884604 ) ) ;
#7284=CARTESIAN_POINT ( 'NONE',  ( 31.59287277085072532, 7.495449159458786426, 1.424999999999890132 ) ) ;
#7292=ORIENTED_EDGE ( 'NONE', *, *, #17751, .T. ) ;
#7308=( NAMED_UNIT ( * ) SI_UNIT ( $, .STERADIAN. ) SOLID_ANGLE_UNIT ( ) );
#7313=CARTESIAN_POINT ( 'NONE',  ( 51.38880644991419189, 3.878826100321112413, -2.050000000000178790 ) ) ;
#7316=DIRECTION ( 'NONE',  ( 3.016910393003118404E-15, 0.000000000000000000, 1.000000000000000000 ) ) ;
#7332=CARTESIAN_POINT ( 'NONE',  ( 47.11820097507338545, -4.249104741286833686, 1.767319601065233892 ) ) ;
#7337=CARTESIAN_POINT ( 'NONE',  ( 50.93264768164066680, -4.319730106884873244, 1.256953381662059055 ) ) ;
#7342=ORIENTED_EDGE ( 'NONE', *, *, #17433, .F. ) ;
#7349=CARTESIAN_POINT ( 'NONE',  ( 29.24156347412778700, 6.028130183534497810, 1.949999999999896261 ) ) ;
#7352=CARTESIAN_POINT ( 'NONE',  ( 53.31748909063354347, 8.199041228893841904, -2.050000000000185452 ) ) ;
#7353=CIRCLE ( 'NONE', #14903, 0.1000000000000000472 ) ;
#7354=LINE ( 'NONE', #24443, #25862 ) ;
#7361=ADVANCED_FACE ( 'NONE', ( #9101 ), #23680, .T. ) ;
#7363=CARTESIAN_POINT ( 'NONE',  ( 51.87416143049284756, 8.598705507415683513, 1.949999999999818767 ) ) ;
#7365=ORIENTED_EDGE ( 'NONE', *, *, #13003, .F. ) ;
#7370=CARTESIAN_POINT ( 'NONE',  ( 52.80968221184929234, 4.034333029853865327, 2.049999999999815969 ) ) ;
#7374=ORIENTED_EDGE ( 'NONE', *, *, #10472, .F. ) ;
#7390=CARTESIAN_POINT ( 'NONE',  ( 52.16611735465125577, 8.588510181879298599, -2.050000000000181011 ) ) ;
#7394=CARTESIAN_POINT ( 'NONE',  ( 31.30720621464603326, 7.411182539856417506, 1.549999999999890798 ) ) ;
#7401=( BOUNDED_CURVE ( )  B_SPLINE_CURVE ( 3, ( #14499, #16580, #16737, #4531 ),
 .UNSPECIFIED., .F., .T. ) 
 B_SPLINE_CURVE_WITH_KNOTS ( ( 4, 4 ),
 ( 3.141592653589793560, 4.712388980384687898 ),
 .UNSPECIFIED. ) 
 CURVE ( )  GEOMETRIC_REPRESENTATION_ITEM ( )  RATIONAL_B_SPLINE_CURVE ( ( 1.000000000000000000, 0.8047378541243654926, 0.8047378541243654926, 1.000000000000000000 ) ) 
 REPRESENTATION_ITEM ( '' )  );
#7421=ADVANCED_FACE ( 'NONE', ( #2909 ), #7115, .T. ) ;
#7429=VECTOR ( 'NONE', #9164, 1000.000000000000114 ) ;
#7433=DIRECTION ( 'NONE',  ( -1.000000000000000000, 0.000000000000000000, 3.491481338843133355E-15 ) ) ;
#7440=CARTESIAN_POINT ( 'NONE',  ( 33.97008042022903851, 8.187964135517418640, -1.950000000000118527 ) ) ;
#7441=TOROIDAL_SURFACE ( 'NONE', #25128, 4.199999999999993072, 0.1000000000000000056 ) ;
#7445=CARTESIAN_POINT ( 'NONE',  ( 52.10570363851881837, 8.590619875341600320, -1.949999390396187637 ) ) ;
#7454=B_SPLINE_CURVE_WITH_KNOTS ( 'NONE', 3,
 ( #14629, #20007, #5601, #24295 ),
 .UNSPECIFIED., .F., .F.,
 ( 4, 4 ),
 ( 0.5073942967076801036, 0.8047316756486366796 ),
 .UNSPECIFIED. ) ;
#7465=ORIENTED_EDGE ( 'NONE', *, *, #26186, .F. ) ;
#7469=AXIS2_PLACEMENT_3D ( 'NONE', #17097, #26105, #31171 ) ;
#7478=CARTESIAN_POINT ( 'NONE',  ( 53.13232117966330037, 4.211086031869615276, -2.050000000000185008 ) ) ;
#7482=CARTESIAN_POINT ( 'NONE',  ( 47.00000000000002132, 2.428612866367529932E-14, -1.640996229256273308E-13 ) ) ;
#7486=EDGE_CURVE ( 'NONE', #22071, #22328, #12553, .T. ) ;
#7493=TOROIDAL_SURFACE ( 'NONE', #25100, 4.199999999999993072, 0.1000000000000000056 ) ;
#7504=B_SPLINE_CURVE_WITH_KNOTS ( 'NONE', 3,
 ( #10997, #13054, #22737, #1033, #14265, #16967, #26615, #30302, #8611, #13514 ),
 .UNSPECIFIED., .F., .F.,
 ( 4, 2, 2, 2, 4 ),
 ( 0.000000000000000000, 0.0003923015305839671263, 0.0007846030611679342525, 0.001176904591751901270, 0.001569206122335868505 ),
 .UNSPECIFIED. ) ;
#7515=CARTESIAN_POINT ( 'NONE',  ( 32.57869118518240015, 7.908463454149416982, 2.049999999999884803 ) ) ;
#7517=AXIS2_PLACEMENT_3D ( 'NONE', #29647, #673, #5600 ) ;
#7528=EDGE_CURVE ( 'NONE', #13195, #13128, #7454, .T. ) ;
#7533=MECHANICAL_DESIGN_GEOMETRIC_PRESENTATION_REPRESENTATION('',(#28252),#15110);
#7545=CARTESIAN_POINT ( 'NONE',  ( 34.56702326949726256, 8.213851659285209550, 1.949999999999879163 ) ) ;
#7547=CARTESIAN_POINT ( 'NONE',  ( 29.24156346101471016, 6.028130203021968114, -2.050000000000362199 ) ) ;
#7556=CARTESIAN_POINT ( 'NONE',  ( 51.87765138016307986, 8.698644590117595499, -2.050000000000180123 ) ) ;
#7566=CARTESIAN_POINT ( 'NONE',  ( 54.07864988756197988, 6.687439357893800285, 2.033314590869161442 ) ) ;
#7575=ORIENTED_EDGE ( 'NONE', *, *, #11711, .F. ) ;
#7576=LINE ( 'NONE', #2520, #27514 ) ;
#7578=CIRCLE ( 'NONE', #16697, 0.1000000000000001443 ) ;
#7592=( BOUNDED_SURFACE ( )  B_SPLINE_SURFACE ( 2, 3, ( 
 ( #17475, #19401, #10340, #29656, #27129, #5448, #24756, #3066, #29043, #20013, #12712, #17645, #4812, #7352, #21940, #9885, #29205, #17182 ),
 ( #26827, #27602, #5637, #2494, #19756, #24475, #2786, #12149, #570, #20061, #22130, #3099, #26858, #24792, #2952, #29242, #7841, #19604 ),
 ( #29385, #22426, #17516, #15288, #12597, #2644, #19897, #718, #29526, #21828, #22282, #29697, #10228, #27171, #5483, #27002, #116, #7556 ),
 ( #17216, #5165, #10080, #15135, #12750, #8017, #14814, #14970, #10378, #12437, #17682, #7697, #27325, #9771, #19436, #29082, #7390, #17068 ),
 ( #26724, #17355, #5308, #422, #5014, #24638, #14675, #24335, #12284, #21971, #260, #9924, #30466, #3880, #27943, #5964, #13530, #15904 ) ),
 .UNSPECIFIED., .F., .F., .F. ) 
 B_SPLINE_SURFACE_WITH_KNOTS ( ( 3, 2, 3 ),
 ( 4, 2, 2, 2, 2, 2, 2, 2, 4 ),
 ( -0.01000000000000000021, 0.000000000000000000, 1.000000000000000000 ),
 ( 1.413716694115406902, 1.826050729899067360, 2.238384765682727817, 2.650718801466387831, 3.063052837250048288, 3.475386873033708746, 3.887720908817368759, 4.300054944601029661, 4.712388980384689674 ),
 .UNSPECIFIED. ) 
 GEOMETRIC_REPRESENTATION_ITEM ( )  RATIONAL_B_SPLINE_SURFACE ( (
 ( 1.000000000000000000, 1.000000000000000000, 1.000000000000000000, 1.000000000000000000, 1.000000000000000000, 1.000000000000000000, 1.000000000000000000, 1.000000000000000000, 1.000000000000000000, 1.000000000000000000, 1.000000000000000000, 1.000000000000000000, 1.000000000000000000, 1.000000000000000000, 1.000000000000000000, 1.000000000000000000, 1.000000000000000000, 1.000000000000000000),
 ( 1.000000000000000000, 1.000000000000000000, 1.000000000000000000, 1.000000000000000000, 1.000000000000000000, 1.000000000000000000, 1.000000000000000000, 1.000000000000000000, 1.000000000000000000, 1.000000000000000000, 1.000000000000000000, 1.000000000000000000, 1.000000000000000000, 1.000000000000000000, 1.000000000000000000, 1.000000000000000000, 1.000000000000000000, 1.000000000000000000),
 ( 1.000000000000000000, 1.000000000000000000, 1.000000000000000000, 1.000000000000000000, 1.000000000000000000, 1.000000000000000000, 1.000000000000000000, 1.000000000000000000, 1.000000000000000000, 1.000000000000000000, 1.000000000000000000, 1.000000000000000000, 1.000000000000000000, 1.000000000000000000, 1.000000000000000000, 1.000000000000000000, 1.000000000000000000, 1.000000000000000000),
 ( 0.7071067811865476838, 0.7071067811865476838, 0.7071067811865475727, 0.7071067811865475727, 0.7071067811865476838, 0.7071067811865476838, 0.7071067811865475727, 0.7071067811865475727, 0.7071067811865473507, 0.7071067811865473507, 0.7071067811865479058, 0.7071067811865479058, 0.7071067811865475727, 0.7071067811865475727, 0.7071067811865463515, 0.7071067811865463515, 0.7071067811865475727, 0.7071067811865475727),
 ( 1.000000000000000000, 1.000000000000000000, 1.000000000000000000, 1.000000000000000000, 1.000000000000000000, 1.000000000000000000, 1.000000000000000000, 1.000000000000000000, 1.000000000000000000, 1.000000000000000000, 1.000000000000000000, 1.000000000000000000, 1.000000000000000000, 1.000000000000000000, 1.000000000000000000, 1.000000000000000000, 1.000000000000000000, 1.000000000000000000) ) ) 
 REPRESENTATION_ITEM ( '' )  SURFACE ( )  );
#7595=CARTESIAN_POINT ( 'NONE',  ( 22.00209989016466494, 7.765045920621504116, -1.950000000000076561 ) ) ;
#7602=CARTESIAN_POINT ( 'NONE',  ( 25.48092967892656446, 5.262749364038179500, 1.424999999999912337 ) ) ;
#7610=CARTESIAN_POINT ( 'NONE',  ( 47.05963571244990362, 8.266527678078146479, -1.550000000000163469 ) ) ;
#7618=CARTESIAN_POINT ( 'NONE',  ( 47.09453520915242564, 9.265918505097243241, -1.950000000000163380 ) ) ;
#7641=CARTESIAN_POINT ( 'NONE',  ( 54.19386703870443966, 5.671865141453449333, 1.949999999999810329 ) ) ;
#7644=CARTESIAN_POINT ( 'NONE',  ( 51.80000000000001847, 2.428612866367529932E-14, -1.808587333520743709E-13 ) ) ;
#7662=FACE_OUTER_BOUND ( 'NONE', #31089, .T. ) ;
#7674=EDGE_CURVE ( 'NONE', #26805, #7259, #27327, .T. ) ;
#7683=VERTEX_POINT ( 'NONE', #16149 ) ;
#7684=CARTESIAN_POINT ( 'NONE',  ( 50.93175545242106494, -4.417905783403957898, -1.285520530455074528 ) ) ;
#7689=CARTESIAN_POINT ( 'NONE',  ( 32.30803788188134718, 7.816246126569818209, -1.950000000000048361 ) ) ;
#7697=CARTESIAN_POINT ( 'NONE',  ( 53.74478519188836856, 7.379842749953419379, -2.050000000000249401 ) ) ;
#7710=ORIENTED_EDGE ( 'NONE', *, *, #30988, .T. ) ;
#7719=CARTESIAN_POINT ( 'NONE',  ( 52.41501436764352206, 3.996684283499680745, 2.045735246708100696 ) ) ;
#7730=CARTESIAN_POINT ( 'NONE',  ( 51.70000000000003126, -3.550773357292059007, 2.049880134335640758 ) ) ;
#7762=ORIENTED_EDGE ( 'NONE', *, *, #4741, .T. ) ;
#7764=CARTESIAN_POINT ( 'NONE',  ( 54.16553928697275921, 6.951169537962178069, -2.050000000000189448 ) ) ;
#7773=PRODUCT ( 'Pocket Clip', 'Pocket Clip', '', ( #18228 ) ) ;
#7777=DIRECTION ( 'NONE',  ( 3.491481338843133355E-15, 0.000000000000000000, 1.000000000000000000 ) ) ;
#7778=EDGE_CURVE ( 'NONE', #22413, #9758, #26579, .T. ) ;
#7781=CARTESIAN_POINT ( 'NONE',  ( 47.73554962785864575, -4.311893144378706744, -1.282556980650735978 ) ) ;
#7782=CARTESIAN_POINT ( 'NONE',  ( 48.00000000000003553, -4.417905791132258564, 1.285520503972574557 ) ) ;
#7783=ORIENTED_EDGE ( 'NONE', *, *, #28785, .T. ) ;
#7789=ORIENTED_EDGE ( 'NONE', *, *, #2651, .F. ) ;
#7793=CARTESIAN_POINT ( 'NONE',  ( 32.53491908475320571, 7.895085025454613437, 1.949999999999886713 ) ) ;
#7800=CARTESIAN_POINT ( 'NONE',  ( 51.70000000000002416, 2.428612866367529932E-14, -1.805095852181900386E-13 ) ) ;
#7801=CARTESIAN_POINT ( 'NONE',  ( 26.61920844897847260, 5.219578739559102232, 2.049999999999775113 ) ) ;
#7816=CARTESIAN_POINT ( 'NONE',  ( 51.68129744679068693, 4.333300462216209681, 2.050000000000262279 ) ) ;
#7828=CARTESIAN_POINT ( 'NONE',  ( 51.03681636671011290, -4.380055612571975843, -1.406160842577909964 ) ) ;
#7829=VERTEX_POINT ( 'NONE', #28657 ) ;
#7831=EDGE_CURVE ( 'NONE', #24006, #15457, #14696, .T. ) ;
#7833=CARTESIAN_POINT ( 'NONE',  ( 31.73163254175006287, 7.673342708999780548, -2.050000000000110401 ) ) ;
#7834=ORIENTED_EDGE ( 'NONE', *, *, #228, .F. ) ;
#7836=CARTESIAN_POINT ( 'NONE',  ( 50.80000000000001847, -4.003661535119149129, -1.269131321892095654 ) ) ;
#7841=CARTESIAN_POINT ( 'NONE',  ( 52.18331218360314949, 8.688678219032366812, -2.050000000000181455 ) ) ;
#7843=CARTESIAN_POINT ( 'NONE',  ( 50.22478246037407246, 8.164214000976986796, 2.049999999999824851 ) ) ;
#7845=DIRECTION ( 'NONE',  ( 1.000000000000000000, 0.000000000000000000, -3.491481338843133355E-15 ) ) ;
#7848=ADVANCED_FACE ( 'NONE', ( #23757 ), #6972, .T. ) ;
#7856=CARTESIAN_POINT ( 'NONE',  ( 54.38834410771541172, 6.716312262692355262, 2.020140340243033350 ) ) ;
#7862=CARTESIAN_POINT ( 'NONE',  ( 47.10000000000003695, 6.982261990806648555E-14, 4.599999999999874412 ) ) ;
#7865=DIRECTION ( 'NONE',  ( -0.03489949670250097613, -0.9993908270190957621, 0.000000000000000000 ) ) ;
#7872=CARTESIAN_POINT ( 'NONE',  ( 52.35001713925458944, 3.980960944483503017, 2.045629575386918919 ) ) ;
#7884=EDGE_CURVE ( 'NONE', #26613, #27565, #19637, .T. ) ;
#7899=CARTESIAN_POINT ( 'NONE',  ( 22.79065618564551343, 6.593681752169803012, 2.049999999999919442 ) ) ;
#7914=CARTESIAN_POINT ( 'NONE',  ( 47.38204862782191640, -3.967700393345040766, 1.365904513876657456 ) ) ;
#7934=CARTESIAN_POINT ( 'NONE',  ( 53.94136487687683967, 6.599443998687462454, -1.761196874214848052 ) ) ;
#7945=DIRECTION ( 'NONE',  ( 0.000000000000000000, 0.8740818021021506956, 0.4857787595540346559 ) ) ;
#7955=CARTESIAN_POINT ( 'NONE',  ( 47.19248715958271845, -4.291463206566032085, 1.660299764304369319 ) ) ;
#7964=VERTEX_POINT ( 'NONE', #8205 ) ;
#7965=ORIENTED_EDGE ( 'NONE', *, *, #7, .F. ) ;
#7969=CARTESIAN_POINT ( 'NONE',  ( 27.74852811682016096, 5.417024961191244437, 1.949999999999903810 ) ) ;
#7976=DIRECTION ( 'NONE',  ( 0.9993908270190956511, -0.03489949670250096919, -3.491481338843132961E-15 ) ) ;
#7977=CARTESIAN_POINT ( 'NONE',  ( 23.07431837909872741, 6.199584074734312722, 1.949999999999919575 ) ) ;
#8005=CARTESIAN_POINT ( 'NONE',  ( 54.22146708689643191, 6.361260388417356637, -2.050000000000189004 ) ) ;
#8007=VERTEX_POINT ( 'NONE', #10116 ) ;
#8009=VERTEX_POINT ( 'NONE', #27506 ) ;
#8010=CARTESIAN_POINT ( 'NONE',  ( 26.00343446089717148, 5.312306467083453221, -2.050000000000090417 ) ) ;
#8011=ORIENTED_EDGE ( 'NONE', *, *, #944, .T. ) ;
#8017=CARTESIAN_POINT ( 'NONE',  ( 53.29207122288455878, 4.934008984266823994, -2.050000000000185896 ) ) ;
#8020=DIRECTION ( 'NONE',  ( -1.000000000000000000, -0.000000000000000000, 3.491481338843133355E-15 ) ) ;
#8030=CARTESIAN_POINT ( 'NONE',  ( 54.41366571437519895, 6.718673005292168376, -1.963089969304977700 ) ) ;
#8036=CARTESIAN_POINT ( 'NONE',  ( 51.59759607754882182, -3.813771782910184260, -1.508835477669506098 ) ) ;
#8045=ORIENTED_EDGE ( 'NONE', *, *, #22825, .T. ) ;
#8060=AXIS2_PLACEMENT_3D ( 'NONE', #31023, #16943, #26588 ) ;
#8067=CARTESIAN_POINT ( 'NONE',  ( 30.16244940506470229, 6.784331066303296964, 2.049999999999894129 ) ) ;
#8080=CARTESIAN_POINT ( 'NONE',  ( 29.69543387591358652, 6.938696499881336521, -1.425000000000103517 ) ) ;
#8085=CARTESIAN_POINT ( 'NONE',  ( 51.80000000000001137, 3.949999999998452971, -1.950000000000180256 ) ) ;
#8088=ADVANCED_FACE ( 'NONE', ( #18342 ), #8806, .T. ) ;
#8090=ORIENTED_EDGE ( 'NONE', *, *, #29132, .T. ) ;
#8094=CARTESIAN_POINT ( 'NONE',  ( 52.61915120152464453, 4.492597126270361230, -1.565330858589896845 ) ) ;
#8122=CARTESIAN_POINT ( 'NONE',  ( 52.06789853512057675, 4.366897080361537675, -1.445771047857228542 ) ) ;
#8127=CARTESIAN_POINT ( 'NONE',  ( 26.00343446089713240, 5.312306467083714345, 2.049999999999908784 ) ) ;
#8136=VECTOR ( 'NONE', #2563, 1000.000000000000000 ) ;
#8139=DIRECTION ( 'NONE',  ( 3.083952846180964840E-15, 8.881784197001241477E-16, 1.000000000000000000 ) ) ;
#8141=CARTESIAN_POINT ( 'NONE',  ( 53.97819099888265271, 5.744223774131685722, 2.011101020406490747 ) ) ;
#8155=CARTESIAN_POINT ( 'NONE',  ( 53.81464057712624793, 5.799094425976102585, -1.689602626210267466 ) ) ;
#8160=CARTESIAN_POINT ( 'NONE',  ( 31.33102771648032459, 7.478136438692663646, -2.050000000000108180 ) ) ;
#8168=CARTESIAN_POINT ( 'NONE',  ( 47.44326941947779375, -3.851351755029098101, 1.408485093544704192 ) ) ;
#8169=CARTESIAN_POINT ( 'NONE',  ( 47.00000000000000711, -3.700421601131886007, -1.984561589293904582 ) ) ;
#8170=AXIS2_PLACEMENT_3D ( 'NONE', #12358, #2415, #19367 ) ;
#8174=CARTESIAN_POINT ( 'NONE',  ( 51.80288952865482344, -4.086537470739417088, 2.116255473933748910 ) ) ;
#8177=DIRECTION ( 'NONE',  ( 0.9993908270190957621, -0.03489949670250100389, -3.492120980335537899E-15 ) ) ;
#8182=CARTESIAN_POINT ( 'NONE',  ( 54.28867365409853107, 5.640057820322910587, -0.9750000000001823874 ) ) ;
#8205=CARTESIAN_POINT ( 'NONE',  ( 34.56702326949724835, 8.213851659285209550, -1.550000000000119948 ) ) ;
#8207=ORIENTED_EDGE ( 'NONE', *, *, #4693, .F. ) ;
#8214=CARTESIAN_POINT ( 'NONE',  ( 23.38432935081488395, 6.109573960516228475, 2.049999999999918554 ) ) ;
#8219=UNCERTAINTY_MEASURE_WITH_UNIT (LENGTH_MEASURE( 1.000000000000000082E-05 ), #19508, 'distance_accuracy_value', 'NONE');
#8229=FACE_OUTER_BOUND ( 'NONE', #10103, .T. ) ;
#8239=CARTESIAN_POINT ( 'NONE',  ( 52.11477178369203500, 3.843881278534198476, -2.050000000000181455 ) ) ;
#8244=CYLINDRICAL_SURFACE ( 'NONE', #5940, 0.1000000000000000472 ) ;
#8260=CARTESIAN_POINT ( 'NONE',  ( 54.23831472968567624, 6.535030234825929263, 2.049999999999810640 ) ) ;
#8270=ORIENTED_EDGE ( 'NONE', *, *, #4217, .T. ) ;
#8274=CARTESIAN_POINT ( 'NONE',  ( 23.88937651017007369, 5.720041407194654148, 1.949999999999850075 ) ) ;
#8283=CARTESIAN_POINT ( 'NONE',  ( 51.80000000000001137, -3.936726248589971444, -1.145507068360074765 ) ) ;
#8285=( BOUNDED_SURFACE ( )  B_SPLINE_SURFACE ( 3, 2, ( 
 ( #7201, #9736, #14631 ),
 ( #9592, #28570, #26355 ),
 ( #4658, #22086, #12396 ),
 ( #21936, #7515, #26823 ),
 ( #16865, #381, #18925 ),
 ( #6879, #16550, #11787 ),
 ( #19251, #14312, #17177 ),
 ( #4808, #26200, #26678 ),
 ( #4505, #4976, #2280 ),
 ( #23982, #5126, #29039 ),
 ( #24296, #2606, #29202 ),
 ( #11943, #14470, #14779 ),
 ( #12252, #75, #31264 ),
 ( #19398, #2452, #7349 ),
 ( #24143, #21633, #14160 ),
 ( #23833, #21790, #31093 ),
 ( #220, #9881, #19556 ),
 ( #24439, #20009, #10336 ),
 ( #10511, #7801, #20338 ),
 ( #8127, #10044, #5272 ),
 ( #27123, #5445, #15980 ),
 ( #26963, #29650, #17798 ),
 ( #12707, #5749, #22539 ),
 ( #3214, #20183, #27285 ),
 ( #1006, #29966, #8274 ),
 ( #17318, #19714, #3063 ),
 ( #12857, #843, #7977 ),
 ( #14922, #17640, #5602 ),
 ( #25051, #13593, #29815 ),
 ( #27436, #530, #17471 ),
 ( #15398, #10660, #6326 ),
 ( #17942, #27585, #15250 ),
 ( #3380, #15095, #13030 ),
 ( #24753, #24896, #22711 ) ),
 .UNSPECIFIED., .F., .F., .F. ) 
 B_SPLINE_SURFACE_WITH_KNOTS ( ( 4, 2, 2, 2, 2, 2, 2, 2, 2, 2, 2, 2, 2, 2, 2, 2, 4 ),
 ( 3, 3 ),
 ( -1.734723475976807094E-18, 0.001741451497654487477, 0.002612177246481731975, 0.003047540120895354115, 0.003482902995308976690, 0.004353628744136221404, 0.005224354492963465685, 0.006965805990617955114, 0.007836531739445200262, 0.008707257488272444543, 0.009577983237099688824, 0.01044870898592693310, 0.01131943473475417739, 0.01219016048358142340, 0.01262552335799504641, 0.01306088623240866768, 0.01393161198123591196 ),
 ( 0.000000000000000000, 1.000000000000000000 ),
 .UNSPECIFIED. ) 
 GEOMETRIC_REPRESENTATION_ITEM ( )  RATIONAL_B_SPLINE_SURFACE ( (
 ( 1.000000000000000000, 0.7071067811865467956, 1.000000000000000000),
 ( 1.000000000000000000, 0.7071067811865467956, 1.000000000000000000),
 ( 1.000000000000000000, 0.7071067811865482389, 1.000000000000000000),
 ( 1.000000000000000000, 0.7071067811865482389, 1.000000000000000000),
 ( 1.000000000000000000, 0.7071067811865467956, 1.000000000000000000),
 ( 1.000000000000000000, 0.7071067811865467956, 1.000000000000000000),
 ( 1.000000000000000000, 0.7071067811865475727, 1.000000000000000000),
 ( 1.000000000000000000, 0.7071067811865475727, 1.000000000000000000),
 ( 1.000000000000000000, 0.7071067811865425767, 1.000000000000000000),
 ( 1.000000000000000000, 0.7071067811865425767, 1.000000000000000000),
 ( 1.000000000000000000, 0.7071067811865441310, 1.000000000000000000),
 ( 1.000000000000000000, 0.7071067811865441310, 1.000000000000000000),
 ( 1.000000000000000000, 0.7071067811865494601, 1.000000000000000000),
 ( 1.000000000000000000, 0.7071067811865494601, 1.000000000000000000),
 ( 1.000000000000000000, 0.7071067811865467956, 1.000000000000000000),
 ( 1.000000000000000000, 0.7071067811865467956, 1.000000000000000000),
 ( 1.000000000000000000, 0.7071067811865406894, 1.000000000000000000),
 ( 1.000000000000000000, 0.7071067811865406894, 1.000000000000000000),
 ( 1.000000000000000000, 0.7071067811865483499, 1.000000000000000000),
 ( 1.000000000000000000, 0.7071067811865483499, 1.000000000000000000),
 ( 1.000000000000000000, 0.7071067811865475727, 1.000000000000000000),
 ( 1.000000000000000000, 0.7071067811865475727, 1.000000000000000000),
 ( 1.000000000000000000, 0.7071067811865475727, 1.000000000000000000),
 ( 1.000000000000000000, 0.7071067811865475727, 1.000000000000000000),
 ( 1.000000000000000000, 0.7071067811865497932, 1.000000000000000000),
 ( 1.000000000000000000, 0.7071067811865497932, 1.000000000000000000),
 ( 1.000000000000000000, 0.7071067811865565655, 1.000000000000000000),
 ( 1.000000000000000000, 0.7071067811865565655, 1.000000000000000000),
 ( 1.000000000000000000, 0.7071067811865490160, 1.000000000000000000),
 ( 1.000000000000000000, 0.7071067811865490160, 1.000000000000000000),
 ( 1.000000000000000000, 0.7071067811865389130, 1.000000000000000000),
 ( 1.000000000000000000, 0.7071067811865389130, 1.000000000000000000),
 ( 1.000000000000000000, 0.7071067811865361374, 1.000000000000000000),
 ( 1.000000000000000000, 0.7071067811865361374, 1.000000000000000000) ) ) 
 REPRESENTATION_ITEM ( '' )  SURFACE ( )  );
#8309=B_SPLINE_CURVE_WITH_KNOTS ( 'NONE', 3,
 ( #22366, #21768, #12374, #5580, #509, #26650, #12090, #7781, #17157, #24120 ),
 .UNSPECIFIED., .F., .F.,
 ( 4, 2, 2, 2, 4 ),
 ( 4.336808689942017255E-19, 0.0003923434276460365509, 0.0007846868552920726681, 0.001177030282938108839, 0.001569373710584144902 ),
 .UNSPECIFIED. ) ;
#8310=CARTESIAN_POINT ( 'NONE',  ( 54.41366571437522026, 6.718673005292167488, 1.976179938779723422 ) ) ;
#8311=DIRECTION ( 'NONE',  ( -1.000000000000000000, 0.000000000000000000, 3.491481338843133355E-15 ) ) ;
#8316=CARTESIAN_POINT ( 'NONE',  ( 47.73776917354344818, -3.930699233196665254, -1.170919866331572079 ) ) ;
#8322=CARTESIAN_POINT ( 'NONE',  ( 51.30632327778202040, -4.280384112422016329, 1.378579207634347936 ) ) ;
#8326=VECTOR ( 'NONE', #15423, 1000.000000000000000 ) ;
#8329=CARTESIAN_POINT ( 'NONE',  ( 54.44213313387141540, 6.358439080500951412, 1.988253682540942258 ) ) ;
#8344=DIRECTION ( 'NONE',  ( -3.489354422748178582E-15, 1.218509414717996338E-16, -1.000000000000000000 ) ) ;
#8345=VECTOR ( 'NONE', #26950, 1000.000000000000114 ) ;
#8346=CARTESIAN_POINT ( 'NONE',  ( 47.05963571244991783, 8.266527678078146479, 1.549999999999835953 ) ) ;
#8347=ORIENTED_EDGE ( 'NONE', *, *, #3822, .F. ) ;
#8352=AXIS2_PLACEMENT_3D ( 'NONE', #27725, #6190, #15837 ) ;
#8357=CIRCLE ( 'NONE', #8871, 2.625000000001610267 ) ;
#8364=CARTESIAN_POINT ( 'NONE',  ( 22.26232992071278005, 7.345532757394721557, 2.049999999999922551 ) ) ;
#8376=CARTESIAN_POINT ( 'NONE',  ( 31.35411506066951404, 7.935106535555555674, 1.424999999999890354 ) ) ;
#8379=CARTESIAN_POINT ( 'NONE',  ( 51.86020163181182596, 8.198949176608044453, -1.950000000000180256 ) ) ;
#8385=CYLINDRICAL_SURFACE ( 'NONE', #17983, 1.000000000000000000 ) ;
#8386=MECHANICAL_DESIGN_GEOMETRIC_PRESENTATION_REPRESENTATION('',(#9426),#21043);
#8391=CARTESIAN_POINT ( 'NONE',  ( 52.05393800078974209, 4.345106731198625560, -2.050000000000180567 ) ) ;
#8401=CARTESIAN_POINT ( 'NONE',  ( 51.80000000000001137, 3.850000000000016520, -2.050000000000180123 ) ) ;
#8407=ADVANCED_FACE ( 'NONE', ( #14967 ), #14749, .T. ) ;
#8416=CARTESIAN_POINT ( 'NONE',  ( 52.45567523936519905, 8.517307475678896012, 2.049999999999817302 ) ) ;
#8429=ORIENTED_EDGE ( 'NONE', *, *, #10188, .T. ) ;
#8435=VECTOR ( 'NONE', #4155, 999.9999999999998863 ) ;
#8457=ORIENTED_EDGE ( 'NONE', *, *, #31125, .T. ) ;
#8469=CARTESIAN_POINT ( 'NONE',  ( 51.77443163147427896, -4.052038242240612043, -1.950335525115999502 ) ) ;
#8473=CARTESIAN_POINT ( 'NONE',  ( 22.41225425283442618, 6.886225701513755126, -2.050000000000144595 ) ) ;
#8477=CARTESIAN_POINT ( 'NONE',  ( 47.12303005161511038, -3.663337715290890362, 1.844354128036148843 ) ) ;
#8481=CARTESIAN_POINT ( 'NONE',  ( 48.00000000000002132, -3.908336260473454615, 1.238913909465752194 ) ) ;
#8494=CARTESIAN_POINT ( 'NONE',  ( 54.38981513202823947, 6.361385888908016817, -2.043118470513792140 ) ) ;
#8496=CARTESIAN_POINT ( 'NONE',  ( 51.59708304119570954, -3.814011388176574702, 1.508225752246529883 ) ) ;
#8502=ORIENTED_EDGE ( 'NONE', *, *, #31055, .T. ) ;
#8509=DIRECTION ( 'NONE',  ( -0.9993908270190958731, 0.03489949670250096919, 3.491595022110081325E-15 ) ) ;
#8527=VERTEX_POINT ( 'NONE', #13527 ) ;
#8538=CARTESIAN_POINT ( 'NONE',  ( 31.35411506066950693, 7.935106535555555674, -1.425000000000108846 ) ) ;
#8539=CARTESIAN_POINT ( 'NONE',  ( 51.06284382647740472, -4.312058781922653239, -1.282041952414082475 ) ) ;
#8540=CYLINDRICAL_SURFACE ( 'NONE', #17567, 160.1997717543138720 ) ;
#8547=EDGE_CURVE ( 'NONE', #125, #10074, #16078, .T. ) ;
#8558=CARTESIAN_POINT ( 'NONE',  ( 52.94597018949752965, 4.198214444775582699, -2.047133864835171124 ) ) ;
#8560=CARTESIAN_POINT ( 'NONE',  ( 51.80000000000001137, 4.175664755576646847, -1.929721184274108436 ) ) ;
#8568=CARTESIAN_POINT ( 'NONE',  ( 51.65273894882759009, 3.822289909571943145, 2.049999999999813305 ) ) ;
#8569=CARTESIAN_POINT ( 'NONE',  ( 24.05318950684998924, 5.396204383593524945, -1.550000000000083533 ) ) ;
#8590=CARTESIAN_POINT ( 'NONE',  ( 25.48092967892657512, 5.262749364038175059, -1.425000000000088862 ) ) ;
#8602=CARTESIAN_POINT ( 'NONE',  ( 53.86856682907188798, 7.562246134602117920, -2.050000000000188116 ) ) ;
#8608=ORIENTED_EDGE ( 'NONE', *, *, #4741, .F. ) ;
#8609=CARTESIAN_POINT ( 'NONE',  ( 34.56269065792915995, 8.313757757582562746, -2.050000000000119726 ) ) ;
#8611=CARTESIAN_POINT ( 'NONE',  ( 47.00000000000002842, -3.995259070520241540, 2.068697874511656654 ) ) ;
#8619=CARTESIAN_POINT ( 'NONE',  ( 22.61091062455492562, 6.637672123835907101, -1.950000000000045253 ) ) ;
#8641=CARTESIAN_POINT ( 'NONE',  ( 50.80000000000002558, -4.031600731908414836, 1.173113608511496597 ) ) ;
#8644=CARTESIAN_POINT ( 'NONE',  ( 52.91918222397609384, 8.304852724747799897, 1.919164453910085610 ) ) ;
#8647=CARTESIAN_POINT ( 'NONE',  ( 51.80000000000001137, -3.550773357292064780, -2.049880134336005799 ) ) ;
#8651=CARTESIAN_POINT ( 'NONE',  ( 27.81714062797481191, 5.541011620835246454, -2.050000000000097522 ) ) ;
#8659=B_SPLINE_CURVE_WITH_KNOTS ( 'NONE', 3,
 ( #19607, #9772, #7394, #23878, #28620, #17073, #16602, #26725, #26245 ),
 .UNSPECIFIED., .F., .F.,
 ( 4, 1, 1, 1, 1, 1, 4 ),
 ( 0.000000000000000000, 0.08990530927501938496, 0.2069505209790863942, 0.2957249676700259844, 0.5865340158044511920, 0.7553074047937105018, 0.9685669348269267953 ),
 .UNSPECIFIED. ) ;
#8683=CARTESIAN_POINT ( 'NONE',  ( 29.29107486424064177, 6.659593085418572755, -1.425000000000101963 ) ) ;
#8691=CARTESIAN_POINT ( 'NONE',  ( 41.48619405471883681, -151.3359592902621955, -2.050000000000163691 ) ) ;
#8696=EDGE_CURVE ( 'NONE', #10424, #9403, #1605, .T. ) ;
#8698=DIRECTION ( 'NONE',  ( 3.083952846180964840E-15, 0.000000000000000000, 1.000000000000000000 ) ) ;
#8702=CARTESIAN_POINT ( 'NONE',  ( 52.43766309949614168, 4.002594832745192122, -2.045777940973402043 ) ) ;
#8703=DIRECTION ( 'NONE',  ( 1.000000000000000000, 0.000000000000000000, -3.491481338843133355E-15 ) ) ;
#8710=CARTESIAN_POINT ( 'NONE',  ( 47.02562379653426206, -3.759602463706844144, -1.865002073832594975 ) ) ;
#8713=CARTESIAN_POINT ( 'NONE',  ( 53.31748909063355768, 8.199041228893841904, 2.049999999999814193 ) ) ;
#8720=CARTESIAN_POINT ( 'NONE',  ( 47.12198605825954445, -4.132863666287243554, -2.022846738277279233 ) ) ;
#8731=CARTESIAN_POINT ( 'NONE',  ( 22.44093457455321783, 6.836382162713701582, -1.425000000000078426 ) ) ;
#8737=CARTESIAN_POINT ( 'NONE',  ( 51.70000000000002416, 6.982261990806648555E-14, -1.793082891011605378E-13 ) ) ;
#8740=CARTESIAN_POINT ( 'NONE',  ( 53.94245690748189048, 6.674762429336749570, 1.915449902665258275 ) ) ;
#8743=DIRECTION ( 'NONE',  ( 0.9993908270191184107, -0.03489949670185085034, -3.491481338843133355E-15 ) ) ;
#8744=( LENGTH_UNIT ( ) NAMED_UNIT ( * ) SI_UNIT ( .MILLI., .METRE. ) );
#8756=ORIENTED_EDGE ( 'NONE', *, *, #17396, .T. ) ;
#8759=ORIENTED_EDGE ( 'NONE', *, *, #17518, .F. ) ;
#8760=CARTESIAN_POINT ( 'NONE',  ( 23.07431837909838634, 6.199584074734630690, -1.950000000000079670 ) ) ;
#8772=DIRECTION ( 'NONE',  ( -0.9993908270190957621, 0.03489949670250100389, 3.492120980335537899E-15 ) ) ;
#8775=CARTESIAN_POINT ( 'NONE',  ( 51.77496349830696687, -4.051364836626919264, 1.951815467915475777 ) ) ;
#8780=DIRECTION ( 'NONE',  ( -1.000000000000000000, -0.000000000000000000, 3.491481338843133355E-15 ) ) ;
#8785=CARTESIAN_POINT ( 'NONE',  ( 51.70000000000003126, -3.550773357292059007, 2.049880134335641202 ) ) ;
#8787=CARTESIAN_POINT ( 'NONE',  ( 52.11477178369204921, 3.843881278534198476, 2.049999999999818190 ) ) ;
#8796=B_SPLINE_CURVE_WITH_KNOTS ( 'NONE', 3,
 ( #29688, #10542, #22890, #1038, #3420, #12888, #17828, #17671, #29846, #5951 ),
 .UNSPECIFIED., .F., .F.,
 ( 4, 2, 2, 2, 4 ),
 ( 0.000000000000000000, 3.859340476725683618E-05, 7.718680953451367236E-05, 0.0001543736190690279410, 0.0003087472381380618452 ),
 .UNSPECIFIED. ) ;
#8806=CYLINDRICAL_SURFACE ( 'NONE', #26887, 2.625000000001610267 ) ;
#8809=EDGE_CURVE ( 'NONE', #17711, #15786, #5274, .T. ) ;
#8814=AXIS2_PLACEMENT_3D ( 'NONE', #22870, #3686, #20347 ) ;
#8823=ORIENTED_EDGE ( 'NONE', *, *, #19750, .F. ) ;
#8838=CARTESIAN_POINT ( 'NONE',  ( 52.69134963215454803, 4.542747918341202507, -1.570391857504957134 ) ) ;
#8840=EDGE_CURVE ( 'NONE', #10424, #5154, #19341, .T. ) ;
#8855=VECTOR ( 'NONE', #17382, 1000.000000000000114 ) ;
#8857=CARTESIAN_POINT ( 'NONE',  ( 47.73415789227374972, -4.410482998349072759, -1.311567113539440221 ) ) ;
#8865=DIRECTION ( 'NONE',  ( 3.491481338843133355E-15, 0.000000000000000000, 1.000000000000000000 ) ) ;
#8869=CARTESIAN_POINT ( 'NONE',  ( 53.82520270936416296, 4.899646637710924679, 2.049999999999811973 ) ) ;
#8871=AXIS2_PLACEMENT_3D ( 'NONE', #22463, #23213, #27941 ) ;
#8874=EDGE_LOOP ( 'NONE', ( #18914, #3079, #21519, #2086 ) ) ;
#8883=ADVANCED_FACE ( 'NONE', ( #15359 ), #10622, .T. ) ;
#8885=AXIS2_PLACEMENT_3D ( 'NONE', #13368, #23062, #11027 ) ;
#8890=CARTESIAN_POINT ( 'NONE',  ( 51.80000000000002558, 4.349402395915089592, 1.698746272247092959 ) ) ;
#8891=AXIS2_PLACEMENT_3D ( 'NONE', #20868, #1678, #13386 ) ;
#8905=AXIS2_PLACEMENT_3D ( 'NONE', #9229, #18581, #13948 ) ;
#8910=CIRCLE ( 'NONE', #8885, 4.199999999999993072 ) ;
#8927=AXIS2_PLACEMENT_3D ( 'NONE', #15411, #27598, #15732 ) ;
#8932=VERTEX_POINT ( 'NONE', #2053 ) ;
#8958=CARTESIAN_POINT ( 'NONE',  ( 51.41799912780150805, -3.967692247893626512, 1.365930198224605707 ) ) ;
#8959=EDGE_LOOP ( 'NONE', ( #17781, #5187, #17851, #7465 ) ) ;
#8960=CARTESIAN_POINT ( 'NONE',  ( 53.71202192472755144, 7.447163568589559191, 2.049999999999939426 ) ) ;
#8988=DIRECTION ( 'NONE',  ( -0.9993908270190953180, 0.03489949670251430575, 3.490905158897711881E-15 ) ) ;
#8991=AXIS2_PLACEMENT_3D ( 'NONE', #22782, #27970, #15645 ) ;
#8993=CIRCLE ( 'NONE', #3447, 4.099999999999992539 ) ;
#8997=DIRECTION ( 'NONE',  ( 3.016910393003118404E-15, 0.000000000000000000, 1.000000000000000000 ) ) ;
#8998=CARTESIAN_POINT ( 'NONE',  ( 54.40293493925265977, 6.717672571224094114, -2.002198665876510741 ) ) ;
#8999=CARTESIAN_POINT ( 'NONE',  ( 52.88898622668489224, 4.646829164113958299, 1.580883332821158671 ) ) ;
#9018=AXIS2_PLACEMENT_3D ( 'NONE', #25987, #9060, #11596 ) ;
#9031=CARTESIAN_POINT ( 'NONE',  ( 41.48619405471884392, -151.3359592902621955, 1.549999999999835953 ) ) ;
#9040=CARTESIAN_POINT ( 'NONE',  ( 54.15675781068899397, 5.684314874070254042, -2.050000000000189004 ) ) ;
#9048=CARTESIAN_POINT ( 'NONE',  ( 51.80000000000002558, -4.291790910095608425, 1.352971095042299954 ) ) ;
#9054=ADVANCED_FACE ( 'NONE', ( #5484 ), #30554, .T. ) ;
#9056=VERTEX_POINT ( 'NONE', #10697 ) ;
#9057=CARTESIAN_POINT ( 'NONE',  ( 25.60313575641834660, 5.243666353503796174, 1.949999999999910472 ) ) ;
#9060=DIRECTION ( 'NONE',  ( 0.000000000000000000, 0.000000000000000000, 1.000000000000000000 ) ) ;
#9086=AXIS2_PLACEMENT_3D ( 'NONE', #24795, #21715, #2953 ) ;
#9098=LINE ( 'NONE', #30943, #19993 ) ;
#9101=FACE_OUTER_BOUND ( 'NONE', #26818, .T. ) ;
#9124=CARTESIAN_POINT ( 'NONE',  ( 22.07280086217093640, 8.086143481909140007, -1.950000000000076339 ) ) ;
#9129=ORIENTED_EDGE ( 'NONE', *, *, #17202, .F. ) ;
#9133=CARTESIAN_POINT ( 'NONE',  ( 53.90311770664830959, 7.548181632372875427, 2.049999999999811084 ) ) ;
#9136=CARTESIAN_POINT ( 'NONE',  ( 50.80000000000001847, -3.908336260473454615, -1.238913909466097918 ) ) ;
#9148=CARTESIAN_POINT ( 'NONE',  ( 52.83066561783866177, 8.351253849600817958, 1.927138392211706686 ) ) ;
#9159=EDGE_CURVE ( 'NONE', #30552, #19284, #12977, .T. ) ;
#9164=DIRECTION ( 'NONE',  ( -0.9993908270190956511, 0.03489949670250096919, 3.491481338843132961E-15 ) ) ;
#9171=CARTESIAN_POINT ( 'NONE',  ( 51.87453755317506676, 8.609476251808864333, 2.002198665876147032 ) ) ;
#9198=AXIS2_PLACEMENT_3D ( 'NONE', #16832, #12220, #23946 ) ;
#9200=DIRECTION ( 'NONE',  ( -0.9993908270190953180, 0.03489949670251430575, 3.490905158897711881E-15 ) ) ;
#9201=CARTESIAN_POINT ( 'NONE',  ( 47.12253285714871964, -4.134031523355535143, -2.020495556749611676 ) ) ;
#9202=DIRECTION ( 'NONE',  ( -3.491481338843133355E-15, 0.000000000000000000, -1.000000000000000000 ) ) ;
#9229=CARTESIAN_POINT ( 'NONE',  ( 22.07280086217093640, 8.086143481909140007, -1.950000000000076339 ) ) ;
#9244=ORIENTED_EDGE ( 'NONE', *, *, #25507, .T. ) ;
#9247=CARTESIAN_POINT ( 'NONE',  ( 54.24289646986905211, 6.361177601056704489, -2.050000000000189004 ) ) ;
#9250=FACE_OUTER_BOUND ( 'NONE', #28529, .T. ) ;
#9265=ORIENTED_EDGE ( 'NONE', *, *, #28787, .T. ) ;
#9281=DIRECTION ( 'NONE',  ( 0.9993908270190958731, -0.03489949670250092062, -3.492262959426260213E-15 ) ) ;
#9283=VERTEX_POINT ( 'NONE', #31274 ) ;
#9287=CARTESIAN_POINT ( 'NONE',  ( 52.10582242447214441, 8.700707108360601794, 2.049999999999818190 ) ) ;
#9293=ORIENTED_EDGE ( 'NONE', *, *, #24282, .T. ) ;
#9316=CARTESIAN_POINT ( 'NONE',  ( 51.80000000000002558, 4.350000000000017408, 1.550321101314541927 ) ) ;
#9328=DIRECTION ( 'NONE',  ( -0.04332611568076707997, 0.9990609829735204173, 0.000000000000000000 ) ) ;
#9330=ORIENTED_EDGE ( 'NONE', *, *, #18277, .F. ) ;
#9336=CARTESIAN_POINT ( 'NONE',  ( 41.48619405471885102, -151.3359592902621955, 2.049999999999835953 ) ) ;
#9338=LINE ( 'NONE', #19005, #30621 ) ;
#9358=CARTESIAN_POINT ( 'NONE',  ( 54.19030381964616083, 6.697848500921247172, -2.050000000000189004 ) ) ;
#9377=B_SPLINE_SURFACE_WITH_KNOTS ( 'NONE', 3, 3, ( 
 ( #19153, #24200, #23885, #14685 ),
 ( #26556, #433, #28793, #19302 ),
 ( #19764, #9782, #26255, #5178 ),
 ( #24033, #21518, #19448, #7104 ),
 ( #2176, #12008, #21689, #271 ),
 ( #7246, #24345, #17226, #16911 ),
 ( #12161, #4868, #14827, #14534 ),
 ( #4563, #14210, #11841, #16765 ),
 ( #31155, #12295, #26409, #129 ),
 ( #29092, #19617, #29254, #7566 ),
 ( #26868, #24486, #2796, #12452 ),
 ( #18001, #22767, #3443, #582 ),
 ( #1199, #3115, #5320, #14985 ),
 ( #29541, #15459, #27338, #12761 ),
 ( #20391, #15303, #24652, #22439 ),
 ( #912, #3589, #5650, #1059 ),
 ( #17366, #5979, #17850, #10564 ),
 ( #24948, #27014, #5497, #2965 ),
 ( #13083, #734, #10709, #7856 ),
 ( #3272, #30014, #8329, #22606 ),
 ( #10857, #25277, #27654, #12610 ),
 ( #17695, #15631, #20545, #17535 ),
 ( #12916, #10393, #20238, #22296 ),
 ( #22911, #10241, #27486, #29870 ),
 ( #8182, #30179, #15148, #20078 ),
 ( #19911, #5806, #25116, #29715 ),
 ( #13227, #27186, #24805, #8030 ),
 ( #23965, #31075, #7034, #2259 ),
 ( #14139, #21445, #23814, #26486 ),
 ( #14296, #1516, #8494, #28874 ),
 ( #2106, #27814, #16527, #18174 ),
 ( #16695, #25426, #24124, #4489 ),
 ( #13371, #28551, #2434, #26337 ),
 ( #30480, #11770, #6271, #7184 ),
 ( #9401, #11924, #9247, #21610 ),
 ( #20705, #4636, #18907, #25575 ),
 ( #3729, #6126, #14448, #15776 ) ),
 .UNSPECIFIED., .F., .F., .F.,
 ( 4, 1, 1, 1, 2, 1, 1, 1, 2, 1, 1, 1, 2, 1, 1, 1, 2, 1, 1, 1, 2, 1, 1, 1, 2, 1, 1, 1, 4 ),
 ( 4, 4 ),
 ( 0.000000000000000000, 0.09793917091270401554, 0.1958783418254080311, 0.2938175127381121299, 0.3917566836508161732, 0.4059014630279186298, 0.4200462424050210863, 0.4341910217821235984, 0.4483358011592260550, 0.4506387114483191292, 0.4529416217374121478, 0.4552445320265053330, 0.4575474423155982961, 0.4619892840416085500, 0.4664311257676187483, 0.4708729674936289467, 0.4753148092196392005, 0.5855976156913508257, 0.6958804221630624509, 0.8061632286347739651, 0.9164460351064855903, 0.9208878768324958441, 0.9253297185585060980, 0.9297715602845164629, 0.9342134020105267167, 0.9365152712282671654, 0.9388171404460077252, 0.9411190096637481739, 0.9434208788814886226 ),
 ( 0.000000000000000000, 1.000000000000000000 ),
 .UNSPECIFIED. ) ;
#9378=ORIENTED_EDGE ( 'NONE', *, *, #14628, .T. ) ;
#9388=CARTESIAN_POINT ( 'NONE',  ( 51.80000048029754822, 4.021162616303429971, -2.019962949071075542 ) ) ;
#9390=CARTESIAN_POINT ( 'NONE',  ( 54.31409749668479492, 6.709390224138187975, 2.049999999999810640 ) ) ;
#9395=TOROIDAL_SURFACE ( 'NONE', #19532, 2.525000000001608846, 0.1000000000000000056 ) ;
#9396=CARTESIAN_POINT ( 'NONE',  ( 54.16612471089924696, 6.839395989833654710, 2.049999999999811084 ) ) ;
#9401=CARTESIAN_POINT ( 'NONE',  ( 54.16748273148216697, 5.680716993501275347, -2.050000000000189893 ) ) ;
#9403=VERTEX_POINT ( 'NONE', #24600 ) ;
#9404=CARTESIAN_POINT ( 'NONE',  ( 47.00000000000002132, -3.701035844659722240, 1.983438066289691770 ) ) ;
#9405=CARTESIAN_POINT ( 'NONE',  ( 27.62808879389202232, 5.849836810644521989, 1.424999999999903677 ) ) ;
#9413=CARTESIAN_POINT ( 'NONE',  ( 51.79853223485510938, 4.577225429117026678, -0.5276849443351092628 ) ) ;
#9426=STYLED_ITEM ( 'NONE', ( #27772 ), #25333 ) ;
#9429=ORIENTED_EDGE ( 'NONE', *, *, #1829, .F. ) ;
#9437=TOROIDAL_SURFACE ( 'NONE', #26595, 2.525000000001608846, 0.1000000000000000056 ) ;
#9459=FACE_OUTER_BOUND ( 'NONE', #23933, .T. ) ;
#9494=EDGE_CURVE ( 'NONE', #10675, #10424, #20951, .T. ) ;
#9506=AXIS2_PLACEMENT_3D ( 'NONE', #28383, #19369, #16986 ) ;
#9510=CARTESIAN_POINT ( 'NONE',  ( 51.80000000000002558, -3.637377585518695611, 2.099877210782855830 ) ) ;
#9514=CARTESIAN_POINT ( 'NONE',  ( 51.70000000000003837, 6.982261990806648555E-14, 4.499999999999857003 ) ) ;
#9522=LINE ( 'NONE', #7843, #26788 ) ;
#9523=CARTESIAN_POINT ( 'NONE',  ( 24.97556103306002839, 5.351466982482016022, -1.950000000000086553 ) ) ;
#9529=CARTESIAN_POINT ( 'NONE',  ( 50.91813586553376325, -3.908336260473453727, 1.238913909465742202 ) ) ;
#9543=ORIENTED_EDGE ( 'NONE', *, *, #14805, .T. ) ;
#9551=CARTESIAN_POINT ( 'NONE',  ( 51.30615523877534656, -3.992023072242621318, -1.294577227648917805 ) ) ;
#9554=ORIENTED_EDGE ( 'NONE', *, *, #2235, .T. ) ;
#9557=CARTESIAN_POINT ( 'NONE',  ( 53.66601923242428995, 4.681126589747570677, -2.050000000000186784 ) ) ;
#9561=CIRCLE ( 'NONE', #27726, 4.600000000000036948 ) ;
#9564=LINE ( 'NONE', #12225, #2368 ) ;
#9566=CARTESIAN_POINT ( 'NONE',  ( 51.80000000000003268, 2.428612866367529932E-14, 4.099999999999811351 ) ) ;
#9567=CARTESIAN_POINT ( 'NONE',  ( 51.80000000000001847, 2.428612866367529932E-14, -1.808587333520743709E-13 ) ) ;
#9572=CARTESIAN_POINT ( 'NONE',  ( 53.46818089146800901, 8.044765782148928679, 2.049999999999813749 ) ) ;
#9576=CARTESIAN_POINT ( 'NONE',  ( 51.58656643569684519, -3.755435527867144962, -1.648753881545417022 ) ) ;
#9592=CARTESIAN_POINT ( 'NONE',  ( 33.97298909694674762, 8.288184271125778935, 2.049999999999881251 ) ) ;
#9597=VERTEX_POINT ( 'NONE', #4152 ) ;
#9607=CIRCLE ( 'NONE', #13101, 0.1000000000000021150 ) ;
#9609=CARTESIAN_POINT ( 'NONE',  ( 53.87827693845233057, 5.944250707180074755, 2.049999999999811973 ) ) ;
#9619=ORIENTED_EDGE ( 'NONE', *, *, #5551, .F. ) ;
#9644=ADVANCED_FACE ( 'NONE', ( #13951 ), #16683, .T. ) ;
#9649=CARTESIAN_POINT ( 'NONE',  ( 22.07280086217093640, 8.086143481909148889, -1.950000000000076339 ) ) ;
#9652=ORIENTED_EDGE ( 'NONE', *, *, #14612, .F. ) ;
#9653=DIRECTION ( 'NONE',  ( -1.000000000000000000, 0.000000000000000000, 3.435095992031092083E-15 ) ) ;
#9667=EDGE_CURVE ( 'NONE', #25173, #28320, #16059, .T. ) ;
#9674=DIRECTION ( 'NONE',  ( 0.000000000000000000, -0.8740818021021516948, 0.4857787595540328796 ) ) ;
#9676=CARTESIAN_POINT ( 'NONE',  ( 52.83066426478726640, 8.351255136974236493, -1.927137645301873814 ) ) ;
#9698=VERTEX_POINT ( 'NONE', #24107 ) ;
#9712=CYLINDRICAL_SURFACE ( 'NONE', #323, 0.1000000000000000472 ) ;
#9717=CARTESIAN_POINT ( 'NONE',  ( 51.88812122917400416, 8.998461838226445408, -2.050000000000180123 ) ) ;
#9718=CARTESIAN_POINT ( 'NONE',  ( 51.70000000000002416, 3.851905453475163110, 1.404572667215161053 ) ) ;
#9728=ORIENTED_EDGE ( 'NONE', *, *, #3684, .T. ) ;
#9736=CARTESIAN_POINT ( 'NONE',  ( 34.56702326949726256, 8.213851659285209550, 2.049999999999878586 ) ) ;
#9747=CARTESIAN_POINT ( 'NONE',  ( 50.87477060347374902, 8.633605004118187765, 1.949999999999822320 ) ) ;
#9749=CARTESIAN_POINT ( 'NONE',  ( 51.68129744678917348, 4.333300462208747206, 1.549999999999819300 ) ) ;
#9751=ORIENTED_EDGE ( 'NONE', *, *, #24073, .F. ) ;
#9758=VERTEX_POINT ( 'NONE', #2577 ) ;
#9765=B_SPLINE_CURVE_WITH_KNOTS ( 'NONE', 3,
 ( #3897, #13544, #23227, #14907 ),
 .UNSPECIFIED., .F., .F.,
 ( 4, 4 ),
 ( 0.3274566953765374877, 0.3970257546597420473 ),
 .UNSPECIFIED. ) ;
#9771=CARTESIAN_POINT ( 'NONE',  ( 53.21917409580258607, 8.083376426877340037, -2.050000000000185008 ) ) ;
#9772=CARTESIAN_POINT ( 'NONE',  ( 33.05069135236685440, 8.148093138862860130, 1.549999999999884803 ) ) ;
#9778=ORIENTED_EDGE ( 'NONE', *, *, #24665, .T. ) ;
#9782=CARTESIAN_POINT ( 'NONE',  ( 53.90845421530191572, 6.078720411350368558, -0.8364387603671682436 ) ) ;
#9788=CARTESIAN_POINT ( 'NONE',  ( 47.76581851340797868, -3.901693722832459521, -1.260438308020617404 ) ) ;
#9806=ORIENTED_EDGE ( 'NONE', *, *, #6268, .T. ) ;
#9809=LINE ( 'NONE', #24229, #28619 ) ;
#9811=EDGE_CURVE ( 'NONE', #30937, #8932, #14, .T. ) ;
#9820=CARTESIAN_POINT ( 'NONE',  ( 51.80000000000001137, 4.175664755576646847, -1.929721184274108436 ) ) ;
#9842=ORIENTED_EDGE ( 'NONE', *, *, #3822, .T. ) ;
#9861=DIRECTION ( 'NONE',  ( -0.3180732113053867383, -0.9480661539417379879, -0.000000000000000000 ) ) ;
#9862=CARTESIAN_POINT ( 'NONE',  ( 47.37886355347654899, -4.356776102639407178, 1.481376528583874252 ) ) ;
#9877=ORIENTED_EDGE ( 'NONE', *, *, #1624, .F. ) ;
#9880=AXIS2_PLACEMENT_3D ( 'NONE', #13442, #12823, #22506 ) ;
#9881=CARTESIAN_POINT ( 'NONE',  ( 27.54696499484943217, 5.363421040470448986, 2.049999999999772893 ) ) ;
#9885=CARTESIAN_POINT ( 'NONE',  ( 52.48761841068137812, 8.622213116012012790, -2.050000000000182343 ) ) ;
#9910=CARTESIAN_POINT ( 'NONE',  ( 22.49424290799312942, 6.943762543480787031, -2.050000000000077538 ) ) ;
#9915=CARTESIAN_POINT ( 'NONE',  ( 31.86617018594280282, 7.736336509539960105, -2.050000000000112177 ) ) ;
#9924=CARTESIAN_POINT ( 'NONE',  ( 53.74478519188839698, 7.379842749953129832, -1.837855077339860976 ) ) ;
#9930=AXIS2_PLACEMENT_3D ( 'NONE', #2645, #22133, #2330 ) ;
#9936=DIRECTION ( 'NONE',  ( 0.9957419851083220141, 0.09218405009836627695, -2.168404344971037661E-15 ) ) ;
#9940=EDGE_CURVE ( 'NONE', #26028, #27144, #16452, .T. ) ;
#9954=CARTESIAN_POINT ( 'NONE',  ( 52.38143600039783365, 3.988258350863520096, 2.045676845274237543 ) ) ;
#9960=VECTOR ( 'NONE', #19223, 1000.000000000000000 ) ;
#9972=CARTESIAN_POINT ( 'NONE',  ( 23.27385761420496735, 6.062155931322325664, -1.950000000000080780 ) ) ;
#9979=CARTESIAN_POINT ( 'NONE',  ( 26.41339658680651326, 5.213169555504943098, 1.424999999999908340 ) ) ;
#9981=AXIS2_PLACEMENT_3D ( 'NONE', #27025, #26419, #5333 ) ;
#9993=VERTEX_POINT ( 'NONE', #22313 ) ;
#9995=CARTESIAN_POINT ( 'NONE',  ( 22.54717926605048106, 7.740376438784041468, -1.425000000000078204 ) ) ;
#9996=VERTEX_POINT ( 'NONE', #27504 ) ;
#10013=CARTESIAN_POINT ( 'NONE',  ( 51.87765138016309407, 8.698644590117595499, 2.049999999999819522 ) ) ;
#10030=CARTESIAN_POINT ( 'NONE',  ( 52.56231129345008668, 3.962517867693161833, -1.055249607820919699 ) ) ;
#10031=CARTESIAN_POINT ( 'NONE',  ( 48.00000000000002842, -4.319730106884874132, 1.256953381662069269 ) ) ;
#10036=ORIENTED_EDGE ( 'NONE', *, *, #14612, .T. ) ;
#10039=CARTESIAN_POINT ( 'NONE',  ( 52.00246240784254326, 4.370935999631933910, 1.433537180069559103 ) ) ;
#10044=CARTESIAN_POINT ( 'NONE',  ( 25.99900894223690173, 5.212247164669934207, 2.050000000000039790 ) ) ;
#10046=CIRCLE ( 'NONE', #7517, 4.199999999999993072 ) ;
#10066=CARTESIAN_POINT ( 'NONE',  ( 51.89161117884415120, 9.098400920926795976, 1.949999999999818767 ) ) ;
#10069=CARTESIAN_POINT ( 'NONE',  ( 53.96114054633191870, 6.379383430131290389, -1.889921144916990592 ) ) ;
#10073=CARTESIAN_POINT ( 'NONE',  ( 31.37624803156776565, 7.388935656075756420, -2.050000000000107292 ) ) ;
#10074=VERTEX_POINT ( 'NONE', #5668 ) ;
#10080=CARTESIAN_POINT ( 'NONE',  ( 51.97945110550962511, 4.337541896208987779, -2.050000000000180567 ) ) ;
#10094=VERTEX_POINT ( 'NONE', #9390 ) ;
#10097=AXIS2_PLACEMENT_3D ( 'NONE', #16447, #31006, #30861 ) ;
#10101=CARTESIAN_POINT ( 'NONE',  ( 51.67801394174050955, -4.132863666287244442, 2.022846738276933287 ) ) ;
#10103=EDGE_LOOP ( 'NONE', ( #17312, #25549, #10036, #26150, #7834, #28688, #21224, #13672 ) ) ;
#10116=CARTESIAN_POINT ( 'NONE',  ( 53.91574522233626965, 6.672251602764244893, -1.774295313897662485 ) ) ;
#10128=CARTESIAN_POINT ( 'NONE',  ( 28.86359278493675973, 5.838313002610194147, 1.424999999999899902 ) ) ;
#10132=ORIENTED_EDGE ( 'NONE', *, *, #3888, .T. ) ;
#10134=CARTESIAN_POINT ( 'NONE',  ( 51.80000000000001137, 4.350000000000017408, -1.550321101314903194 ) ) ;
#10139=ORIENTED_EDGE ( 'NONE', *, *, #11711, .T. ) ;
#10164=ADVANCED_FACE ( 'NONE', ( #13959 ), #9712, .T. ) ;
#10168=CARTESIAN_POINT ( 'NONE',  ( 52.89380626919926698, 4.088132893582258731, -0.3545262462039958096 ) ) ;
#10177=ORIENTED_EDGE ( 'NONE', *, *, #3230, .F. ) ;
#10188=EDGE_CURVE ( 'NONE', #23309, #25954, #17025, .T. ) ;
#10207=ORIENTED_EDGE ( 'NONE', *, *, #18345, .F. ) ;
#10215=CARTESIAN_POINT ( 'NONE',  ( 51.30625150934615419, -4.280436737593984908, -1.378429032882124927 ) ) ;
#10217=CARTESIAN_POINT ( 'NONE',  ( 51.70000000000002416, 6.982261990806648555E-14, -1.793082891011605378E-13 ) ) ;
#10219=CARTESIAN_POINT ( 'NONE',  ( 29.24156347413317647, 6.028130183538130460, -1.950000000000102984 ) ) ;
#10221=EDGE_LOOP ( 'NONE', ( #31323, #30998, #7057, #30193, #24945, #16852, #28169, #4250, #14613, #409, #8270, #27244 ) ) ;
#10223=CARTESIAN_POINT ( 'NONE',  ( 54.41366571437522026, 6.718673005292167488, 1.949999999999809663 ) ) ;
#10228=CARTESIAN_POINT ( 'NONE',  ( 53.75840399023271488, 7.746411475361853149, -2.050000000000187228 ) ) ;
#10235=DIRECTION ( 'NONE',  ( 3.491481338843133355E-15, 0.000000000000000000, 1.000000000000000000 ) ) ;
#10241=CARTESIAN_POINT ( 'NONE',  ( 54.40419027210252523, 5.984372876903068850, -1.843143693225357538E-13 ) ) ;
#10245=CARTESIAN_POINT ( 'NONE',  ( 52.88620718028471401, 4.625382794676526466, 1.578939844535152570 ) ) ;
#10262=CARTESIAN_POINT ( 'NONE',  ( 47.05963571244991073, 8.266527678078146479, -1.550000000000163469 ) ) ;
#10265=DIRECTION ( 'NONE',  ( 3.489354422748178582E-15, -1.218509414717996338E-16, 1.000000000000000000 ) ) ;
#10271=CARTESIAN_POINT ( 'NONE',  ( 53.45668887520044876, 7.806764284940763687, -1.876589106057076295 ) ) ;
#10276=CARTESIAN_POINT ( 'NONE',  ( 31.71090952588640732, 7.663588669452821911, 2.049999999999887912 ) ) ;
#10300=CARTESIAN_POINT ( 'NONE',  ( 52.88620718028472822, 4.625382794676503373, -2.050000000000184119 ) ) ;
#10304=CARTESIAN_POINT ( 'NONE',  ( 51.06302884844836143, -4.023893809447297798, 1.198232146805239928 ) ) ;
#10306=CARTESIAN_POINT ( 'NONE',  ( 26.19155409318043226, 5.638511060912941630, -1.425000000000091305 ) ) ;
#10318=CARTESIAN_POINT ( 'NONE',  ( 51.80000000000001137, 6.475000000000062705, -2.050000000000180123 ) ) ;
#10319=CARTESIAN_POINT ( 'NONE',  ( 47.49374849065389270, -4.280436737593935170, 1.378429032881762994 ) ) ;
#10322=CARTESIAN_POINT ( 'NONE',  ( 33.05069135236684019, 8.148093138862860130, -1.550000000000114619 ) ) ;
#10330=CARTESIAN_POINT ( 'NONE',  ( 31.84692766216867810, 7.617555580675888116, 1.949999999999889599 ) ) ;
#10336=CARTESIAN_POINT ( 'NONE',  ( 26.92903764427223123, 5.249711979587693200, 1.949999999999972422 ) ) ;
#10337=ORIENTED_EDGE ( 'NONE', *, *, #22040, .T. ) ;
#10340=CARTESIAN_POINT ( 'NONE',  ( 52.02336772807328913, 3.827384603151627651, -2.050000000000181455 ) ) ;
#10349=CARTESIAN_POINT ( 'NONE',  ( 50.35762544161296006, 8.151359338959888845, 1.549999999999824629 ) ) ;
#10353=ORIENTED_EDGE ( 'NONE', *, *, #15824, .T. ) ;
#10364=ORIENTED_EDGE ( 'NONE', *, *, #23410, .T. ) ;
#10366=FACE_OUTER_BOUND ( 'NONE', #23638, .T. ) ;
#10370=CARTESIAN_POINT ( 'NONE',  ( 32.27289361194181083, 7.909974131749012649, -2.050000000000113509 ) ) ;
#10378=CARTESIAN_POINT ( 'NONE',  ( 53.87827693845231636, 5.944250707180074755, -2.050000000000187228 ) ) ;
#10379=CARTESIAN_POINT ( 'NONE',  ( 47.10000000821191435, -3.608818513796487437, -1.949335135736566249 ) ) ;
#10384=CIRCLE ( 'NONE', #8352, 159.6997717543496833 ) ;
#10393=CARTESIAN_POINT ( 'NONE',  ( 54.40301486585899937, 5.980869397714326574, 0.9749999999998116840 ) ) ;
#10401=CARTESIAN_POINT ( 'NONE',  ( 51.75922852344036329, 4.143493964997498225, 1.955480185863871956 ) ) ;
#10404=CARTESIAN_POINT ( 'NONE',  ( 51.67105141853712524, -3.772456960769059453, -1.610749547355440292 ) ) ;
#10406=ORIENTED_EDGE ( 'NONE', *, *, #3039, .F. ) ;
#10424=VERTEX_POINT ( 'NONE', #25346 ) ;
#10429=EDGE_CURVE ( 'NONE', #9996, #15276, #10932, .T. ) ;
#10433=EDGE_CURVE ( 'NONE', #27144, #9993, #23297, .T. ) ;
#10436=DIRECTION ( 'NONE',  ( -0.3180732113053867383, -0.9480661539417379879, -0.000000000000000000 ) ) ;
#10437=CARTESIAN_POINT ( 'NONE',  ( 32.52839478919696603, 7.997762531131884955, 2.049999999999888800 ) ) ;
#10448=EDGE_LOOP ( 'NONE', ( #21627, #10502, #14369, #12830 ) ) ;
#10449=LINE ( 'NONE', #20131, #13831 ) ;
#10462=EDGE_LOOP ( 'NONE', ( #24456, #9554, #3917 ) ) ;
#10472=EDGE_CURVE ( 'NONE', #26143, #13128, #16213, .T. ) ;
#10475=CARTESIAN_POINT ( 'NONE',  ( 24.57460841532290630, 5.893272594507614315, -1.425000000000085754 ) ) ;
#10477=EDGE_CURVE ( 'NONE', #26805, #4199, #19018, .T. ) ;
#10502=ORIENTED_EDGE ( 'NONE', *, *, #6579, .F. ) ;
#10503=CARTESIAN_POINT ( 'NONE',  ( 34.49381514799785009, 8.210676854548648151, 1.949999999999878719 ) ) ;
#10511=CARTESIAN_POINT ( 'NONE',  ( 26.61241883252574070, 5.319505464261285788, 2.049999999999907008 ) ) ;
#10522=CARTESIAN_POINT ( 'NONE',  ( 50.87477060347630697, 8.633605004120575188, 1.549999999999822631 ) ) ;
#10531=ADVANCED_FACE ( 'NONE', ( #28506 ), #23924, .T. ) ;
#10538=ORIENTED_EDGE ( 'NONE', *, *, #25940, .F. ) ;
#10542=CARTESIAN_POINT ( 'NONE',  ( 51.71302666497697942, 3.851408839085467495, -1.405934584416819400 ) ) ;
#10544=CARTESIAN_POINT ( 'NONE',  ( 30.17828911090724375, 6.795520168003006845, -2.050000000000104627 ) ) ;
#10546=CARTESIAN_POINT ( 'NONE',  ( 54.40293493925265267, 6.717672571224089673, 2.002198665876135930 ) ) ;
#10549=CARTESIAN_POINT ( 'NONE',  ( 47.12240576366414757, -3.662050566052967415, 1.846868639358291819 ) ) ;
#10550=CARTESIAN_POINT ( 'NONE',  ( 47.86840742095310475, -4.031600731367475099, -1.173113608354439563 ) ) ;
#10555=CYLINDRICAL_SURFACE ( 'NONE', #12940, 0.09999999999999972800 ) ;
#10561=DIRECTION ( 'NONE',  ( -0.6819983600625022513, 0.7313537016191670181, 2.468850131082277965E-15 ) ) ;
#10564=CARTESIAN_POINT ( 'NONE',  ( 54.32946475390676966, 6.710822919118950125, 2.049999999999810196 ) ) ;
#10571=DIRECTION ( 'NONE',  ( 0.03489949670185131525, 0.9993908270191184107, 0.000000000000000000 ) ) ;
#10574=CARTESIAN_POINT ( 'NONE',  ( 51.80000000000002558, 4.175664755576631748, 1.929721184273780255 ) ) ;
#10581=CARTESIAN_POINT ( 'NONE',  ( 53.91566439300392943, 6.672259399342834740, -1.839335743490527530 ) ) ;
#10598=CARTESIAN_POINT ( 'NONE',  ( 22.68377116885792333, 6.706477478074083010, 2.049999999999920774 ) ) ;
#10612=FACE_OUTER_BOUND ( 'NONE', #10448, .T. ) ;
#10622=CYLINDRICAL_SURFACE ( 'NONE', #25605, 0.1000000000000001721 ) ;
#10623=CARTESIAN_POINT ( 'NONE',  ( 52.09213388422764979, 8.600000000000108002, -1.949999998429221337 ) ) ;
#10643=CARTESIAN_POINT ( 'NONE',  ( 53.93929004300593277, 7.474130129650687238, 2.049999999999811084 ) ) ;
#10652=VECTOR ( 'NONE', #11713, 1000.000000000000000 ) ;
#10660=CARTESIAN_POINT ( 'NONE',  ( 22.32354329421583472, 7.018810582754515970, 2.049999999999858158 ) ) ;
#10668=FACE_OUTER_BOUND ( 'NONE', #184, .T. ) ;
#10672=DIRECTION ( 'NONE',  ( 1.000000000000000000, 0.000000000000000000, -3.491481338843133355E-15 ) ) ;
#10675=VERTEX_POINT ( 'NONE', #21874 ) ;
#10687=EDGE_CURVE ( 'NONE', #21368, #28904, #25743, .T. ) ;
#10690=CARTESIAN_POINT ( 'NONE',  ( 23.88937651016952657, 5.720041407194943694, -1.950000000000082112 ) ) ;
#10696=CARTESIAN_POINT ( 'NONE',  ( 47.88101986748534244, -3.908336255397547809, 1.238913925478448252 ) ) ;
#10697=CARTESIAN_POINT ( 'NONE',  ( 51.70000000000000995, -4.020776289669855785, -2.234582293948758736 ) ) ;
#10698=EDGE_CURVE ( 'NONE', #25407, #9597, #946, .T. ) ;
#10703=CARTESIAN_POINT ( 'NONE',  ( 50.93238199930985388, -4.417905785811345076, 1.285520522239830044 ) ) ;
#10705=CARTESIAN_POINT ( 'NONE',  ( 50.83686442967772479, 8.734989671305513070, -2.050000000000176570 ) ) ;
#10709=CARTESIAN_POINT ( 'NONE',  ( 54.42157938624325197, 6.359826701677585348, 2.020140340243033350 ) ) ;
#10717=ORIENTED_EDGE ( 'NONE', *, *, #18097, .T. ) ;
#10724=LINE ( 'NONE', #8346, #8855 ) ;
#10732=VERTEX_POINT ( 'NONE', #1231 ) ;
#10736=APPLICATION_CONTEXT ( 'automotive_design' ) ;
#10737=FACE_OUTER_BOUND ( 'NONE', #31113, .T. ) ;
#10742=CARTESIAN_POINT ( 'NONE',  ( 25.68828371051467130, 5.335084521667699420, 2.049999999999909228 ) ) ;
#10754=CARTESIAN_POINT ( 'NONE',  ( 23.27131915274574681, 6.595123925190214287, 1.424999999999918332 ) ) ;
#10755=ORIENTED_EDGE ( 'NONE', *, *, #13112, .F. ) ;
#10763=ORIENTED_EDGE ( 'NONE', *, *, #9667, .F. ) ;
#10766=CARTESIAN_POINT ( 'NONE',  ( 53.55869261961971972, 7.702978059423484680, -2.050000000000185896 ) ) ;
#10770=CARTESIAN_POINT ( 'NONE',  ( 31.20024169534877601, 7.859880414064924103, -1.425000000000108402 ) ) ;
#10784=CARTESIAN_POINT ( 'NONE',  ( 47.38264676386181407, -3.967853068034124853, -1.365472663301307232 ) ) ;
#10787=CARTESIAN_POINT ( 'NONE',  ( 53.75840399023272198, 7.746411475361852261, 2.049999999999812417 ) ) ;
#10790=EDGE_CURVE ( 'NONE', #27880, #15664, #27136, .T. ) ;
#10797=CARTESIAN_POINT ( 'NONE',  ( 31.30765689092466530, 7.353940011527059895, 1.949999999999889599 ) ) ;
#10824=ORIENTED_EDGE ( 'NONE', *, *, #3591, .F. ) ;
#10828=VECTOR ( 'NONE', #23434, 999.9999999999998863 ) ;
#10835=CARTESIAN_POINT ( 'NONE',  ( 51.77906683064299642, -4.146898708458731875, -1.994789398600458785 ) ) ;
#10841=DIRECTION ( 'NONE',  ( 0.000000000000000000, 0.000000000000000000, 1.000000000000000000 ) ) ;
#10851=EDGE_CURVE ( 'NONE', #320, #4290, #7046, .T. ) ;
#10857=CARTESIAN_POINT ( 'NONE',  ( 54.28867365409861634, 5.640057820322910587, 1.963089969304594895 ) ) ;
#10862=CARTESIAN_POINT ( 'NONE',  ( 51.80000005504633975, 4.055700188233500647, 2.007411739157320074 ) ) ;
#10866=CARTESIAN_POINT ( 'NONE',  ( 51.67759423633589932, -3.662050566052894141, -1.846868639358791864 ) ) ;
#10867=ORIENTED_EDGE ( 'NONE', *, *, #11165, .T. ) ;
#10868=LINE ( 'NONE', #30189, #29075 ) ;
#10883=ORIENTED_EDGE ( 'NONE', *, *, #3641, .T. ) ;
#10895=CARTESIAN_POINT ( 'NONE',  ( 33.37803294657273767, 8.220288670912871964, 2.049999999999885247 ) ) ;
#10897=PLANE ( 'NONE',  #6240 ) ;
#10919=AXIS2_PLACEMENT_3D ( 'NONE', #18257, #3670, #27897 ) ;
#10921=CARTESIAN_POINT ( 'NONE',  ( 52.61915120152472269, 4.492597126270304386, -2.050000000000182787 ) ) ;
#10925=FACE_OUTER_BOUND ( 'NONE', #27752, .T. ) ;
#10932=LINE ( 'NONE', #8401, #24593 ) ;
#10933=CIRCLE ( 'NONE', #6404, 0.1000000000000000472 ) ;
#10937=VECTOR ( 'NONE', #14091, 1000.000000000000000 ) ;
#10941=CARTESIAN_POINT ( 'NONE',  ( 27.72148966843208839, 5.417328426838181166, -1.425000000000096856 ) ) ;
#10945=CARTESIAN_POINT ( 'NONE',  ( 52.48761841068139233, 8.622213116012012790, 2.049999999999817302 ) ) ;
#10976=FACE_OUTER_BOUND ( 'NONE', #3907, .T. ) ;
#10977=EDGE_CURVE ( 'NONE', #17715, #12157, #15882, .T. ) ;
#10984=CARTESIAN_POINT ( 'NONE',  ( 53.91574522235882228, 6.672251602522421443, 1.774295301432037286 ) ) ;
#10990=SURFACE_STYLE_USAGE ( .BOTH. , #25538 ) ;
#10997=CARTESIAN_POINT ( 'NONE',  ( 48.00000000000002132, -4.319730106884873244, 1.256953381662069269 ) ) ;
#11001=ORIENTED_EDGE ( 'NONE', *, *, #6391, .T. ) ;
#11004=CARTESIAN_POINT ( 'NONE',  ( 22.61091062207862379, 6.637672121856656560, -2.050000000000011813 ) ) ;
#11009=AXIS2_PLACEMENT_3D ( 'NONE', #24920, #14949, #3085 ) ;
#11018=CARTESIAN_POINT ( 'NONE',  ( 48.00000000000001421, -4.003661535119149129, -1.269131321892086106 ) ) ;
#11023=CARTESIAN_POINT ( 'NONE',  ( 50.80000000000001137, -4.417905791132255899, 1.285520503972564343 ) ) ;
#11027=DIRECTION ( 'NONE',  ( 3.304235192336781034E-15, 0.000000000000000000, 1.000000000000000000 ) ) ;
#11033=ORIENTED_EDGE ( 'NONE', *, *, #13741, .F. ) ;
#11034=CARTESIAN_POINT ( 'NONE',  ( 52.80702527127470347, 4.040723488129245311, 2.049999999999815969 ) ) ;
#11041=VERTEX_POINT ( 'NONE', #13657 ) ;
#11056=EDGE_CURVE ( 'NONE', #22413, #26613, #24123, .T. ) ;
#11064=CARTESIAN_POINT ( 'NONE',  ( 47.10000000000000853, 2.480048031931718505E-14, -4.200000000000157385 ) ) ;
#11066=CARTESIAN_POINT ( 'NONE',  ( 41.48619405471885102, -151.3359592902621955, 1.949999999999835865 ) ) ;
#11072=DIRECTION ( 'NONE',  ( 3.491481338843133750E-15, 0.000000000000000000, 1.000000000000000000 ) ) ;
#11087=LINE ( 'NONE', #22833, #25555 ) ;
#11094=CARTESIAN_POINT ( 'NONE',  ( 51.70000000000000995, 4.174380580618773706, -1.932497546739578631 ) ) ;
#11100=DIRECTION ( 'NONE',  ( -1.000000000000000000, -0.000000000000000000, 3.491481338843133355E-15 ) ) ;
#11102=CARTESIAN_POINT ( 'NONE',  ( 52.72267294271967586, 4.003822062839298646, 2.049999999999815969 ) ) ;
#11108=CARTESIAN_POINT ( 'NONE',  ( 47.27480557050417076, -4.265347051556910962, -1.724604836179407075 ) ) ;
#11116=VERTEX_POINT ( 'NONE', #57 ) ;
#11128=FACE_OUTER_BOUND ( 'NONE', #2882, .T. ) ;
#11132=CARTESIAN_POINT ( 'NONE',  ( 53.91566439300397917, 6.672259399342800990, 1.839335743490167818 ) ) ;
#11134=ORIENTED_EDGE ( 'NONE', *, *, #19319, .F. ) ;
#11152=CARTESIAN_POINT ( 'NONE',  ( 25.06719628360101737, 5.330953183167694398, -2.050000000000087752 ) ) ;
#11153=ADVANCED_FACE ( 'NONE', ( #24732 ), #5727, .T. ) ;
#11156=EDGE_CURVE ( 'NONE', #3746, #4182, #13876, .T. ) ;
#11161=CARTESIAN_POINT ( 'NONE',  ( 50.80000000000001137, -4.291790910095608425, -1.352971095042658778 ) ) ;
#11162=CARTESIAN_POINT ( 'NONE',  ( 47.02938631638114941, -3.672971185000220906, 1.825899123715450934 ) ) ;
#11165=EDGE_CURVE ( 'NONE', #19028, #23041, #9607, .T. ) ;
#11167=CARTESIAN_POINT ( 'NONE',  ( 54.06654434747343885, 5.714581503706766874, -2.050000000000188116 ) ) ;
#11168=CARTESIAN_POINT ( 'NONE',  ( 51.70000000000003837, 2.428612866367529932E-14, 4.199999999999812772 ) ) ;
#11174=ADVANCED_FACE ( 'NONE', ( #17451 ), #19987, .T. ) ;
#11177=ORIENTED_EDGE ( 'NONE', *, *, #9940, .F. ) ;
#11182=CARTESIAN_POINT ( 'NONE',  ( 53.25508263676794485, 8.249290793645352338, 2.049999999999814193 ) ) ;
#11187=CARTESIAN_POINT ( 'NONE',  ( 28.66498512588421477, 5.839168430874288163, -2.050000000000100631 ) ) ;
#11195=ORIENTED_EDGE ( 'NONE', *, *, #17439, .F. ) ;
#11203=VECTOR ( 'NONE', #8311, 1000.000000000000000 ) ;
#11209=CARTESIAN_POINT ( 'NONE',  ( 53.32659978131828638, 4.996751601655196495, 1.614826230506383409 ) ) ;
#11219=CIRCLE ( 'NONE', #6172, 2.525000000001611511 ) ;
#11251=CARTESIAN_POINT ( 'NONE',  ( 52.02306152107794901, 3.830941655646745936, 2.049999999999818190 ) ) ;
#11272=FACE_OUTER_BOUND ( 'NONE', #14587, .T. ) ;
#11292=ORIENTED_EDGE ( 'NONE', *, *, #17433, .T. ) ;
#11296=CARTESIAN_POINT ( 'NONE',  ( 25.08803375997270990, 5.428914793826271179, -2.050000000000086864 ) ) ;
#11311=DIRECTION ( 'NONE',  ( 3.489354422748178582E-15, -1.218509414717996338E-16, 1.000000000000000000 ) ) ;
#11314=CARTESIAN_POINT ( 'NONE',  ( 50.28942560560668795, 8.224494709121804803, -2.050000000000174794 ) ) ;
#11319=AXIS2_PLACEMENT_3D ( 'NONE', #26731, #4561, #23883 ) ;
#11321=CARTESIAN_POINT ( 'NONE',  ( 51.03702166449080835, -3.901511898670509737, 1.261029562208011212 ) ) ;
#11324=CARTESIAN_POINT ( 'NONE',  ( 52.98658227084826677, 8.418175601153722099, 2.049999999999815081 ) ) ;
#11331=ORIENTED_EDGE ( 'NONE', *, *, #15801, .F. ) ;
#11334=ADVANCED_FACE ( 'NONE', ( #15846 ), #27563, .F. ) ;
#11354=EDGE_CURVE ( 'NONE', #4199, #3631, #17677, .T. ) ;
#11356=EDGE_CURVE ( 'NONE', #11041, #5230, #6346, .T. ) ;
#11359=EDGE_CURVE ( 'NONE', #3896, #12339, #6043, .T. ) ;
#11361=DIRECTION ( 'NONE',  ( -0.9993908270190956511, 0.03489949670250089980, 3.469446951951485842E-15 ) ) ;
#11372=EDGE_LOOP ( 'NONE', ( #17825, #17964, #24614, #13431 ) ) ;
#11373=CARTESIAN_POINT ( 'NONE',  ( 53.91582462592152325, 6.672259099522118930, 0.8960135317204955818 ) ) ;
#11379=AXIS2_PLACEMENT_3D ( 'NONE', #9031, #30882, #9200 ) ;
#11400=CARTESIAN_POINT ( 'NONE',  ( 47.19197484456741876, -4.291220349888532404, -1.660930850246812307 ) ) ;
#11416=AXIS2_PLACEMENT_3D ( 'NONE', #25883, #26204, #4511 ) ;
#11435=CARTESIAN_POINT ( 'NONE',  ( 27.10659297677967317, 5.279073180725292858, -1.425000000000094413 ) ) ;
#11439=AXIS2_PLACEMENT_3D ( 'NONE', #22394, #12257, #536 ) ;
#11445=DIRECTION ( 'NONE',  ( -1.000000000000000000, -0.000000000000000000, 3.491481338843133355E-15 ) ) ;
#11457=CIRCLE ( 'NONE', #14048, 4.600000000000036948 ) ;
#11464=AXIS2_PLACEMENT_3D ( 'NONE', #12366, #5719, #7945 ) ;
#11470=LINE ( 'NONE', #30786, #21522 ) ;
#11471=VERTEX_POINT ( 'NONE', #471 ) ;
#11493=VECTOR ( 'NONE', #29730, 1000.000000000000000 ) ;
#11506=CARTESIAN_POINT ( 'NONE',  ( 53.13060515908007631, 4.213974700431092124, 2.049999999999814637 ) ) ;
#11512=EDGE_LOOP ( 'NONE', ( #24838, #2629, #4281, #23834 ) ) ;
#11514=CIRCLE ( 'NONE', #30211, 0.09999999999999942268 ) ;
#11517=AXIS2_PLACEMENT_3D ( 'NONE', #12499, #24389, #472 ) ;
#11522=CARTESIAN_POINT ( 'NONE',  ( 53.36555380356171696, 7.911905146458437343, 1.886361318289319522 ) ) ;
#11540=CARTESIAN_POINT ( 'NONE',  ( 54.36607077795601839, 6.714235712056786376, -2.039222690361167434 ) ) ;
#11542=CARTESIAN_POINT ( 'NONE',  ( 51.70000000000002416, 4.174380580618757719, 1.932497546739255556 ) ) ;
#11549=ORIENTED_EDGE ( 'NONE', *, *, #13003, .T. ) ;
#11565=ADVANCED_FACE ( 'NONE', ( #12202 ), #5075, .T. ) ;
#11573=CARTESIAN_POINT ( 'NONE',  ( 41.48619405471885102, -151.3359592902622239, 2.049999999999835953 ) ) ;
#11596=DIRECTION ( 'NONE',  ( 1.000000000000000000, 0.000000000000000000, 0.000000000000000000 ) ) ;
#11599=VERTEX_POINT ( 'NONE', #22952 ) ;
#11601=AXIS2_PLACEMENT_3D ( 'NONE', #19489, #29137, #17125 ) ;
#11604=CARTESIAN_POINT ( 'NONE',  ( 28.44937284992262150, 5.648694717987697622, -1.425000000000099298 ) ) ;
#11614=CARTESIAN_POINT ( 'NONE',  ( 52.91409500010723121, 8.434844866547615894, 2.049999999999815525 ) ) ;
#11618=ADVANCED_FACE ( 'NONE', ( #17889 ), #15652, .T. ) ;
#11619=CARTESIAN_POINT ( 'NONE',  ( 51.67696994838494362, -3.663337715290890362, -1.844354128036493234 ) ) ;
#11621=ADVANCED_FACE ( 'NONE', ( #12967 ), #18681, .T. ) ;
#11629=ORIENTED_EDGE ( 'NONE', *, *, #5092, .F. ) ;
#11640=VERTEX_POINT ( 'NONE', #17740 ) ;
#11660=( BOUNDED_SURFACE ( )  B_SPLINE_SURFACE ( 3, 2, ( 
 ( #22122, #12279, #19888 ),
 ( #29378, #24786, #416 ),
 ( #5157, #27162, #21963 ),
 ( #12589, #5007, #24628 ),
 ( #7689, #27319, #10370 ),
 ( #14665, #251, #9915 ),
 ( #2945, #14807, #7833 ),
 ( #12891, #3249, #12429 ),
 ( #5632, #10073, #8160 ),
 ( #24928, #22581, #24328 ),
 ( #29236, #885, #19747 ),
 ( #17349, #20051, #10544 ),
 ( #17509, #15282, #26996 ),
 ( #10219, #7547, #5301 ),
 ( #15126, #29690, #19595 ),
 ( #20217, #17208, #29848 ),
 ( #14959, #24467, #22276 ),
 ( #17830, #3093, #561 ),
 ( #29518, #5478, #12741 ),
 ( #22418, #710, #8010 ),
 ( #17673, #6105, #23042 ),
 ( #20523, #11152, #11296 ),
 ( #1636, #6409, #30457 ),
 ( #16070, #18449, #23355 ),
 ( #10690, #6251, #20978 ),
 ( #15435, #25088, #20828 ),
 ( #8760, #30151, #20373 ),
 ( #28087, #25403, #3422 ),
 ( #8619, #11004, #13673 ),
 ( #1495, #8473, #27466 ),
 ( #27935, #20685, #13061 ),
 ( #22744, #3710, #30310 ),
 ( #13349, #18296, #30613 ),
 ( #5954, #15756, #25723 ) ),
 .UNSPECIFIED., .F., .F., .T. ) 
 B_SPLINE_SURFACE_WITH_KNOTS ( ( 4, 2, 2, 2, 2, 2, 2, 2, 2, 2, 2, 2, 2, 2, 2, 2, 4 ),
 ( 3, 3 ),
 ( -1.734723475976807094E-18, 0.001741451497654476635, 0.002612177246481715929, 0.003047540120895335467, 0.003482902995308955005, 0.004353628744136194516, 0.005224354492963433592, 0.006965805990617911746, 0.007836531739445151690, 0.008707257488272390766, 0.009577983237099629843, 0.01044870898592686892, 0.01131943473475410800, 0.01219016048358134707, 0.01262552335799496661, 0.01306088623240858615, 0.01393161198123582523 ),
 ( 0.000000000000000000, 1.000000000000000000 ),
 .UNSPECIFIED. ) 
 GEOMETRIC_REPRESENTATION_ITEM ( )  RATIONAL_B_SPLINE_SURFACE ( (
 ( 1.000000000000000000, 0.7071067811865475727, 1.000000000000000000),
 ( 1.000000000000000000, 0.7071067811865475727, 1.000000000000000000),
 ( 1.000000000000000000, 0.7071067811865475727, 1.000000000000000000),
 ( 1.000000000000000000, 0.7071067811865475727, 1.000000000000000000),
 ( 1.000000000000000000, 0.7071067811865467956, 1.000000000000000000),
 ( 1.000000000000000000, 0.7071067811865467956, 1.000000000000000000),
 ( 1.000000000000000000, 0.7071067811865494601, 1.000000000000000000),
 ( 1.000000000000000000, 0.7071067811865494601, 1.000000000000000000),
 ( 1.000000000000000000, 0.7071067811865490160, 1.000000000000000000),
 ( 1.000000000000000000, 0.7071067811865490160, 1.000000000000000000),
 ( 1.000000000000000000, 0.7071067811865490160, 1.000000000000000000),
 ( 1.000000000000000000, 0.7071067811865490160, 1.000000000000000000),
 ( 1.000000000000000000, 0.7071067811865490160, 1.000000000000000000),
 ( 1.000000000000000000, 0.7071067811865490160, 1.000000000000000000),
 ( 1.000000000000000000, 0.7071067811865482389, 1.000000000000000000),
 ( 1.000000000000000000, 0.7071067811865482389, 1.000000000000000000),
 ( 1.000000000000000000, 0.7071067811865452413, 1.000000000000000000),
 ( 1.000000000000000000, 0.7071067811865452413, 1.000000000000000000),
 ( 1.000000000000000000, 0.7071067811865475727, 1.000000000000000000),
 ( 1.000000000000000000, 0.7071067811865475727, 1.000000000000000000),
 ( 1.000000000000000000, 0.7071067811865482389, 1.000000000000000000),
 ( 1.000000000000000000, 0.7071067811865482389, 1.000000000000000000),
 ( 1.000000000000000000, 0.7071067811865436870, 1.000000000000000000),
 ( 1.000000000000000000, 0.7071067811865436870, 1.000000000000000000),
 ( 1.000000000000000000, 0.7071067811865460184, 1.000000000000000000),
 ( 1.000000000000000000, 0.7071067811865460184, 1.000000000000000000),
 ( 1.000000000000000000, 0.7071067811865460184, 1.000000000000000000),
 ( 1.000000000000000000, 0.7071067811865460184, 1.000000000000000000),
 ( 1.000000000000000000, 0.7071067811865471286, 1.000000000000000000),
 ( 1.000000000000000000, 0.7071067811865471286, 1.000000000000000000),
 ( 1.000000000000000000, 0.7071067811865467956, 1.000000000000000000),
 ( 1.000000000000000000, 0.7071067811865467956, 1.000000000000000000),
 ( 1.000000000000000000, 0.7071067811865467956, 1.000000000000000000),
 ( 1.000000000000000000, 0.7071067811865467956, 1.000000000000000000) ) ) 
 REPRESENTATION_ITEM ( '' )  SURFACE ( )  );
#11662=CARTESIAN_POINT ( 'NONE',  ( 53.53640187423186347, 5.215699251213393950, 2.049999999999812861 ) ) ;
#11665=CARTESIAN_POINT ( 'NONE',  ( 51.25604564026579624, -3.873096995916275098, -1.345769568645377223 ) ) ;
#11686=CARTESIAN_POINT ( 'NONE',  ( 50.87477060347374902, 8.633605004118187765, 1.949999999999822320 ) ) ;
#11694=ORIENTED_EDGE ( 'NONE', *, *, #9811, .F. ) ;
#11696=CARTESIAN_POINT ( 'NONE',  ( 34.56269065792917417, 8.313757757582560970, 1.949999999999879607 ) ) ;
#11697=CARTESIAN_POINT ( 'NONE',  ( 51.88812122917402547, 8.998461838226445408, 2.049999999999819522 ) ) ;
#11699=EDGE_LOOP ( 'NONE', ( #11292, #17698, #16181, #30483 ) ) ;
#11706=CARTESIAN_POINT ( 'NONE',  ( 51.70000000000002416, 6.982261990806648555E-14, -1.793082891011605378E-13 ) ) ;
#11711=EDGE_CURVE ( 'NONE', #133, #4604, #7578, .T. ) ;
#11713=DIRECTION ( 'NONE',  ( -0.4772254810013855097, 0.8787808829753844808, 1.772289120718281137E-15 ) ) ;
#11722=CIRCLE ( 'NONE', #21357, 0.1000000000000000472 ) ;
#11725=CARTESIAN_POINT ( 'NONE',  ( 51.94586448161385306, 3.919599535333307294, -2.045267140517447402 ) ) ;
#11756=EDGE_CURVE ( 'NONE', #9597, #5233, #27802, .T. ) ;
#11759=CARTESIAN_POINT ( 'NONE',  ( 51.73504510627559938, 4.165466613856895428, -1.939072597264996700 ) ) ;
#11770=CARTESIAN_POINT ( 'NONE',  ( 54.28500427175510623, 6.002439417116981701, -2.050000000000186784 ) ) ;
#11775=CARTESIAN_POINT ( 'NONE',  ( 51.77478101728125637, -4.051679580537264513, 1.951144708070448708 ) ) ;
#11779=CARTESIAN_POINT ( 'NONE',  ( 22.54717926605044909, 7.740376438784151603, 1.424999999999921663 ) ) ;
#11781=CARTESIAN_POINT ( 'NONE',  ( 51.82286850391904665, 4.509570184545037108, -0.9171356268414241342 ) ) ;
#11787=CARTESIAN_POINT ( 'NONE',  ( 31.90749320846298431, 7.645246315295118222, 1.949999999999919797 ) ) ;
#11807=VECTOR ( 'NONE', #25858, 1000.000000000000114 ) ;
#11813=FACE_OUTER_BOUND ( 'NONE', #25033, .T. ) ;
#11814=CARTESIAN_POINT ( 'NONE',  ( 50.80000000000001847, -3.937842575352405117, -1.145831896685998830 ) ) ;
#11817=CARTESIAN_POINT ( 'NONE',  ( 22.26297291748177898, 7.344068067229269303, -2.050000000000077094 ) ) ;
#11824=CARTESIAN_POINT ( 'NONE',  ( 52.10571136498352018, 8.590619605527507474, 1.949999390375997343 ) ) ;
#11841=CARTESIAN_POINT ( 'NONE',  ( 53.96114084830844604, 6.379385664344251694, 1.889910665294559422 ) ) ;
#11867=EDGE_CURVE ( 'NONE', #24179, #21603, #20740, .T. ) ;
#11871=CARTESIAN_POINT ( 'NONE',  ( 27.72596399900197994, 5.416480400817087038, -1.950000000000096101 ) ) ;
#11876=CARTESIAN_POINT ( 'NONE',  ( 47.76174270024939261, -4.379902212273319329, -1.406632791261494653 ) ) ;
#11882=CARTESIAN_POINT ( 'NONE',  ( 54.22146708689643191, 6.361260388417356637, -2.050000000000189004 ) ) ;
#11896=ORIENTED_EDGE ( 'NONE', *, *, #16016, .T. ) ;
#11918=ADVANCED_FACE ( 'NONE', ( #24811 ), #29102, .F. ) ;
#11924=CARTESIAN_POINT ( 'NONE',  ( 54.27565932475310717, 6.003153976823456972, -2.050000000000189893 ) ) ;
#11925=CARTESIAN_POINT ( 'NONE',  ( 50.80000000000001847, -3.908336260473453727, -1.238913909466097474 ) ) ;
#11937=CARTESIAN_POINT ( 'NONE',  ( 51.87992451262095983, 4.432176970433021168, -1.232860998884740766 ) ) ;
#11943=CARTESIAN_POINT ( 'NONE',  ( 30.17828911090722954, 6.795520168002859407, 2.049999999999894129 ) ) ;
#11949=AXIS2_PLACEMENT_3D ( 'NONE', #7644, #17304, #24735 ) ;
#11950=EDGE_CURVE ( 'NONE', #30600, #19284, #25229, .T. ) ;
#11955=EDGE_CURVE ( 'NONE', #8932, #16106, #27297, .T. ) ;
#11964=CARTESIAN_POINT ( 'NONE',  ( 53.49139514279642782, 5.155866831720373966, 1.635615235160198466 ) ) ;
#11974=DIRECTION ( 'NONE',  ( -0.4772254810013855097, 0.8787808829753843698, 1.772289120718281137E-15 ) ) ;
#12000=( BOUNDED_SURFACE ( )  B_SPLINE_SURFACE ( 3, 2, ( 
 ( #15468, #8647, #17703 ),
 ( #25124, #1207, #18327 ),
 ( #10866, #27348, #3280 ),
 ( #743, #10404, #15311 ),
 ( #20085, #8036, #24956 ),
 ( #6746, #28121, #19120 ),
 ( #11665, #13553, #28765 ),
 ( #20859, #26059, #18800 ),
 ( #21189, #6444, #14018 ),
 ( #9136, #11814, #13847 ) ),
 .UNSPECIFIED., .F., .F., .T. ) 
 B_SPLINE_SURFACE_WITH_KNOTS ( ( 4, 2, 2, 2, 4 ),
 ( 3, 3 ),
 ( -1.029992063861229212E-18, 0.0003537660104434870454, 0.0007075320208869751749, 0.001061298031330463413, 0.001415064041773951434 ),
 ( 0.000000000000000000, 1.000000000000000000 ),
 .UNSPECIFIED. ) 
 GEOMETRIC_REPRESENTATION_ITEM ( )  RATIONAL_B_SPLINE_SURFACE ( (
 ( 1.000000000000000000, 0.7071067811865712205, 1.000000000000000000),
 ( 1.000000000000000000, 0.7179295922952823039, 1.000000000000000000),
 ( 1.000000000000000000, 0.7246425758715334675, 1.000000000000000000),
 ( 1.000000000000000000, 0.7309548279203578192, 1.000000000000000000),
 ( 1.000000000000000000, 0.7305336397956169181, 1.000000000000000000),
 ( 1.000000000000000000, 0.7264835597194815309, 1.000000000000000000),
 ( 1.000000000000000000, 0.7229248932012791728, 1.000000000000000000),
 ( 1.000000000000000000, 0.7174039707101230734, 1.000000000000000000),
 ( 1.000000000000000000, 0.7154085637344075321, 1.000000000000000000),
 ( 1.000000000000000000, 0.7154752000627011554, 1.000000000000000000) ) ) 
 REPRESENTATION_ITEM ( '' )  SURFACE ( )  );
#12005=LINE ( 'NONE', #18980, #21482 ) ;
#12008=CARTESIAN_POINT ( 'NONE',  ( 53.90845325060750071, 6.078717535930443283, 0.8364386040616162976 ) ) ;
#12045=CARTESIAN_POINT ( 'NONE',  ( 51.87416143049283335, 8.598705507415685290, -1.950000000000180256 ) ) ;
#12049=CARTESIAN_POINT ( 'NONE',  ( 22.25735896772343025, 7.137076052088948686, 1.424999999999921885 ) ) ;
#12050=ORIENTED_EDGE ( 'NONE', *, *, #29281, .F. ) ;
#12065=EDGE_LOOP ( 'NONE', ( #26134, #20941, #20796, #7365 ) ) ;
#12075=CARTESIAN_POINT ( 'NONE',  ( 53.13060515908006920, 4.213974700431092124, -2.050000000000185008 ) ) ;
#12076=CARTESIAN_POINT ( 'NONE',  ( 51.70000000000000995, -3.637377585518695611, -2.099877210783217318 ) ) ;
#12090=CARTESIAN_POINT ( 'NONE',  ( 47.49416525120574306, -4.280467579807392120, -1.378329539257057368 ) ) ;
#12101=ORIENTED_EDGE ( 'NONE', *, *, #23940, .F. ) ;
#12127=DIRECTION ( 'NONE',  ( -3.489354422748178582E-15, 1.218509414717996338E-16, -1.000000000000000000 ) ) ;
#12129=ADVANCED_FACE ( 'NONE', ( #22447 ), #12000, .T. ) ;
#12130=CARTESIAN_POINT ( 'NONE',  ( 51.80000000000002558, 8.701414213562481237, 2.049999999999819522 ) ) ;
#12136=ORIENTED_EDGE ( 'NONE', *, *, #30159, .T. ) ;
#12139=CARTESIAN_POINT ( 'NONE',  ( 30.31473038485998828, 6.776227631128587170, -1.950000000000104983 ) ) ;
#12143=CARTESIAN_POINT ( 'NONE',  ( 53.35461118278485770, 7.923754912502171344, 1.887454836110121770 ) ) ;
#12149=CARTESIAN_POINT ( 'NONE',  ( 54.13139471328950236, 5.522381836601891969, -2.050000000000188116 ) ) ;
#12150=AXIS2_PLACEMENT_3D ( 'NONE', #7800, #22243, #19555 ) ;
#12151=DIRECTION ( 'NONE',  ( 3.083952846180964840E-15, 0.000000000000000000, 1.000000000000000000 ) ) ;
#12157=VERTEX_POINT ( 'NONE', #10066 ) ;
#12161=CARTESIAN_POINT ( 'NONE',  ( 53.81450004168216594, 5.799141575175354113, 1.730551604087905204 ) ) ;
#12168=CARTESIAN_POINT ( 'NONE',  ( 51.70000000000000995, -4.020776289669855785, -2.234582293948758736 ) ) ;
#12178=CARTESIAN_POINT ( 'NONE',  ( 51.77437620346577773, -3.759602463706845921, 1.865002073832249252 ) ) ;
#12187=DIRECTION ( 'NONE',  ( 3.489354422748178582E-15, -1.218509414717996338E-16, 1.000000000000000000 ) ) ;
#12194=ADVANCED_FACE ( 'NONE', ( #17200 ), #26704, .F. ) ;
#12202=FACE_OUTER_BOUND ( 'NONE', #6359, .T. ) ;
#12214=CARTESIAN_POINT ( 'NONE',  ( 50.93273830208138975, -4.031600731908413060, -1.173113608511851869 ) ) ;
#12219=CARTESIAN_POINT ( 'NONE',  ( 52.80968221184927103, 4.034333029853865327, -2.050000000000183675 ) ) ;
#12220=DIRECTION ( 'NONE',  ( 3.051840300662039536E-15, -0.4857787595540328796, 0.8740818021021518058 ) ) ;
#12221=LINE ( 'NONE', #10013, #15965 ) ;
#12225=CARTESIAN_POINT ( 'NONE',  ( 51.80000000000002558, -4.387164041431067751, 1.383037119376577140 ) ) ;
#12228=DIRECTION ( 'NONE',  ( 1.000000000000000000, 0.000000000000000000, -3.491481338843133355E-15 ) ) ;
#12231=CARTESIAN_POINT ( 'NONE',  ( 51.87765138016307986, 8.698644590117595499, -2.050000000000180123 ) ) ;
#12233=CARTESIAN_POINT ( 'NONE',  ( 47.10000000000002274, 6.982261990806648555E-14, -1.632474749424821370E-13 ) ) ;
#12236=CARTESIAN_POINT ( 'NONE',  ( 52.89442146867855854, 4.088415591072481980, 0.3516000293862507342 ) ) ;
#12239=DIRECTION ( 'NONE',  ( -9.754918421198724481E-16, 0.9601771338024399638, -0.2793919678926571892 ) ) ;
#12242=DIRECTION ( 'NONE',  ( -1.000000000000000000, 0.000000000000000000, 3.469446951951483476E-15 ) ) ;
#12249=EDGE_LOOP ( 'NONE', ( #5509, #9842, #10337, #26716 ) ) ;
#12252=CARTESIAN_POINT ( 'NONE',  ( 29.93605863096246367, 6.616288078318590671, 2.049999999999895461 ) ) ;
#12257=DIRECTION ( 'NONE',  ( -1.000000000000000000, -0.000000000000000000, 3.491481338843133355E-15 ) ) ;
#12266=ADVANCED_FACE ( 'NONE', ( #554 ), #100, .F. ) ;
#12269=CIRCLE ( 'NONE', #152, 0.1000000000000001443 ) ;
#12279=CARTESIAN_POINT ( 'NONE',  ( 34.56702326949724124, 8.213851659285211326, -2.050000000000119726 ) ) ;
#12281=CARTESIAN_POINT ( 'NONE',  ( 51.99340984296998158, 4.356875777028168528, 1.476187001954879952 ) ) ;
#12284=CARTESIAN_POINT ( 'NONE',  ( 53.87827693845218846, 5.944250707180090743, -1.708828125785526675 ) ) ;
#12295=CARTESIAN_POINT ( 'NONE',  ( 54.00139016905851008, 6.058270281819565284, 1.948881089517881637 ) ) ;
#12303=DIRECTION ( 'NONE',  ( 3.023770467182126270E-15, 0.4999707644721522182, 0.8660422822663637055 ) ) ;
#12320=CYLINDRICAL_SURFACE ( 'NONE', #6466, 4.600000000000036948 ) ;
#12323=CARTESIAN_POINT ( 'NONE',  ( 26.50971933136674608, 5.213424020870816022, -1.950000000000092770 ) ) ;
#12330=CARTESIAN_POINT ( 'NONE',  ( 29.64923672893716855, 6.300449151053627794, 1.424999999999897238 ) ) ;
#12339=VERTEX_POINT ( 'NONE', #23033 ) ;
#12343=ORIENTED_EDGE ( 'NONE', *, *, #28240, .T. ) ;
#12351=( NAMED_UNIT ( * ) PLANE_ANGLE_UNIT ( ) SI_UNIT ( $, .RADIAN. ) );
#12353=EDGE_CURVE ( 'NONE', #10074, #7683, #7504, .T. ) ;
#12357=CARTESIAN_POINT ( 'NONE',  ( 52.98753545145216037, 8.419778228641124684, -2.050000000000184563 ) ) ;
#12358=CARTESIAN_POINT ( 'NONE',  ( 22.07280086217094706, 8.086143481909154218, 1.949999999999922906 ) ) ;
#12366=CARTESIAN_POINT ( 'NONE',  ( 47.10000000000000853, -3.933368109459638884, -2.186004417993339111 ) ) ;
#12370=EDGE_LOOP ( 'NONE', ( #15040, #27187, #22997, #17999 ) ) ;
#12374=CARTESIAN_POINT ( 'NONE',  ( 47.02521898271880474, -4.051679580537261849, -1.951144708070795541 ) ) ;
#12377=CARTESIAN_POINT ( 'NONE',  ( 46.99709697984359025, -4.086844330037576078, 2.115703333131348174 ) ) ;
#12389=CARTESIAN_POINT ( 'NONE',  ( 51.89794158693270987, 4.415147102489865638, 1.292252039327525859 ) ) ;
#12392=LINE ( 'NONE', #377, #17642 ) ;
#12396=CARTESIAN_POINT ( 'NONE',  ( 33.40812713800838196, 8.122903761242909582, 1.949999999999884936 ) ) ;
#12397=ORIENTED_EDGE ( 'NONE', *, *, #17439, .T. ) ;
#12416=CARTESIAN_POINT ( 'NONE',  ( 53.71501932699290904, 7.815554144461332342, 2.049999999999812417 ) ) ;
#12429=CARTESIAN_POINT ( 'NONE',  ( 31.46392738815579548, 7.544460793879616212, -2.050000000000109512 ) ) ;
#12437=CARTESIAN_POINT ( 'NONE',  ( 53.94440344817328281, 6.524635634306427789, -2.050000000000187228 ) ) ;
#12452=CARTESIAN_POINT ( 'NONE',  ( 54.15033841019267413, 6.694122904935910334, 2.049999999999792877 ) ) ;
#12457=CARTESIAN_POINT ( 'NONE',  ( 51.88812122917396152, 8.998461838224883991, 1.949999999999818989 ) ) ;
#12463=ADVANCED_FACE ( 'NONE', ( #19203 ), #16665, .F. ) ;
#12465=CARTESIAN_POINT ( 'NONE',  ( 47.10000000000000853, -3.550773357292059451, -2.049880134335985815 ) ) ;
#12472=CIRCLE ( 'NONE', #16541, 0.1000000000000002970 ) ;
#12475=CIRCLE ( 'NONE', #31205, 4.500000000000037303 ) ;
#12477=CARTESIAN_POINT ( 'NONE',  ( 51.80000000000001137, 6.475000000000062705, -1.950000000000180256 ) ) ;
#12482=CARTESIAN_POINT ( 'NONE',  ( 31.68228470681282971, 7.543995930034753883, -1.950000000000109868 ) ) ;
#12490=CARTESIAN_POINT ( 'NONE',  ( 28.44937284992260729, 5.648694717987689629, 1.424999999999900790 ) ) ;
#12499=CARTESIAN_POINT ( 'NONE',  ( 50.22478246037405825, 8.164214000976988572, -1.950000000000174483 ) ) ;
#12504=CARTESIAN_POINT ( 'NONE',  ( 47.86726169791864294, -4.031600731908413948, 1.173113608511507255 ) ) ;
#12505=ORIENTED_EDGE ( 'NONE', *, *, #30506, .T. ) ;
#12517=( LENGTH_UNIT ( ) NAMED_UNIT ( * ) SI_UNIT ( .MILLI., .METRE. ) );
#12518=EDGE_LOOP ( 'NONE', ( #29788, #29404, #4804, #15564, #4607, #2621, #13372, #27094 ) ) ;
#12525=DIRECTION ( 'NONE',  ( 1.000000000000000000, 0.000000000000000000, -3.491481338843133355E-15 ) ) ;
#12553=LINE ( 'NONE', #21789, #21302 ) ;
#12570=CARTESIAN_POINT ( 'NONE',  ( 51.39453088482485299, 4.389042235173730155, 2.049999999999819966 ) ) ;
#12572=ORIENTED_EDGE ( 'NONE', *, *, #14624, .F. ) ;
#12584=CARTESIAN_POINT ( 'NONE',  ( 54.15033848193498756, 6.694122911624470262, -2.050000000000185008 ) ) ;
#12586=EDGE_CURVE ( 'NONE', #10094, #11116, #24394, .T. ) ;
#12589=CARTESIAN_POINT ( 'NONE',  ( 32.57869118458719981, 7.908463456459825736, -1.950000000000176925 ) ) ;
#12593=CARTESIAN_POINT ( 'NONE',  ( 47.10000000000002984, -3.550773357292059007, 2.049880134335656745 ) ) ;
#12597=CARTESIAN_POINT ( 'NONE',  ( 53.04927178323139714, 4.171861402708406885, -2.050000000000185008 ) ) ;
#12610=CARTESIAN_POINT ( 'NONE',  ( 54.41366571437522737, 6.718673005292168376, 1.963089969304595783 ) ) ;
#12624=CARTESIAN_POINT ( 'NONE',  ( 52.79223755100147741, 4.124864650457799264, 2.046664448805795011 ) ) ;
#12626=CARTESIAN_POINT ( 'NONE',  ( 34.56702326949724835, 8.213851659285209550, -2.050000000000119726 ) ) ;
#12630=CIRCLE ( 'NONE', #24771, 4.500000000000037303 ) ;
#12636=CIRCLE ( 'NONE', #1519, 0.1000000000000000472 ) ;
#12643=CARTESIAN_POINT ( 'NONE',  ( 23.92596721145586258, 5.813591174092887393, 2.049999999999916334 ) ) ;
#12647=UNCERTAINTY_MEASURE_WITH_UNIT (LENGTH_MEASURE( 1.000000000000000082E-05 ), #8744, 'distance_accuracy_value', 'NONE');
#12655=CARTESIAN_POINT ( 'NONE',  ( 48.00000000000002132, -4.031600731908413948, 1.173113608511506367 ) ) ;
#12657=ORIENTED_EDGE ( 'NONE', *, *, #29717, .T. ) ;
#12688=CARTESIAN_POINT ( 'NONE',  ( 52.71963143566818388, 4.013862682579961927, 0.8481297820164899193 ) ) ;
#12690=ORIENTED_EDGE ( 'NONE', *, *, #4217, .F. ) ;
#12700=CARTESIAN_POINT ( 'NONE',  ( 30.14940651961542528, 6.652605095929053469, 1.949999999999894706 ) ) ;
#12707=CARTESIAN_POINT ( 'NONE',  ( 24.79111845547922499, 5.500805180497224889, 2.049999999999913225 ) ) ;
#12711=ADVANCED_FACE ( 'NONE', ( #10612 ), #20290, .T. ) ;
#12712=CARTESIAN_POINT ( 'NONE',  ( 54.18071634157380601, 6.868323337799980166, -2.050000000000189448 ) ) ;
#12737=CARTESIAN_POINT ( 'NONE',  ( 53.99324464492229225, 6.679476996055688787, -1.975347834873397490 ) ) ;
#12738=ORIENTED_EDGE ( 'NONE', *, *, #2186, .F. ) ;
#12739=FACE_OUTER_BOUND ( 'NONE', #3772, .T. ) ;
#12741=CARTESIAN_POINT ( 'NONE',  ( 26.61241883252577978, 5.319505464261553129, -2.050000000000092193 ) ) ;
#12742=ADVANCED_FACE ( 'NONE', ( #8229 ), #8540, .F. ) ;
#12746=B_SPLINE_CURVE_WITH_KNOTS ( 'NONE', 3,
 ( #285, #29885, #748, #24818, #19629, #7872, #9954, #7719, #17240, #17712, #22157, #15316, #14838, #12624, #594, #17549, #27354, #24961, #24499, #26880, #2810, #3287 ),
 .UNSPECIFIED., .F., .F.,
 ( 4, 2, 2, 1, 1, 2, 2, 2, 2, 2, 2, 4 ),
 ( 2.427614462101942325E-07, 0.1250002124163139827, 0.1875001972437477793, 0.2187501896574692850, 0.2343751858643298436, 0.2421876839677601367, 0.2500001820711904021, 0.3750001517259984873, 0.4375001365533990882, 0.4687501289670995552, 0.5000001213808000777, 1.000000000000000000 ),
 .UNSPECIFIED. ) ;
#12750=CARTESIAN_POINT ( 'NONE',  ( 52.82099478266074755, 4.588601447596422744, -2.050000000000184119 ) ) ;
#12761=CARTESIAN_POINT ( 'NONE',  ( 54.24490706950494712, 6.702939575443663145, 2.049999999999809308 ) ) ;
#12763=B_SPLINE_CURVE_WITH_KNOTS ( 'NONE', 3,
 ( #17656, #863, #5616, #13046, #15589, #23022, #8602, #15738, #27606, #15265, #22727, #20666, #5932, #13191, #3078, #1023, #5462 ),
 .UNSPECIFIED., .F., .F.,
 ( 4, 2, 2, 1, 2, 2, 2, 2, 4 ),
 ( 0.5409539115281891686, 0.5983346725871655503, 0.6270250531166537966, 0.6557154336461419319, 0.7130961947051183136, 0.7704769557640946953, 0.8278577168230711880, 0.8852384778820474587, 1.000000000000000000 ),
 .UNSPECIFIED. ) ;
#12768=DIRECTION ( 'NONE',  ( -0.9993908270191184107, 0.03489949670185085034, 3.491481338843133355E-15 ) ) ;
#12786=ORIENTED_EDGE ( 'NONE', *, *, #3415, .T. ) ;
#12796=VERTEX_POINT ( 'NONE', #16302 ) ;
#12805=CARTESIAN_POINT ( 'NONE',  ( 30.08242191457678061, 7.215531071606934965, 1.424999999999894351 ) ) ;
#12811=EDGE_CURVE ( 'NONE', #12339, #30600, #20086, .T. ) ;
#12816=CARTESIAN_POINT ( 'NONE',  ( 53.12888913849683092, 4.216863368992567196, -2.050000000000185008 ) ) ;
#12820=CARTESIAN_POINT ( 'NONE',  ( 51.80000000000001847, 6.982261990806648555E-14, -1.796574372350448449E-13 ) ) ;
#12823=DIRECTION ( 'NONE',  ( 0.000000000000000000, -1.000000000000000000, 0.000000000000000000 ) ) ;
#12830=ORIENTED_EDGE ( 'NONE', *, *, #9494, .F. ) ;
#12836=CARTESIAN_POINT ( 'NONE',  ( 47.02093316935654599, -4.146898708459136884, 1.994789398600220309 ) ) ;
#12841=VERTEX_POINT ( 'NONE', #4420 ) ;
#12847=VERTEX_POINT ( 'NONE', #1888 ) ;
#12853=ORIENTED_EDGE ( 'NONE', *, *, #11756, .T. ) ;
#12857=CARTESIAN_POINT ( 'NONE',  ( 23.13461596521384323, 6.279931474727747265, 2.049999999999918110 ) ) ;
#12867=DIRECTION ( 'NONE',  ( 9.754918421198724481E-16, 0.9601771338024399638, 0.2793919678926571892 ) ) ;
#12868=FACE_OUTER_BOUND ( 'NONE', #23718, .T. ) ;
#12873=CARTESIAN_POINT ( 'NONE',  ( 54.06651298255822979, 5.714592026537127722, 2.049999999999811529 ) ) ;
#12883=VERTEX_POINT ( 'NONE', #29107 ) ;
#12885=CIRCLE ( 'NONE', #9880, 0.1000000000000002554 ) ;
#12886=CARTESIAN_POINT ( 'NONE',  ( 50.80000000000001137, -4.319730106884872356, -1.256953381662414326 ) ) ;
#12888=CARTESIAN_POINT ( 'NONE',  ( 51.76667388380258927, 3.850183871955880299, -1.478071712164887197 ) ) ;
#12891=CARTESIAN_POINT ( 'NONE',  ( 31.50816695936942224, 7.454773701385264850, -1.950000000000142286 ) ) ;
#12902=CARTESIAN_POINT ( 'NONE',  ( 47.44380078827037295, -3.851485842263134174, -1.408112718338090819 ) ) ;
#12916=CARTESIAN_POINT ( 'NONE',  ( 54.28867365409855950, 5.640057820322907922, 0.9749999999998116840 ) ) ;
#12924=CARTESIAN_POINT ( 'NONE',  ( 52.08333333333334281, 4.368973594129894167, -2.050000000000181455 ) ) ;
#12931=CARTESIAN_POINT ( 'NONE',  ( 48.00000000000001421, -4.003661535119149129, -1.169131321892086017 ) ) ;
#12940=AXIS2_PLACEMENT_3D ( 'NONE', #2375, #14565, #2539 ) ;
#12955=VECTOR ( 'NONE', #1163, 999.9999999999998863 ) ;
#12967=FACE_OUTER_BOUND ( 'NONE', #13772, .T. ) ;
#12974=AXIS2_PLACEMENT_3D ( 'NONE', #499, #348, #14750 ) ;
#12977=CIRCLE ( 'NONE', #22112, 0.1000000000000000472 ) ;
#12985=ORIENTED_EDGE ( 'NONE', *, *, #19931, .T. ) ;
#12989=CARTESIAN_POINT ( 'NONE',  ( 53.55869261961984051, 7.702978059423601032, -1.861455469535500340 ) ) ;
#13000=CARTESIAN_POINT ( 'NONE',  ( 52.41492537898349013, 3.996662292477194178, -2.045735003821204767 ) ) ;
#13003=EDGE_CURVE ( 'NONE', #320, #363, #142, .T. ) ;
#13004=EDGE_LOOP ( 'NONE', ( #18694, #15793, #14879, #21198, #17746, #10717, #20288, #28905 ) ) ;
#13012=CARTESIAN_POINT ( 'NONE',  ( 51.65313719492862532, 3.829415913202793398, 2.049999999999819522 ) ) ;
#13014=AXIS2_PLACEMENT_3D ( 'NONE', #9649, #26734, #22143 ) ;
#13016=CARTESIAN_POINT ( 'NONE',  ( 51.86020163181184017, 8.198949176608044453, 2.049999999999819522 ) ) ;
#13030=CARTESIAN_POINT ( 'NONE',  ( 22.00282357718615245, 7.757228888719249760, 1.949999999999923128 ) ) ;
#13046=CARTESIAN_POINT ( 'NONE',  ( 54.05502230659780594, 7.179870641707980283, -2.050000000000187672 ) ) ;
#13054=CARTESIAN_POINT ( 'NONE',  ( 47.86735275623932750, -4.319730106884873244, 1.256953381662070379 ) ) ;
#13061=CARTESIAN_POINT ( 'NONE',  ( 22.40865038670843390, 7.071719536792667071, -2.050000000000077982 ) ) ;
#13069=CARTESIAN_POINT ( 'NONE',  ( 47.73664259148971212, -4.023874009802445251, -1.198297772469074207 ) ) ;
#13070=CARTESIAN_POINT ( 'NONE',  ( 51.80000000000000426, 7.038595743567426471E-14, -4.600000000000216360 ) ) ;
#13083=CARTESIAN_POINT ( 'NONE',  ( 54.25934656145521018, 5.649896967619270960, 2.026383240762962057 ) ) ;
#13089=DIRECTION ( 'NONE',  ( 0.9993908270190956511, -0.03489949670250103858, -3.469446951953534514E-15 ) ) ;
#13097=DIRECTION ( 'NONE',  ( 3.384826294588897856E-15, 0.000000000000000000, 1.000000000000000000 ) ) ;
#13101=AXIS2_PLACEMENT_3D ( 'NONE', #7641, #9861, #2887 ) ;
#13112=EDGE_CURVE ( 'NONE', #21603, #18295, #30715, .T. ) ;
#13116=CARTESIAN_POINT ( 'NONE',  ( 27.80355388919737436, 5.537003769396955377, 2.049999999999903011 ) ) ;
#13124=VERTEX_POINT ( 'NONE', #17864 ) ;
#13128=VERTEX_POINT ( 'NONE', #24962 ) ;
#13141=CARTESIAN_POINT ( 'NONE',  ( 53.87654288987800300, 4.973000991543902849, -2.050000000000187672 ) ) ;
#13149=CARTESIAN_POINT ( 'NONE',  ( 50.87826055314398133, 8.733544086820096197, -2.050000000000176570 ) ) ;
#13160=CARTESIAN_POINT ( 'NONE',  ( 54.21707933481623343, 5.861459378068796688, 2.049999999999810640 ) ) ;
#13164=ORIENTED_EDGE ( 'NONE', *, *, #15765, .T. ) ;
#13173=CARTESIAN_POINT ( 'NONE',  ( 53.81457038914302871, 5.799118248596165870, 1.689328270749656191 ) ) ;
#13191=CARTESIAN_POINT ( 'NONE',  ( 52.78843926895370231, 8.494246790034939210, -2.050000000000183231 ) ) ;
#13195=VERTEX_POINT ( 'NONE', #18489 ) ;
#13213=( BOUNDED_SURFACE ( )  B_SPLINE_SURFACE ( 2, 3, ( 
 ( #22350, #19819, #2870, #12219, #7478, #2714, #21903, #5094, #19674, #186, #7764, #2414, #14744, #19513, #12357, #24713, #17284, #5235 ),
 ( #7313, #14888, #14596, #3025, #12075, #9557, #28857, #7169, #16831, #16981, #14428, #21752, #41, #26632, #4939, #24262, #3794, #3338 ),
 ( #1117, #25186, #8239, #27545, #12816, #20448, #13141, #15532, #18233, #20302, #22829, #800, #17904, #3644, #27246, #27869, #6186, #15830 ),
 ( #20148, #19970, #8391, #10921, #10300, #20613, #5709, #5563, #29930, #25483, #18076, #29774, #10766, #15689, #13435, #30074, #29605, #27398 ),
 ( #15212, #1258, #13280, #8094, #972, #27720, #5871, #24858, #3500, #7934, #15360, #6038, #12989, #22968, #22675, #25339, #10623, #17760 ) ),
 .UNSPECIFIED., .F., .F., .F. ) 
 B_SPLINE_SURFACE_WITH_KNOTS ( ( 3, 2, 3 ),
 ( 4, 2, 2, 2, 2, 2, 2, 2, 4 ),
 ( -0.01000000000000000021, 0.000000000000000000, 1.000000000000000000 ),
 ( 1.413716694115406902, 1.826050729899067360, 2.238384765682727817, 2.650718801466387831, 3.063052837250048288, 3.475386873033708746, 3.887720908817368759, 4.300054944601029661, 4.712388980384689674 ),
 .UNSPECIFIED. ) 
 GEOMETRIC_REPRESENTATION_ITEM ( )  RATIONAL_B_SPLINE_SURFACE ( (
 ( 1.000000000000000000, 1.000000000000000000, 1.000000000000000000, 1.000000000000000000, 1.000000000000000000, 1.000000000000000000, 1.000000000000000000, 1.000000000000000000, 1.000000000000000000, 1.000000000000000000, 1.000000000000000000, 1.000000000000000000, 1.000000000000000000, 1.000000000000000000, 1.000000000000000000, 1.000000000000000000, 1.000000000000000000, 1.000000000000000000),
 ( 1.000000000000000000, 1.000000000000000000, 1.000000000000000000, 1.000000000000000000, 1.000000000000000000, 1.000000000000000000, 1.000000000000000000, 1.000000000000000000, 1.000000000000000000, 1.000000000000000000, 1.000000000000000000, 1.000000000000000000, 1.000000000000000000, 1.000000000000000000, 1.000000000000000000, 1.000000000000000000, 1.000000000000000000, 1.000000000000000000),
 ( 1.000000000000000000, 1.000000000000000000, 1.000000000000000000, 1.000000000000000000, 1.000000000000000000, 1.000000000000000000, 1.000000000000000000, 1.000000000000000000, 1.000000000000000000, 1.000000000000000000, 1.000000000000000000, 1.000000000000000000, 1.000000000000000000, 1.000000000000000000, 1.000000000000000000, 1.000000000000000000, 1.000000000000000000, 1.000000000000000000),
 ( 0.7071067811865476838, 0.7071067811865476838, 0.7071067811865475727, 0.7071067811865475727, 0.7071067811865476838, 0.7071067811865476838, 0.7071067811865475727, 0.7071067811865475727, 0.7071067811865473507, 0.7071067811865473507, 0.7071067811865479058, 0.7071067811865479058, 0.7071067811865475727, 0.7071067811865475727, 0.7071067811865463515, 0.7071067811865463515, 0.7071067811865475727, 0.7071067811865475727),
 ( 1.000000000000000000, 1.000000000000000000, 1.000000000000000000, 1.000000000000000000, 1.000000000000000000, 1.000000000000000000, 1.000000000000000000, 1.000000000000000000, 1.000000000000000000, 1.000000000000000000, 1.000000000000000000, 1.000000000000000000, 1.000000000000000000, 1.000000000000000000, 1.000000000000000000, 1.000000000000000000, 1.000000000000000000, 1.000000000000000000) ) ) 
 REPRESENTATION_ITEM ( '' )  SURFACE ( )  );
#13227=CARTESIAN_POINT ( 'NONE',  ( 54.28867365409860213, 5.640057820322910587, -1.963089969304966820 ) ) ;
#13235=ORIENTED_EDGE ( 'NONE', *, *, #8809, .F. ) ;
#13259=ORIENTED_EDGE ( 'NONE', *, *, #11354, .F. ) ;
#13278=VERTEX_POINT ( 'NONE', #30827 ) ;
#13280=CARTESIAN_POINT ( 'NONE',  ( 52.05393800078982025, 4.345106731198570493, -1.549654688285467596 ) ) ;
#13288=DIRECTION ( 'NONE',  ( 3.489354422748178582E-15, -1.218509414717996338E-16, 1.000000000000000000 ) ) ;
#13307=CARTESIAN_POINT ( 'NONE',  ( 22.04321716858594016, 7.679566743993225586, -1.425000000000077316 ) ) ;
#13308=ORIENTED_EDGE ( 'NONE', *, *, #16519, .F. ) ;
#13334=ORIENTED_EDGE ( 'NONE', *, *, #2433, .T. ) ;
#13349=CARTESIAN_POINT ( 'NONE',  ( 22.00282357718609916, 7.757228888719899906, -1.949999999999942002 ) ) ;
#13364=DIRECTION ( 'NONE',  ( 0.000000000000000000, 0.000000000000000000, -1.000000000000000000 ) ) ;
#13368=CARTESIAN_POINT ( 'NONE',  ( 47.00000000000002132, 2.428612866367529932E-14, -1.640996229256273308E-13 ) ) ;
#13371=CARTESIAN_POINT ( 'NONE',  ( 54.18345076886460987, 5.675359767207155848, -2.050000000000190781 ) ) ;
#13372=ORIENTED_EDGE ( 'NONE', *, *, #5129, .F. ) ;
#13375=CARTESIAN_POINT ( 'NONE',  ( 52.91918222397625726, 8.304852724747879833, 2.049999999999815525 ) ) ;
#13381=CARTESIAN_POINT ( 'NONE',  ( 30.67858157643048500, 7.123080578496862714, -2.050000000000106848 ) ) ;
#13386=DIRECTION ( 'NONE',  ( 0.000000000000000000, -0.2793919678926574668, 0.9601771338024398528 ) ) ;
#13387=EDGE_LOOP ( 'NONE', ( #15164, #18048, #9429, #19497 ) ) ;
#13415=CARTESIAN_POINT ( 'NONE',  ( 53.91582462592153746, 6.672259099522125148, 1.484227406530594262 ) ) ;
#13417=CARTESIAN_POINT ( 'NONE',  ( 30.08242191457676995, 7.215531071606934965, -1.425000000000104849 ) ) ;
#13418=CARTESIAN_POINT ( 'NONE',  ( 51.80000000000001137, -3.933368109459640660, -2.186004417993355542 ) ) ;
#13419=CARTESIAN_POINT ( 'NONE',  ( 41.48619405472010868, -151.3359592902261852, 1.549999999999835953 ) ) ;
#13422=AXIS2_PLACEMENT_3D ( 'NONE', #2927, #15417, #18132 ) ;
#13431=ORIENTED_EDGE ( 'NONE', *, *, #6988, .T. ) ;
#13432=B_SPLINE_CURVE_WITH_KNOTS ( 'NONE', 3,
 ( #6454, #16114, #25763, #13714, #27298, #27141 ),
 .UNSPECIFIED., .F., .F.,
 ( 4, 2, 4 ),
 ( 0.000000000000000000, 0.5000000000000000000, 1.000000000000000000 ),
 .UNSPECIFIED. ) ;
#13435=CARTESIAN_POINT ( 'NONE',  ( 52.91918222397625016, 8.304852724747879833, -2.050000000000184119 ) ) ;
#13442=CARTESIAN_POINT ( 'NONE',  ( 47.10000000000003695, 6.982261990806648555E-14, 4.499999999999873879 ) ) ;
#13444=CARTESIAN_POINT ( 'NONE',  ( 52.64059584688627780, 4.063092876230792072, -2.046235406917140232 ) ) ;
#13460=CARTESIAN_POINT ( 'NONE',  ( 53.76063741390514394, 7.747904304409473752, 2.049999999999812417 ) ) ;
#13461=DIRECTION ( 'NONE',  ( 0.000000000000000000, 0.000000000000000000, 1.000000000000000000 ) ) ;
#13463=ORIENTED_EDGE ( 'NONE', *, *, #7884, .F. ) ;
#13464=CARTESIAN_POINT ( 'NONE',  ( 41.48619405471885102, -151.3359592902622239, 1.949999999999835865 ) ) ;
#13475=VERTEX_POINT ( 'NONE', #23009 ) ;
#13493=VECTOR ( 'NONE', #17590, 999.9999999999998863 ) ;
#13514=CARTESIAN_POINT ( 'NONE',  ( 47.00000000000002842, -3.933368109459640660, 2.186004417993010485 ) ) ;
#13523=VECTOR ( 'NONE', #30348, 1000.000000000000000 ) ;
#13527=CARTESIAN_POINT ( 'NONE',  ( 51.87416143049284756, 8.598705507415683513, 1.949999999999818767 ) ) ;
#13530=CARTESIAN_POINT ( 'NONE',  ( 52.16611735465139077, 8.588510181886395145, -1.949999998429221337 ) ) ;
#13544=CARTESIAN_POINT ( 'NONE',  ( 54.04559870188514736, 5.332923641039334584, -2.050000000000188116 ) ) ;
#13547=CARTESIAN_POINT ( 'NONE',  ( 51.52211690305919944, -3.792101016927673207, 1.560991511224173900 ) ) ;
#13550=CARTESIAN_POINT ( 'NONE',  ( 53.12888913849685224, 4.216863368992567196, 2.049999999999814637 ) ) ;
#13553=CARTESIAN_POINT ( 'NONE',  ( 51.30415252705748941, -3.900546889229941971, -1.266936454265872314 ) ) ;
#13556=CARTESIAN_POINT ( 'NONE',  ( 32.27298585237639372, 7.910008090200282282, -2.050000000000112177 ) ) ;
#13557=CARTESIAN_POINT ( 'NONE',  ( 47.07708546080151280, 8.766223091587681537, 1.549999999999835953 ) ) ;
#13562=ORIENTED_EDGE ( 'NONE', *, *, #16519, .T. ) ;
#13574=CARTESIAN_POINT ( 'NONE',  ( 53.30089595108377409, 4.970692136877041811, 1.612337884061097348 ) ) ;
#13580=CARTESIAN_POINT ( 'NONE',  ( 51.87582967299545800, 8.646477722258158138, 2.039222690360799728 ) ) ;
#13585=DIRECTION ( 'NONE',  ( 3.489354422748178582E-15, -1.218509414717996338E-16, 1.000000000000000000 ) ) ;
#13592=CARTESIAN_POINT ( 'NONE',  ( 50.80000000000002558, 0.2793919678926817252, 0.9601771338022635494 ) ) ;
#13593=CARTESIAN_POINT ( 'NONE',  ( 22.61091062207858116, 6.637672121856524221, 2.049999999999720934 ) ) ;
#13596=EDGE_CURVE ( 'NONE', #30852, #24179, #407, .T. ) ;
#13602=CARTESIAN_POINT ( 'NONE',  ( 50.87477060347375613, 8.633605004118185988, 2.008578643762513050 ) ) ;
#13605=CARTESIAN_POINT ( 'NONE',  ( 52.44049727168176389, 4.003343267869601263, -2.045783429862717995 ) ) ;
#13617=CARTESIAN_POINT ( 'NONE',  ( 54.12895949791517580, 5.523355893849346110, 2.049999999999811084 ) ) ;
#13623=EDGE_LOOP ( 'NONE', ( #18754, #10406, #10763, #10207 ) ) ;
#13629=CARTESIAN_POINT ( 'NONE',  ( 21.97322666366011745, 8.076925076899298617, 1.949999999999923128 ) ) ;
#13642=CARTESIAN_POINT ( 'NONE',  ( 22.04321716858594016, 7.679566743993225586, -1.425000000000077316 ) ) ;
#13647=LINE ( 'NONE', #1947, #8435 ) ;
#13654=CARTESIAN_POINT ( 'NONE',  ( 47.10000000000000853, 7.038595743567426471E-14, -4.600000000000200373 ) ) ;
#13657=CARTESIAN_POINT ( 'NONE',  ( 51.80000000000001137, 4.350000000000017408, -1.550321101314903194 ) ) ;
#13659=ORIENTED_EDGE ( 'NONE', *, *, #6908, .F. ) ;
#13672=ORIENTED_EDGE ( 'NONE', *, *, #5182, .T. ) ;
#13673=CARTESIAN_POINT ( 'NONE',  ( 22.68548117337039471, 6.704541182151974255, -2.050000000000079314 ) ) ;
#13680=ADVANCED_FACE ( 'NONE', ( #19366 ), #13213, .T. ) ;
#13690=CARTESIAN_POINT ( 'NONE',  ( 51.68195507589560123, -4.249103233463753071, 1.767380283559480958 ) ) ;
#13694=CARTESIAN_POINT ( 'NONE',  ( 50.35762544161294585, 8.151359338959888845, -1.950000000000174927 ) ) ;
#13700=CARTESIAN_POINT ( 'NONE',  ( 52.05393800078974920, 4.345106731198625560, 2.049999999999818190 ) ) ;
#13702=DIRECTION ( 'NONE',  ( 3.489354422748178582E-15, -1.218509414717996338E-16, 1.000000000000000000 ) ) ;
#13709=DIRECTION ( 'NONE',  ( 0.9993908270191184107, -0.03489949670185085034, -3.491481338843133355E-15 ) ) ;
#13714=CARTESIAN_POINT ( 'NONE',  ( 51.87453755317503834, 8.609476251808864333, -2.002198665876508521 ) ) ;
#13735=ADVANCED_FACE ( 'NONE', ( #14711 ), #12320, .T. ) ;
#13740=DIRECTION ( 'NONE',  ( 3.384826294588897856E-15, 0.000000000000000000, 1.000000000000000000 ) ) ;
#13741=EDGE_CURVE ( 'NONE', #28051, #22264, #638, .T. ) ;
#13745=CARTESIAN_POINT ( 'NONE',  ( 53.29166889513722793, 4.961539162849967433, -1.611464872099122481 ) ) ;
#13757=CARTESIAN_POINT ( 'NONE',  ( 47.02503650169320082, -4.051364836627049826, -1.951815467915571922 ) ) ;
#13772=EDGE_LOOP ( 'NONE', ( #8207, #4560, #28890, #878 ) ) ;
#13786=CARTESIAN_POINT ( 'NONE',  ( 28.86359278493677039, 5.838313002610202140, -1.425000000000100409 ) ) ;
#13792=CARTESIAN_POINT ( 'NONE',  ( 50.87477060347373481, 8.633605004118187765, -2.050000000000176570 ) ) ;
#13801=CARTESIAN_POINT ( 'NONE',  ( 51.80000000000002558, 6.475000000000062705, 1.949999999999818767 ) ) ;
#13803=ORIENTED_EDGE ( 'NONE', *, *, #3684, .F. ) ;
#13804=CARTESIAN_POINT ( 'NONE',  ( 54.15675781068899397, 5.684314874070254042, -2.050000000000189004 ) ) ;
#13810=CARTESIAN_POINT ( 'NONE',  ( 51.80290302015603032, -4.086844330038878148, -2.115703333131829567 ) ) ;
#13831=VECTOR ( 'NONE', #17743, 1000.000000000000000 ) ;
#13838=ORIENTED_EDGE ( 'NONE', *, *, #27210, .F. ) ;
#13844=CARTESIAN_POINT ( 'NONE',  ( 52.11520194349620283, 3.840337079369375406, 2.049999999999818190 ) ) ;
#13847=CARTESIAN_POINT ( 'NONE',  ( 50.80000000000001847, -4.031600731908414836, -1.173113608511851647 ) ) ;
#13848=EDGE_CURVE ( 'NONE', #28571, #7964, #21157, .T. ) ;
#13861=CARTESIAN_POINT ( 'NONE',  ( 47.44023805160308882, -4.327157167232345003, 1.563052875988448776 ) ) ;
#13876=B_SPLINE_CURVE_WITH_KNOTS ( 'NONE', 3,
 ( #15378, #3045, #5420, #15075, #2590, #12688, #27100, #12236, #19695, #361, #10168, #24568, #199, #10030, #29330, #22368, #19837, #29467, #14763, #658 ),
 .UNSPECIFIED., .F., .F.,
 ( 4, 2, 2, 2, 2, 2, 2, 2, 2, 4 ),
 ( -9.867963739368879538E-05, 0.0004287238591677978820, 0.0009561273557292845459, 0.001483530852290771643, 0.002010934348852258524, 0.002538337845413745405, 0.003065741341975232719, 0.003329443090255982448, 0.003593144838536732177, 0.004120548335098232068 ),
 .UNSPECIFIED. ) ;
#13886=B_SPLINE_SURFACE_WITH_KNOTS ( 'NONE', 3, 1, ( 
 ( #9995, #18910 ),
 ( #28554, #6865 ),
 ( #16533, #21448 ),
 ( #20287, #10754 ),
 ( #15347, #22957 ),
 ( #18060, #20753 ),
 ( #15678, #3322 ),
 ( #6174, #29763 ),
 ( #8683, #18363 ),
 ( #8080, #959 ),
 ( #13417, #12805 ),
 ( #20436, #17745 ),
 ( #28001, #1411 ),
 ( #27387, #30230 ),
 ( #8538, #8376 ) ),
 .UNSPECIFIED., .F., .F., .F.,
 ( 4, 1, 1, 1, 1, 1, 1, 1, 1, 1, 1, 1, 4 ),
 ( 2, 2 ),
 ( 0.03200690811995968860, 0.06212998257909596589, 0.1242599651581919318, 0.2485199303163838636, 0.3727798954745757953, 0.4970398606327676716, 0.6212998257909596589, 0.6834298083700556248, 0.7455597909491514796, 0.8076897735282474455, 0.8387547648177954285, 0.8698197561073434114, 0.8953196945511240346 ),
 ( 0.000000000000000000, 1.000000000000000000 ),
 .UNSPECIFIED. ) ;
#13892=CARTESIAN_POINT ( 'NONE',  ( 51.70000000000002416, 6.982261990806648555E-14, -1.793082891011605378E-13 ) ) ;
#13896=CIRCLE ( 'NONE', #264, 160.5997717543497743 ) ;
#13897=CARTESIAN_POINT ( 'NONE',  ( 51.80000000000001137, 6.475000000000062705, -2.050000000000180123 ) ) ;
#13904=CIRCLE ( 'NONE', #4309, 4.099999999999992539 ) ;
#13909=CARTESIAN_POINT ( 'NONE',  ( 41.48619405471883681, -151.3359592902622239, -1.950000000000163380 ) ) ;
#13917=CARTESIAN_POINT ( 'NONE',  ( 47.10000001624534605, -4.079529477378120994, -2.128865254697307474 ) ) ;
#13936=CARTESIAN_POINT ( 'NONE',  ( 51.80000000000002558, 3.987920669275808905, 2.032050446608677507 ) ) ;
#13944=AXIS2_PLACEMENT_3D ( 'NONE', #1056, #578, #5973 ) ;
#13948=DIRECTION ( 'NONE',  ( -0.9993908270191123044, 0.03489949670202457249, 4.336808689942002748E-15 ) ) ;
#13951=FACE_OUTER_BOUND ( 'NONE', #10221, .T. ) ;
#13955=VECTOR ( 'NONE', #12239, 999.9999999999998863 ) ;
#13959=FACE_OUTER_BOUND ( 'NONE', #24293, .T. ) ;
#13976=B_SPLINE_CURVE_WITH_KNOTS ( 'NONE', 3,
 ( #12045, #7445, #21719, #9676, #28972, #7279, #26594, #4904, #14569, #24232, #2543, #21872, #10271, #30043, #3760, #5839, #27217, #15496 ),
 .UNSPECIFIED., .F., .F.,
 ( 4, 2, 2, 2, 2, 1, 1, 2, 2, 4 ),
 ( 0.000000000000000000, 0.1171184220236923118, 0.2342368440473846236, 0.2488766468003461019, 0.2525365974885872000, 0.2561965481768282982, 0.2635164495533074969, 0.2927960550592145217, 0.3513552660710277942, 0.4684736880946559490 ),
 .UNSPECIFIED. ) ;
#13987=VECTOR ( 'NONE', #27595, 1000.000000000000114 ) ;
#13994=DIRECTION ( 'NONE',  ( 0.000000000000000000, 0.000000000000000000, 1.000000000000000000 ) ) ;
#14009=DIRECTION ( 'NONE',  ( -0.7313537016191670181, -0.6819983600625022513, 2.468850131082252327E-15 ) ) ;
#14014=ORIENTED_EDGE ( 'NONE', *, *, #2235, .F. ) ;
#14015=CARTESIAN_POINT ( 'NONE',  ( 52.38400031671234558, 8.538946093000230775, 1.943109374214545770 ) ) ;
#14017=DIRECTION ( 'NONE',  ( 3.491481338843133355E-15, 0.000000000000000000, 1.000000000000000000 ) ) ;
#14018=CARTESIAN_POINT ( 'NONE',  ( 50.93220014711046417, -4.031600731540152083, -1.173113608404695585 ) ) ;
#14022=AXIS2_PLACEMENT_3D ( 'NONE', #19419, #15118, #2627 ) ;
#14023=ORIENTED_EDGE ( 'NONE', *, *, #211, .F. ) ;
#14031=CARTESIAN_POINT ( 'NONE',  ( 53.32365433735401439, 7.956691627322815208, 1.890490914785547094 ) ) ;
#14048=AXIS2_PLACEMENT_3D ( 'NONE', #15377, #22367, #27099 ) ;
#14049=LINE ( 'NONE', #11686, #22047 ) ;
#14065=DIRECTION ( 'NONE',  ( 0.03489949670250097613, 0.9993908270190957621, 0.000000000000000000 ) ) ;
#14087=ADVANCED_FACE ( 'NONE', ( #14677 ), #24336, .T. ) ;
#14091=DIRECTION ( 'NONE',  ( -1.000000000000000000, 0.000000000000000000, 3.491481338843133355E-15 ) ) ;
#14095=AXIS2_PLACEMENT_3D ( 'NONE', #17116, #10436, #18046 ) ;
#14112=ORIENTED_EDGE ( 'NONE', *, *, #29660, .F. ) ;
#14114=EDGE_CURVE ( 'NONE', #7683, #24892, #845, .T. ) ;
#14118=EDGE_CURVE ( 'NONE', #13124, #8009, #8659, .T. ) ;
#14128=CARTESIAN_POINT ( 'NONE',  ( 51.75935175331192539, 4.143357532304555946, -1.955579579481696806 ) ) ;
#14135=CARTESIAN_POINT ( 'NONE',  ( 53.96628743859024979, 7.375742867302039762, 2.049999999999812417 ) ) ;
#14139=CARTESIAN_POINT ( 'NONE',  ( 54.25934562490486002, 5.649897281828979878, -2.026384253567227400 ) ) ;
#14154=CARTESIAN_POINT ( 'NONE',  ( 51.79856634703980944, 4.577364735441398658, 0.5261184863197011508 ) ) ;
#14160=CARTESIAN_POINT ( 'NONE',  ( 28.70703846152719052, 5.747922418238211151, 1.949999999999901368 ) ) ;
#14172=B_SPLINE_SURFACE_WITH_KNOTS ( 'NONE', 3, 3, ( 
 ( #2940, #15431, #8005, #20043 ),
 ( #29686, #20369, #26990, #12584 ),
 ( #14802, #20213, #24780, #3089 ),
 ( #880, #19743, #17345, #12737 ),
 ( #22740, #27315, #10069, #5628 ),
 ( #24463, #5297, #2774, #705 ),
 ( #8155, #29373, #15278, #17826 ) ),
 .UNSPECIFIED., .F., .F., .F.,
 ( 4, 1, 1, 1, 4 ),
 ( 4, 4 ),
 ( 0.9434208788814886226, 0.9575656591611163559, 0.9717104394407443113, 0.9858552197203721557, 1.000000000000000000 ),
 ( 0.000000000000000000, 1.000000000000000000 ),
 .UNSPECIFIED. ) ;
#14175=CARTESIAN_POINT ( 'NONE',  ( 41.48619405471883681, -151.3359592902621955, -2.050000000000163691 ) ) ;
#14179=ORIENTED_EDGE ( 'NONE', *, *, #24512, .F. ) ;
#14184=ORIENTED_EDGE ( 'NONE', *, *, #26168, .T. ) ;
#14204=DIRECTION ( 'NONE',  ( -0.9993908270190957621, 0.03489949670250106634, 3.490838185622846777E-15 ) ) ;
#14209=CARTESIAN_POINT ( 'NONE',  ( 53.24194194228307708, 4.913799063695436509, 1.606901569590256873 ) ) ;
#14210=CARTESIAN_POINT ( 'NONE',  ( 53.92227604462289747, 6.075002921772748365, 1.819877325055229145 ) ) ;
#14226=CARTESIAN_POINT ( 'NONE',  ( 51.70000000000002416, 6.982261990806648555E-14, -1.793082891011605378E-13 ) ) ;
#14240=DIRECTION ( 'NONE',  ( 3.491481338843133355E-15, -0.000000000000000000, 1.000000000000000000 ) ) ;
#14247=EDGE_CURVE ( 'NONE', #15276, #25126, #10933, .T. ) ;
#14256=CARTESIAN_POINT ( 'NONE',  ( 51.88812122917394021, 8.998461838226448961, -2.050000000000180123 ) ) ;
#14265=CARTESIAN_POINT ( 'NONE',  ( 47.38300905981536459, -4.256549615192540159, 1.449195206876313202 ) ) ;
#14272=ORIENTED_EDGE ( 'NONE', *, *, #15765, .F. ) ;
#14295=CARTESIAN_POINT ( 'NONE',  ( 31.59287277085100243, 7.495449159457947097, -1.098631611690421797E-13 ) ) ;
#14296=CARTESIAN_POINT ( 'NONE',  ( 54.22606406116597810, 5.661063141734079984, -2.046523645606439956 ) ) ;
#14300=CARTESIAN_POINT ( 'NONE',  ( 51.06445037214141536, -4.311893144378706744, 1.282556980650388700 ) ) ;
#14312=CARTESIAN_POINT ( 'NONE',  ( 31.77414890175571927, 7.582826005769804922, 2.049999999999889244 ) ) ;
#14333=CARTESIAN_POINT ( 'NONE',  ( 53.88135321025247748, 4.969568719840013138, 2.049999999999811973 ) ) ;
#14359=DIRECTION ( 'NONE',  ( 0.9993908270191184107, -0.03489949670185085034, -3.491481338843133355E-15 ) ) ;
#14369=ORIENTED_EDGE ( 'NONE', *, *, #8696, .F. ) ;
#14384=DIRECTION ( 'NONE',  ( -1.000000000000000000, 0.000000000000000000, 3.491481338843133355E-15 ) ) ;
#14388=VERTEX_POINT ( 'NONE', #15909 ) ;
#14389=CARTESIAN_POINT ( 'NONE',  ( 47.02992830280592074, -3.673656954000148023, -1.824471899732945879 ) ) ;
#14395=EDGE_CURVE ( 'NONE', #29801, #22859, #15515, .T. ) ;
#14401=CARTESIAN_POINT ( 'NONE',  ( 26.87602198329691205, 5.247164978609345276, 1.424999999999906564 ) ) ;
#14409=TOROIDAL_SURFACE ( 'NONE', #27611, 4.500000000000037303, 0.1000000000000000056 ) ;
#14414=DIRECTION ( 'NONE',  ( -0.03489949670185085034, -0.9993908270191184107, -2.271278457551021927E-27 ) ) ;
#14425=EDGE_CURVE ( 'NONE', #12841, #5179, #19995, .T. ) ;
#14428=CARTESIAN_POINT ( 'NONE',  ( 54.16371155698126216, 6.950779743548840983, -2.050000000000189004 ) ) ;
#14429=DIRECTION ( 'NONE',  ( -9.754918421198724481E-16, 0.9601771338024399638, -0.2793919678926571892 ) ) ;
#14433=VECTOR ( 'NONE', #24564, 1000.000000000000000 ) ;
#14448=CARTESIAN_POINT ( 'NONE',  ( 54.22146708689643191, 6.361260388417356637, -2.050000000000189004 ) ) ;
#14450=B_SPLINE_CURVE_WITH_KNOTS ( 'NONE', 3,
 ( #10134, #5073, #22021, #9820 ),
 .UNSPECIFIED., .F., .F.,
 ( 4, 4 ),
 ( 0.000000000000000000, 1.000000000000000000 ),
 .UNSPECIFIED. ) ;
#14454=CARTESIAN_POINT ( 'NONE',  ( 31.35411506561226602, 7.935106537971987173, 1.424999999999891021 ) ) ;
#14462=CARTESIAN_POINT ( 'NONE',  ( 51.83503441027635716, 4.481775199104232499, 1.044099630206801743 ) ) ;
#14467=DIRECTION ( 'NONE',  ( 0.9993908270190957621, -0.03489949670250097613, -3.491481338843133355E-15 ) ) ;
#14470=CARTESIAN_POINT ( 'NONE',  ( 30.23587923126626364, 6.713699170112940706, 2.049999999999764011 ) ) ;
#14474=CARTESIAN_POINT ( 'NONE',  ( 47.06312566212015724, 8.366466760780054912, -1.950000000000163380 ) ) ;
#14485=AXIS2_PLACEMENT_3D ( 'NONE', #728, #10561, #29709 ) ;
#14489=CIRCLE ( 'NONE', #21588, 4.500000000000037303 ) ;
#14490=CARTESIAN_POINT ( 'NONE',  ( 51.39453088482486010, 4.389042235173731044, 1.549999999999820410 ) ) ;
#14497=CARTESIAN_POINT ( 'NONE',  ( 54.16568811108924564, 5.603438171869654205, 2.049999999999811084 ) ) ;
#14499=CARTESIAN_POINT ( 'NONE',  ( 50.87477060347373481, 8.633605004118187765, -1.950000000000176925 ) ) ;
#14509=CARTESIAN_POINT ( 'NONE',  ( 53.54945434694669615, 7.685534019892441115, 1.865296441523391024 ) ) ;
#14534=CARTESIAN_POINT ( 'NONE',  ( 53.91566580141705600, 6.672244292255798293, 1.816235488581843693 ) ) ;
#14537=CIRCLE ( 'NONE', #13014, 0.1000000000000007133 ) ;
#14561=VECTOR ( 'NONE', #18614, 1000.000000000000000 ) ;
#14564=CARTESIAN_POINT ( 'NONE',  ( 51.80000000000002558, 4.175664755576631748, 1.929721184273780255 ) ) ;
#14565=DIRECTION ( 'NONE',  ( -0.9993908270191184107, 0.03489949670185085034, 3.491481338843133355E-15 ) ) ;
#14569=CARTESIAN_POINT ( 'NONE',  ( 53.35813067190703407, 7.919951180354087406, -1.887104237684443353 ) ) ;
#14572=CARTESIAN_POINT ( 'NONE',  ( 22.11060592828335558, 7.457498294695584562, 1.424999999999924105 ) ) ;
#14587=EDGE_LOOP ( 'NONE', ( #4238, #21846, #3793, #11177 ) ) ;
#14593=SURFACE_STYLE_USAGE ( .BOTH. , #4933 ) ;
#14596=CARTESIAN_POINT ( 'NONE',  ( 52.11520194349618862, 3.840337079369375406, -2.050000000000181455 ) ) ;
#14612=EDGE_CURVE ( 'NONE', #16445, #4765, #20598, .T. ) ;
#14613=ORIENTED_EDGE ( 'NONE', *, *, #6582, .T. ) ;
#14621=EDGE_LOOP ( 'NONE', ( #31136, #8045, #30770, #6134, #26373, #31284 ) ) ;
#14622=CARTESIAN_POINT ( 'NONE',  ( 50.80000000000002558, -3.936726248589973221, 1.145507068359715941 ) ) ;
#14624=EDGE_CURVE ( 'NONE', #24006, #17544, #27646, .T. ) ;
#14628=EDGE_CURVE ( 'NONE', #23376, #27880, #11087, .T. ) ;
#14629=CARTESIAN_POINT ( 'NONE',  ( 51.80000048029754822, 4.021162616303429971, -2.019962949071075542 ) ) ;
#14631=CARTESIAN_POINT ( 'NONE',  ( 34.56702326949726256, 8.213851659285209550, 1.949999999999879385 ) ) ;
#14636=VECTOR ( 'NONE', #28426, 999.9999999999998863 ) ;
#14662=CARTESIAN_POINT ( 'NONE',  ( 23.93113343277026317, 5.410774079442639994, -1.950000000000083000 ) ) ;
#14665=CARTESIAN_POINT ( 'NONE',  ( 31.90749320846404657, 7.645246315295578299, -1.950000000000144063 ) ) ;
#14668=CARTESIAN_POINT ( 'NONE',  ( 51.80000000000002558, -4.031600731908413948, 1.173113608511492822 ) ) ;
#14669=ADVANCED_FACE ( 'NONE', ( #10925 ), #22107, .T. ) ;
#14670=CARTESIAN_POINT ( 'NONE',  ( 51.80000000000002558, 4.350000000000017408, 1.495827530165114050 ) ) ;
#14675=CARTESIAN_POINT ( 'NONE',  ( 53.49139514279641361, 5.155866831720374854, -1.635615235160539749 ) ) ;
#14677=FACE_OUTER_BOUND ( 'NONE', #18102, .T. ) ;
#14685=CARTESIAN_POINT ( 'NONE',  ( 53.91582462592152325, 6.672259099522126036, -1.774223561664970861 ) ) ;
#14696=CIRCLE ( 'NONE', #3580, 0.1000000000000002554 ) ;
#14708=DIRECTION ( 'NONE',  ( 0.000000000000000000, 0.000000000000000000, -1.000000000000000000 ) ) ;
#14711=FACE_OUTER_BOUND ( 'NONE', #26191, .T. ) ;
#14732=VERTEX_POINT ( 'NONE', #4115 ) ;
#14737=ORIENTED_EDGE ( 'NONE', *, *, #7674, .F. ) ;
#14741=EDGE_LOOP ( 'NONE', ( #11134, #2854, #1679, #7575 ) ) ;
#14744=CARTESIAN_POINT ( 'NONE',  ( 53.71501932699289483, 7.815554144461332342, -2.050000000000187228 ) ) ;
#14749=TOROIDAL_SURFACE ( 'NONE', #30942, 4.500000000000037303, 0.1000000000000000056 ) ;
#14750=DIRECTION ( 'NONE',  ( 3.491481338843133355E-15, 0.000000000000000000, 1.000000000000000000 ) ) ;
#14759=FACE_OUTER_BOUND ( 'NONE', #23851, .T. ) ;
#14763=CARTESIAN_POINT ( 'NONE',  ( 51.87803684735047227, 3.845118170584751915, -1.423186137768011505 ) ) ;
#14766=FACE_OUTER_BOUND ( 'NONE', #6903, .T. ) ;
#14779=CARTESIAN_POINT ( 'NONE',  ( 30.23587923389744958, 6.713699166094349025, 1.949999999999828315 ) ) ;
#14785=B_SPLINE_CURVE_WITH_KNOTS ( 'NONE', 3,
 ( #27321, #14963, #714, #29521, #15130, #8477, #20525, #12593 ),
 .UNSPECIFIED., .F., .F.,
 ( 4, 2, 2, 4 ),
 ( 0.000000000000000000, 0.0007042195513453405453, 0.001056329327018010709, 0.001408439102690681091 ),
 .UNSPECIFIED. ) ;
#14793=CARTESIAN_POINT ( 'NONE',  ( 52.98236138753793512, 8.264679131573696935, 1.919164453910085610 ) ) ;
#14795=ORIENTED_EDGE ( 'NONE', *, *, #9494, .T. ) ;
#14796=ORIENTED_EDGE ( 'NONE', *, *, #11867, .T. ) ;
#14802=CARTESIAN_POINT ( 'NONE',  ( 54.02713021818536987, 5.727804820055879098, -2.034063242164690255 ) ) ;
#14805=EDGE_CURVE ( 'NONE', #13278, #14388, #29398, .T. ) ;
#14806=ORIENTED_EDGE ( 'NONE', *, *, #15293, .T. ) ;
#14807=CARTESIAN_POINT ( 'NONE',  ( 31.77414890175468898, 7.582826005769556232, -2.049999999999980282 ) ) ;
#14814=CARTESIAN_POINT ( 'NONE',  ( 53.49139514279633545, 5.155866831720416599, -2.050000000000122835 ) ) ;
#14820=EDGE_CURVE ( 'NONE', #16720, #17544, #12472, .T. ) ;
#14822=EDGE_CURVE ( 'NONE', #30937, #13475, #2874, .T. ) ;
#14827=CARTESIAN_POINT ( 'NONE',  ( 53.94302949754625587, 6.378738024272571749, 1.816235488581843693 ) ) ;
#14838=CARTESIAN_POINT ( 'NONE',  ( 52.64068875113407131, 4.063124538860861001, 2.046235746538459743 ) ) ;
#14873=CARTESIAN_POINT ( 'NONE',  ( 47.49384476122470033, -3.992023072242622206, 1.294577227648573192 ) ) ;
#14879=ORIENTED_EDGE ( 'NONE', *, *, #28240, .F. ) ;
#14888=CARTESIAN_POINT ( 'NONE',  ( 51.74548155811469741, 3.822334312940638412, -2.050000000000177902 ) ) ;
#14899=DIRECTION ( 'NONE',  ( -1.000000000000000000, -0.000000000000000000, 3.491481338843133355E-15 ) ) ;
#14903=AXIS2_PLACEMENT_3D ( 'NONE', #26953, #15241, #24887 ) ;
#14904=CARTESIAN_POINT ( 'NONE',  ( 47.10000000000003695, 2.428612866367529932E-14, 4.099999999999827338 ) ) ;
#14907=CARTESIAN_POINT ( 'NONE',  ( 54.15675781068899397, 5.684314874070254042, -2.050000000000189004 ) ) ;
#14911=AXIS2_PLACEMENT_3D ( 'NONE', #13464, #1446, #4136 ) ;
#14922=CARTESIAN_POINT ( 'NONE',  ( 22.79271333219191931, 6.591595603791505553, 2.049999999999919442 ) ) ;
#14926=B_SPLINE_CURVE_WITH_KNOTS ( 'NONE', 3,
 ( #24284, #16701, #2438, #21616, #19074, #2595, #9405, #4796, #205, #18912, #16534, #26189, #23971, #4492, #14454 ),
 .UNSPECIFIED., .F., .F.,
 ( 4, 1, 1, 1, 1, 1, 1, 1, 1, 1, 1, 1, 4 ),
 ( 0.03200690811994862106, 0.06212998257909596589, 0.1242599651581919179, 0.2485199303163838636, 0.3727798954745757953, 0.4970398606327676716, 0.6212998257909596589, 0.6834298083700556248, 0.7455597909491514796, 0.8076897735282474455, 0.8387547648177954285, 0.8698197561073434114, 0.8953196948241715081 ),
 .UNSPECIFIED. ) ;
#14941=CARTESIAN_POINT ( 'NONE',  ( 53.74478519188840409, 7.379842749953129832, 1.837855077339518362 ) ) ;
#14945=ORIENTED_EDGE ( 'NONE', *, *, #21423, .T. ) ;
#14949=DIRECTION ( 'NONE',  ( -9.754918421198722508E-16, -0.9601771338024398528, -0.2793919678926571337 ) ) ;
#14954=CARTESIAN_POINT ( 'NONE',  ( 50.93148713995405785, -4.319730106380442081, -1.256953381515634849 ) ) ;
#14959=CARTESIAN_POINT ( 'NONE',  ( 27.54696499482717442, 5.363421040582472266, -1.950000000000027711 ) ) ;
#14963=CARTESIAN_POINT ( 'NONE',  ( 47.76370854686960854, -3.908336260473453727, 1.238913909465753971 ) ) ;
#14967=FACE_OUTER_BOUND ( 'NONE', #21782, .T. ) ;
#14970=CARTESIAN_POINT ( 'NONE',  ( 53.78456803694546551, 5.661108390837235937, -2.050000000000250289 ) ) ;
#14972=CYLINDRICAL_SURFACE ( 'NONE', #23732, 0.2500000000000002220 ) ;
#14985=CARTESIAN_POINT ( 'NONE',  ( 54.21130113843405951, 6.699806482265510787, 2.049999999999811529 ) ) ;
#14991=DIRECTION ( 'NONE',  ( 3.491481338843133355E-15, -0.000000000000000000, 1.000000000000000000 ) ) ;
#14993=CARTESIAN_POINT ( 'NONE',  ( 47.12350347295471664, -3.663955391962992802, -1.843087722223818004 ) ) ;
#15000=AXIS2_PLACEMENT_3D ( 'NONE', #26294, #8703, #25658 ) ;
#15011=CIRCLE ( 'NONE', #25607, 4.199999999999993072 ) ;
#15027=CARTESIAN_POINT ( 'NONE',  ( 27.56628230087643416, 5.372092466067856620, 1.424999999999904565 ) ) ;
#15032=ORIENTED_EDGE ( 'NONE', *, *, #27741, .T. ) ;
#15040=ORIENTED_EDGE ( 'NONE', *, *, #10433, .T. ) ;
#15052=AXIS2_PLACEMENT_3D ( 'NONE', #23560, #16757, #14204 ) ;
#15075=CARTESIAN_POINT ( 'NONE',  ( 52.37358958628623640, 3.908449573900731444, 1.241066825229008685 ) ) ;
#15082=ORIENTED_EDGE ( 'NONE', *, *, #228, .T. ) ;
#15085=ORIENTED_EDGE ( 'NONE', *, *, #6697, .F. ) ;
#15094=AXIS2_PLACEMENT_3D ( 'NONE', #31207, #19195, #1736 ) ;
#15095=CARTESIAN_POINT ( 'NONE',  ( 22.00282357524792687, 7.757228885921422012, 2.050000000000460787 ) ) ;
#15103=DIRECTION ( 'NONE',  ( 9.754918421198724481E-16, 0.9601771338024399638, 0.2793919678926571892 ) ) ;
#15110=( GEOMETRIC_REPRESENTATION_CONTEXT ( 3 ) GLOBAL_UNCERTAINTY_ASSIGNED_CONTEXT ( ( #8219 ) ) GLOBAL_UNIT_ASSIGNED_CONTEXT ( ( #19508, #22964, #25182 ) ) REPRESENTATION_CONTEXT ( 'NONE', 'WORKASPACE' ) );
#15118=DIRECTION ( 'NONE',  ( -0.9993908270191184107, 0.03489949670185085034, 3.491481338843133355E-15 ) ) ;
#15126=CARTESIAN_POINT ( 'NONE',  ( 28.70703846152805028, 5.747922418238541553, -1.950000000000162936 ) ) ;
#15129=CIRCLE ( 'NONE', #18181, 160.6997717543497686 ) ;
#15130=CARTESIAN_POINT ( 'NONE',  ( 47.21343356430319460, -3.755435527867144962, 1.648753881545072630 ) ) ;
#15135=CARTESIAN_POINT ( 'NONE',  ( 52.54946733419072302, 4.465216787881787219, -2.050000000000182787 ) ) ;
#15136=CARTESIAN_POINT ( 'NONE',  ( 48.00000000000001421, -4.031600731908414836, -1.173113608511841877 ) ) ;
#15148=CARTESIAN_POINT ( 'NONE',  ( 54.44703553260186624, 6.360744355421148022, -0.9750000000001826095 ) ) ;
#15154=CARTESIAN_POINT ( 'NONE',  ( 53.89553379148907908, 6.017104844469305824, 1.708828125785182728 ) ) ;
#15164=ORIENTED_EDGE ( 'NONE', *, *, #2248, .T. ) ;
#15167=CARTESIAN_POINT ( 'NONE',  ( 48.00000000000001421, -4.003661535119149129, -1.269131321892086106 ) ) ;
#15180=B_SPLINE_CURVE_WITH_KNOTS ( 'NONE', 3,
 ( #5959, #19893, #5634, #10546, #8310, #10223 ),
 .UNSPECIFIED., .F., .F.,
 ( 4, 2, 4 ),
 ( 0.000000000000000000, 0.5000000000000000000, 1.000000000000000000 ),
 .UNSPECIFIED. ) ;
#15212=CARTESIAN_POINT ( 'NONE',  ( 51.46757676178951613, 4.376162276235350035, -1.550000000000179012 ) ) ;
#15235=CARTESIAN_POINT ( 'NONE',  ( 51.80000000000002558, 0.2793919678926817807, 0.9601771338022603297 ) ) ;
#15241=DIRECTION ( 'NONE',  ( 0.9993908270190957621, -0.03489949670250097613, -3.491481338843133355E-15 ) ) ;
#15250=CARTESIAN_POINT ( 'NONE',  ( 22.09542497196702371, 7.445411295444298361, 1.949999999999922240 ) ) ;
#15265=CARTESIAN_POINT ( 'NONE',  ( 53.46805841003781978, 8.044896776089471402, -2.050000000000185452 ) ) ;
#15267=CARTESIAN_POINT ( 'NONE',  ( 53.38897031725308295, 5.061772353509735645, 1.621051207520878723 ) ) ;
#15268=AXIS2_PLACEMENT_3D ( 'NONE', #9336, #4104, #4253 ) ;
#15276=VERTEX_POINT ( 'NONE', #4353 ) ;
#15278=CARTESIAN_POINT ( 'NONE',  ( 53.94314916079858335, 6.379172879799750007, -1.774223561664970861 ) ) ;
#15282=CARTESIAN_POINT ( 'NONE',  ( 29.99460041311474612, 6.535150002936296332, -2.049999999999972733 ) ) ;
#15288=CARTESIAN_POINT ( 'NONE',  ( 52.72145679358933279, 4.007061708474140893, -2.050000000000183675 ) ) ;
#15289=EDGE_CURVE ( 'NONE', #22328, #8527, #23222, .T. ) ;
#15290=CARTESIAN_POINT ( 'NONE',  ( 47.12910489933606328, -3.772469189071208095, -1.610667359469886595 ) ) ;
#15293=EDGE_CURVE ( 'NONE', #29801, #8009, #1819, .T. ) ;
#15298=CARTESIAN_POINT ( 'NONE',  ( 50.31971926781693583, 8.252744006147214151, -2.050000000000174794 ) ) ;
#15303=CARTESIAN_POINT ( 'NONE',  ( 54.29334943003577507, 6.002962681774890008, 2.049999999999807532 ) ) ;
#15310=CARTESIAN_POINT ( 'NONE',  ( 51.70000000000003126, -4.020776289669855785, 2.234582293948397691 ) ) ;
#15311=CARTESIAN_POINT ( 'NONE',  ( 51.67650754010888647, -3.859221392886597712, -1.645001822843487949 ) ) ;
#15316=CARTESIAN_POINT ( 'NONE',  ( 52.54185214673768911, 4.030541857796934302, 2.045987466503689234 ) ) ;
#15317=CARTESIAN_POINT ( 'NONE',  ( 41.48619405471883681, -151.3359592902622239, -2.050000000000163691 ) ) ;
#15318=ORIENTED_EDGE ( 'NONE', *, *, #15801, .T. ) ;
#15320=CARTESIAN_POINT ( 'NONE',  ( 53.94245690748179811, 6.674762429336770886, -1.915449902665558701 ) ) ;
#15326=ORIENTED_EDGE ( 'NONE', *, *, #20270, .T. ) ;
#15347=CARTESIAN_POINT ( 'NONE',  ( 24.57460841532290630, 5.893272594507614315, -1.425000000000085754 ) ) ;
#15352=DIRECTION ( 'NONE',  ( 0.000000000000000000, 0.000000000000000000, 1.000000000000000000 ) ) ;
#15359=FACE_OUTER_BOUND ( 'NONE', #29362, .T. ) ;
#15360=CARTESIAN_POINT ( 'NONE',  ( 53.90340377275677497, 6.895264694548083995, -1.787725782035514355 ) ) ;
#15365=CARTESIAN_POINT ( 'NONE',  ( 30.89639353666900945, 7.705332861838119385, -1.425000000000107292 ) ) ;
#15370=CARTESIAN_POINT ( 'NONE',  ( 52.28357475172138891, 3.966531851984107959, -2.045538984187684317 ) ) ;
#15372=CARTESIAN_POINT ( 'NONE',  ( 51.76665129121496989, 4.175715153428437354, -1.929612129901383977 ) ) ;
#15377=CARTESIAN_POINT ( 'NONE',  ( 47.10000000000002274, 6.982261990806648555E-14, -1.632474749424821370E-13 ) ) ;
#15378=CARTESIAN_POINT ( 'NONE',  ( 51.70000000000002416, 3.851905453475163110, 1.404572667215161053 ) ) ;
#15379=CARTESIAN_POINT ( 'NONE',  ( 51.70000000000000995, 2.478823385132571090E-14, -4.100000000000172840 ) ) ;
#15382=CARTESIAN_POINT ( 'NONE',  ( 30.31473038485998828, 6.776227631128587170, -1.550000000000105294 ) ) ;
#15398=CARTESIAN_POINT ( 'NONE',  ( 22.40865038670895260, 7.071719536792469896, 2.049999999999921663 ) ) ;
#15411=CARTESIAN_POINT ( 'NONE',  ( 51.80000000000002558, 6.475000000000062705, 2.049999999999819522 ) ) ;
#15417=DIRECTION ( 'NONE',  ( -3.489354422748178582E-15, 1.218509414717996338E-16, -1.000000000000000000 ) ) ;
#15419=CARTESIAN_POINT ( 'NONE',  ( 53.81457038914302871, 5.799118248596165870, 1.689328270749656191 ) ) ;
#15420=ORIENTED_EDGE ( 'NONE', *, *, #23358, .F. ) ;
#15421=DIRECTION ( 'NONE',  ( 0.000000000000000000, 0.000000000000000000, 1.000000000000000000 ) ) ;
#15423=DIRECTION ( 'NONE',  ( 1.000000000000000000, -0.000000000000000000, -3.491481338843133355E-15 ) ) ;
#15431=CARTESIAN_POINT ( 'NONE',  ( 54.26434950415730896, 6.004763229855418771, -2.050000000000188560 ) ) ;
#15435=CARTESIAN_POINT ( 'NONE',  ( 23.33428888190753980, 6.022557145544042534, -1.950000000000082112 ) ) ;
#15446=CARTESIAN_POINT ( 'NONE',  ( 47.27741771404776472, -3.791878011401586868, 1.561538262852513625 ) ) ;
#15451=CARTESIAN_POINT ( 'NONE',  ( 51.25569095016093257, -4.350592967663767574, 1.494824413850131428 ) ) ;
#15457=VERTEX_POINT ( 'NONE', #5458 ) ;
#15459=CARTESIAN_POINT ( 'NONE',  ( 54.28498591791677796, 6.002444397903692774, 2.049999999999814637 ) ) ;
#15465=CARTESIAN_POINT ( 'NONE',  ( 51.71858290632728483, 4.174878015463704628, 1.931423039627790494 ) ) ;
#15467=CARTESIAN_POINT ( 'NONE',  ( 51.80000000000001137, 6.475000000000062705, -2.050000000000180123 ) ) ;
#15468=CARTESIAN_POINT ( 'NONE',  ( 51.70000000000000995, -3.550773357292059007, -2.049880134336001802 ) ) ;
#15496=CARTESIAN_POINT ( 'NONE',  ( 53.91574522233626965, 6.672251602764244893, -1.774295313897662485 ) ) ;
#15502=CARTESIAN_POINT ( 'NONE',  ( 23.13157261764652972, 6.282290353147255146, 2.049999999999918110 ) ) ;
#15511=AXIS2_PLACEMENT_3D ( 'NONE', #21046, #23569, #8997 ) ;
#15512=ORIENTED_EDGE ( 'NONE', *, *, #21273, .F. ) ;
#15515=CIRCLE ( 'NONE', #5405, 160.1997717543138720 ) ;
#15528=ORIENTED_EDGE ( 'NONE', *, *, #31217, .F. ) ;
#15532=CARTESIAN_POINT ( 'NONE',  ( 54.16075265905997327, 5.605215124043997577, -2.050000000000188560 ) ) ;
#15535=DIRECTION ( 'NONE',  ( -3.489354422748178582E-15, 1.218509414717996338E-16, -1.000000000000000000 ) ) ;
#15545=ORIENTED_EDGE ( 'NONE', *, *, #2975, .F. ) ;
#15550=CARTESIAN_POINT ( 'NONE',  ( 48.00000000000001421, -4.031600731908413948, -1.173113608511841877 ) ) ;
#15551=CARTESIAN_POINT ( 'NONE',  ( 51.70000000000002416, 6.982261990806648555E-14, -1.793082891011605378E-13 ) ) ;
#15553=CARTESIAN_POINT ( 'NONE',  ( 53.82754651211528341, 4.897847608402548403, 2.049999999999811973 ) ) ;
#15554=CARTESIAN_POINT ( 'NONE',  ( 34.56702326949724835, 8.213851659285209550, -1.550000000000119948 ) ) ;
#15558=VERTEX_POINT ( 'NONE', #3227 ) ;
#15560=B_SPLINE_CURVE_WITH_KNOTS ( 'NONE', 3,
 ( #15869, #1463, #16346, #23648, #18582, #28227, #28532, #13786, #11604, #25691, #16196, #11435, #23323, #6371, #25378, #23179, #8590, #3835, #18889, #30913, #23010, #30581, #8731, #21126, #21285, #18269, #28380, #13642 ),
 .UNSPECIFIED., .F., .F.,
 ( 4, 2, 2, 2, 2, 2, 2, 2, 2, 2, 2, 2, 2, 4 ),
 ( 0.003059686050519344613, 0.004393787003443038949, 0.005060837479904890454, 0.005727887956366741959, 0.007061988909290444101, 0.007729039385752295606, 0.008396089862214146243, 0.009063140338675997748, 0.009730190815137849253, 0.01106429176806155226, 0.01239839272098525527, 0.01306544319744710331, 0.01339896843567802559, 0.01373249367390894961 ),
 .UNSPECIFIED. ) ;
#15563=CARTESIAN_POINT ( 'NONE',  ( 47.54039588126945404, -4.349885043120369055, -1.496908008647668709 ) ) ;
#15564=ORIENTED_EDGE ( 'NONE', *, *, #3960, .T. ) ;
#15573=ORIENTED_EDGE ( 'NONE', *, *, #23952, .T. ) ;
#15579=CARTESIAN_POINT ( 'NONE',  ( 34.56702326949724835, 8.213851659285209550, -1.950000000000119860 ) ) ;
#15589=CARTESIAN_POINT ( 'NONE',  ( 54.02638549814044211, 7.248122547115673164, -2.050000000000188560 ) ) ;
#15590=ORIENTED_EDGE ( 'NONE', *, *, #3581, .T. ) ;
#15596=CARTESIAN_POINT ( 'NONE',  ( 51.80000000000001137, -4.319730106884873244, -1.256953381662418101 ) ) ;
#15618=CARTESIAN_POINT ( 'NONE',  ( 47.00299618517622946, -3.613796805337473383, 1.940711795750564628 ) ) ;
#15631=CARTESIAN_POINT ( 'NONE',  ( 54.40536568400169415, 5.987876372949615167, 1.624999999999809930 ) ) ;
#15645=DIRECTION ( 'NONE',  ( -0.9993908270190956511, 0.03489949670250096919, 3.491481338843132961E-15 ) ) ;
#15647=DIRECTION ( 'NONE',  ( -3.489354422748178188E-15, 1.218509414717996091E-16, -1.000000000000000000 ) ) ;
#15652=TOROIDAL_SURFACE ( 'NONE', #1482, 159.7997717543496776, 0.1000000000000000056 ) ;
#15658=EDGE_CURVE ( 'NONE', #9993, #9597, #1469, .T. ) ;
#15664=VERTEX_POINT ( 'NONE', #13173 ) ;
#15678=CARTESIAN_POINT ( 'NONE',  ( 27.62808879389201522, 5.849836810644521989, -1.425000000000096412 ) ) ;
#15686=SHAPE_REPRESENTATION_RELATIONSHIP ( 'NONE' , 'NONE' ,  #549, #2132 ) ;
#15689=CARTESIAN_POINT ( 'NONE',  ( 53.16217804548203674, 8.131925109091699966, -2.050000000000185008 ) ) ;
#15710=CARTESIAN_POINT ( 'NONE',  ( 52.18331218360316370, 8.688678219032366812, 2.049999999999818190 ) ) ;
#15732=DIRECTION ( 'NONE',  ( -1.000000000000000000, 1.786249915856167978E-14, 3.435095992031092083E-15 ) ) ;
#15738=CARTESIAN_POINT ( 'NONE',  ( 53.74860301653917816, 7.732465014774306589, -2.050000000000187672 ) ) ;
#15753=DIRECTION ( 'NONE',  ( -1.000000000000000000, -0.000000000000000000, 3.491481338843133355E-15 ) ) ;
#15756=CARTESIAN_POINT ( 'NONE',  ( 21.97322666366011745, 8.076925076899296840, -2.050000000000075762 ) ) ;
#15765=EDGE_CURVE ( 'NONE', #15927, #16106, #1355, .T. ) ;
#15770=CARTESIAN_POINT ( 'NONE',  ( 51.06584210772579269, -4.410482998349241512, 1.311567113538989693 ) ) ;
#15776=CARTESIAN_POINT ( 'NONE',  ( 54.19008868793212486, 6.697828837789025158, -2.050000000000189004 ) ) ;
#15780=CARTESIAN_POINT ( 'NONE',  ( 51.77007169719453117, -3.673656954000176889, 1.824471899732607261 ) ) ;
#15781=EDGE_LOOP ( 'NONE', ( #17532, #8823, #25247, #12101 ) ) ;
#15782=CARTESIAN_POINT ( 'NONE',  ( 53.81176349924878366, 5.730864617276189676, 2.049999999999812417 ) ) ;
#15786=VERTEX_POINT ( 'NONE', #23955 ) ;
#15787=CARTESIAN_POINT ( 'NONE',  ( 32.54912305740081990, 8.004110617865640265, -2.050000000000113509 ) ) ;
#15793=ORIENTED_EDGE ( 'NONE', *, *, #14425, .T. ) ;
#15801=EDGE_CURVE ( 'NONE', #4799, #12883, #28672, .T. ) ;
#15804=CIRCLE ( 'NONE', #2148, 4.600000000000036948 ) ;
#15810=CARTESIAN_POINT ( 'NONE',  ( 33.97047170734846588, 8.288075094363309248, 2.049999999999882139 ) ) ;
#15812=CARTESIAN_POINT ( 'NONE',  ( 51.80000000000002558, 6.475000000000062705, 2.049999999999819522 ) ) ;
#15816=VERTEX_POINT ( 'NONE', #21600 ) ;
#15824=EDGE_CURVE ( 'NONE', #15927, #3896, #31240, .T. ) ;
#15830=CARTESIAN_POINT ( 'NONE',  ( 51.80000000000001137, 8.700000000000107647, -2.050000000000180123 ) ) ;
#15837=DIRECTION ( 'NONE',  ( -0.9993908270190958731, 0.03489949670250092062, 3.490905158897711881E-15 ) ) ;
#15839=CARTESIAN_POINT ( 'NONE',  ( 53.74977035838708161, 4.800378271572134814, -2.050000000000184119 ) ) ;
#15846=FACE_OUTER_BOUND ( 'NONE', #29396, .T. ) ;
#15849=CARTESIAN_POINT ( 'NONE',  ( 53.94065574304038080, 7.474792160838902966, 2.049999999999810196 ) ) ;
#15850=CARTESIAN_POINT ( 'NONE',  ( 48.00000000000001421, -4.319730106884873244, -1.256953381662404778 ) ) ;
#15862=ORIENTED_EDGE ( 'NONE', *, *, #29771, .T. ) ;
#15869=CARTESIAN_POINT ( 'NONE',  ( 31.59287277085155665, 7.495449159457250765, -1.425000000000109956 ) ) ;
#15877=CARTESIAN_POINT ( 'NONE',  ( 54.12540754135503107, 6.691802926424371023, 2.049999999999799538 ) ) ;
#15882=LINE ( 'NONE', #16054, #24220 ) ;
#15887=ORIENTED_EDGE ( 'NONE', *, *, #22419, .T. ) ;
#15889=CARTESIAN_POINT ( 'NONE',  ( 51.68179902492697408, -4.249104741287451859, -1.767319601065211909 ) ) ;
#15904=CARTESIAN_POINT ( 'NONE',  ( 51.87416143049283335, 8.598705507415685290, -1.950000000000180256 ) ) ;
#15906=EDGE_CURVE ( 'NONE', #11471, #10732, #20594, .T. ) ;
#15909=CARTESIAN_POINT ( 'NONE',  ( 50.87477060347374902, 8.633605004118187765, 1.949999999999822320 ) ) ;
#15911=CARTESIAN_POINT ( 'NONE',  ( 51.58853050958410336, -4.227727696248162026, 1.816297733665127812 ) ) ;
#15919=CARTESIAN_POINT ( 'NONE',  ( 51.80000000000003268, -3.700421601131613780, 1.984561589293431405 ) ) ;
#15921=CARTESIAN_POINT ( 'NONE',  ( 51.80000000000002558, 8.700707106781294442, 2.049999999999819522 ) ) ;
#15927=VERTEX_POINT ( 'NONE', #22685 ) ;
#15928=CARTESIAN_POINT ( 'NONE',  ( 26.61278927081361090, 5.319531372976052275, -2.050000000000092637 ) ) ;
#15965=VECTOR ( 'NONE', #21905, 1000.000000000000114 ) ;
#15977=VECTOR ( 'NONE', #13288, 1000.000000000000000 ) ;
#15978=CARTESIAN_POINT ( 'NONE',  ( 53.73313642785004873, 5.556167542617246546, -1.667742524038318352 ) ) ;
#15980=CARTESIAN_POINT ( 'NONE',  ( 25.68808851933979298, 5.234409799644741845, 1.949999999999910916 ) ) ;
#15981=ORIENTED_EDGE ( 'NONE', *, *, #22449, .T. ) ;
#15996=AXIS2_PLACEMENT_3D ( 'NONE', #19142, #16756, #12151 ) ;
#15997=LINE ( 'NONE', #26132, #26127 ) ;
#15999=ORIENTED_EDGE ( 'NONE', *, *, #2830, .F. ) ;
#16005=CARTESIAN_POINT ( 'NONE',  ( 51.80000000000001137, 4.350000000000017408, -2.050000000000180123 ) ) ;
#16008=CARTESIAN_POINT ( 'NONE',  ( 51.87765138016309407, 8.698644590117595499, 2.049999999999819522 ) ) ;
#16016=EDGE_CURVE ( 'NONE', #19416, #26766, #4232, .T. ) ;
#16018=DIRECTION ( 'NONE',  ( 3.016910393003118404E-15, 0.000000000000000000, 1.000000000000000000 ) ) ;
#16028=EDGE_LOOP ( 'NONE', ( #14272, #17376, #20407, #30106 ) ) ;
#16039=DIRECTION ( 'NONE',  ( 3.016910393003118404E-15, 0.000000000000000000, 1.000000000000000000 ) ) ;
#16041=EDGE_CURVE ( 'NONE', #22264, #23376, #29165, .T. ) ;
#16053=FACE_OUTER_BOUND ( 'NONE', #26318, .T. ) ;
#16054=CARTESIAN_POINT ( 'NONE',  ( 51.89161117884420094, 9.098400920928357394, 1.949999999999818767 ) ) ;
#16059=CIRCLE ( 'NONE', #9506, 0.09999999999999933942 ) ;
#16061=FACE_OUTER_BOUND ( 'NONE', #28521, .T. ) ;
#16070=CARTESIAN_POINT ( 'NONE',  ( 24.17629218420043102, 5.599093920765165322, -1.950000000000019273 ) ) ;
#16078=LINE ( 'NONE', #30620, #11203 ) ;
#16083=DIRECTION ( 'NONE',  ( 0.000000000000000000, 0.000000000000000000, 1.000000000000000000 ) ) ;
#16087=CARTESIAN_POINT ( 'NONE',  ( 51.77958208625742031, -4.146195171498040288, 1.996297985640307360 ) ) ;
#16101=ORIENTED_EDGE ( 'NONE', *, *, #24967, .T. ) ;
#16102=CARTESIAN_POINT ( 'NONE',  ( 53.25573957143296155, 8.250120694359615925, 2.049999999999814193 ) ) ;
#16106=VERTEX_POINT ( 'NONE', #7730 ) ;
#16108=CARTESIAN_POINT ( 'NONE',  ( 23.93173257309099000, 5.810883422836172763, -2.050000000000082423 ) ) ;
#16114=CARTESIAN_POINT ( 'NONE',  ( 51.87673771347595419, 8.672480599449029270, -2.050000000000180567 ) ) ;
#16126=EDGE_CURVE ( 'NONE', #2006, #320, #8357, .T. ) ;
#16148=CARTESIAN_POINT ( 'NONE',  ( 52.98660665890137267, 4.708212704504920687, -1.586977526147875350 ) ) ;
#16149=CARTESIAN_POINT ( 'NONE',  ( 47.00000000000002842, -3.933368109459640660, 2.186004417993010485 ) ) ;
#16156=DIRECTION ( 'NONE',  ( -1.000000000000000000, -0.000000000000000000, 3.491481338843133355E-15 ) ) ;
#16161=CARTESIAN_POINT ( 'NONE',  ( 31.59287277085072532, 7.495449159458786426, 1.424999999999890132 ) ) ;
#16164=CARTESIAN_POINT ( 'NONE',  ( 48.00000000000001421, -4.319730106884872356, -1.256953381662404556 ) ) ;
#16175=ORIENTED_EDGE ( 'NONE', *, *, #21915, .F. ) ;
#16177=DIRECTION ( 'NONE',  ( -1.000000000000000000, -0.000000000000000000, 3.491481338843133355E-15 ) ) ;
#16181=ORIENTED_EDGE ( 'NONE', *, *, #3039, .T. ) ;
#16196=CARTESIAN_POINT ( 'NONE',  ( 27.56628230087644127, 5.372092466067858396, -1.425000000000095746 ) ) ;
#16210=VERTEX_POINT ( 'NONE', #31270 ) ;
#16211=CARTESIAN_POINT ( 'NONE',  ( 54.11179973533069898, 5.509196088239827205, 2.049999999999811084 ) ) ;
#16213=B_SPLINE_CURVE_WITH_KNOTS ( 'NONE', 3,
 ( #18240, #15839, #22979, #27877, #1265, #8558, #980, #20458, #13444, #23147, #13605, #8702, #27408, #13000, #18386, #5720, #15370, #25019, #3349, #11725, #4269 ),
 .UNSPECIFIED., .F., .F.,
 ( 4, 2, 2, 1, 2, 2, 2, 1, 1, 2, 2, 4 ),
 ( 0.000000000000000000, 0.4999999998174028959, 0.5312499998059895256, 0.5624999997945763219, 0.6249999997717561318, 0.7499999997261151963, 0.7578124997232579263, 0.7656249997204006563, 0.7812499997146973296, 0.8124999997032911203, 0.8749999996804787017, 0.9999999996348539755 ),
 .UNSPECIFIED. ) ;
#16214=FACE_OUTER_BOUND ( 'NONE', #30103, .T. ) ;
#16215=AXIS2_PLACEMENT_3D ( 'NONE', #16936, #7126, #7433 ) ;
#16230=FACE_OUTER_BOUND ( 'NONE', #402, .T. ) ;
#16236=DIRECTION ( 'NONE',  ( -1.000000000000000000, 0.000000000000000000, 3.491481338843133355E-15 ) ) ;
#16242=CARTESIAN_POINT ( 'NONE',  ( 53.85185227134009978, 5.786610019663855020, -1.878038514704438500 ) ) ;
#16252=CARTESIAN_POINT ( 'NONE',  ( 51.30406804459317271, -3.900599430603180817, 1.266782962024575410 ) ) ;
#16254=CARTESIAN_POINT ( 'NONE',  ( 53.90177594311671072, 7.547472342232321552, 2.049999999999811973 ) ) ;
#16259=EDGE_LOOP ( 'NONE', ( #1034, #20704, #19742, #10177 ) ) ;
#16260=CARTESIAN_POINT ( 'NONE',  ( 31.59287277085155665, 7.495449159457250765, -1.425000000000109956 ) ) ;
#16301=CARTESIAN_POINT ( 'NONE',  ( 51.60138551324653378, -4.191665075176590705, -1.623492990431073979 ) ) ;
#16302=CARTESIAN_POINT ( 'NONE',  ( 51.80000000000001137, -3.933368109459640660, -2.186004417993355542 ) ) ;
#16303=ORIENTED_EDGE ( 'NONE', *, *, #25693, .F. ) ;
#16307=ADVANCED_FACE ( 'NONE', ( #21164 ), #16554, .T. ) ;
#16321=DIRECTION ( 'NONE',  ( -1.000000000000000000, -0.000000000000000000, 3.491481338843133355E-15 ) ) ;
#16342=ORIENTED_EDGE ( 'NONE', *, *, #24969, .F. ) ;
#16346=CARTESIAN_POINT ( 'NONE',  ( 30.78427835929706902, 7.077770142316450297, -1.425000000000106626 ) ) ;
#16376=CARTESIAN_POINT ( 'NONE',  ( 54.12540754135502397, 6.691802926424378128, -2.050000000000183675 ) ) ;
#16403=ADVANCED_FACE ( 'NONE', ( #7662 ), #7592, .T. ) ;
#16404=CARTESIAN_POINT ( 'NONE',  ( 53.71283936284426375, 7.813984279442741432, 2.049999999999812417 ) ) ;
#16417=CARTESIAN_POINT ( 'NONE',  ( 53.38804190906846259, 7.887047813379708394, 1.884060075242533161 ) ) ;
#16420=CARTESIAN_POINT ( 'NONE',  ( 47.87910813548244704, -4.387164041431067751, 1.383037119376591351 ) ) ;
#16436=ADVANCED_FACE ( 'NONE', ( #22589 ), #21766, .T. ) ;
#16442=CARTESIAN_POINT ( 'NONE',  ( 51.80000000000001137, 6.475000000000062705, -2.050000000000180123 ) ) ;
#16444=EDGE_LOOP ( 'NONE', ( #25113, #25468, #19062, #6872, #8759, #22993, #20285, #10883 ) ) ;
#16445=VERTEX_POINT ( 'NONE', #1046 ) ;
#16447=CARTESIAN_POINT ( 'NONE',  ( 41.48619405471883681, -151.3359592902621955, -2.050000000000163691 ) ) ;
#16452=LINE ( 'NONE', #26109, #25656 ) ;
#16458=ORIENTED_EDGE ( 'NONE', *, *, #23887, .F. ) ;
#16461=( BOUNDED_CURVE ( )  B_SPLINE_CURVE ( 3, ( #15298, #24944, #25745, #13694 ),
 .UNSPECIFIED., .F., .T. ) 
 B_SPLINE_CURVE_WITH_KNOTS ( ( 4, 4 ),
 ( 1.570796326794897890, 3.141592653589794448 ),
 .UNSPECIFIED. ) 
 CURVE ( )  GEOMETRIC_REPRESENTATION_ITEM ( )  RATIONAL_B_SPLINE_CURVE ( ( 1.000000000000000000, 0.8047378541243649375, 0.8047378541243649375, 1.000000000000000000 ) ) 
 REPRESENTATION_ITEM ( '' )  );
#16471=CARTESIAN_POINT ( 'NONE',  ( 47.11804492410362144, -4.249103233463815243, -1.767380283559819576 ) ) ;
#16515=CARTESIAN_POINT ( 'NONE',  ( 51.70000000000000995, 4.174380580618773706, -1.932497546739578631 ) ) ;
#16516=DIRECTION ( 'NONE',  ( 3.384826294588897856E-15, 0.000000000000000000, 1.000000000000000000 ) ) ;
#16519=EDGE_CURVE ( 'NONE', #28370, #4182, #13904, .T. ) ;
#16523=CARTESIAN_POINT ( 'NONE',  ( 53.74845224966695412, 7.732683774216504879, 2.049999999999811973 ) ) ;
#16527=CARTESIAN_POINT ( 'NONE',  ( 54.36194317780777396, 6.362460706117157194, -2.050000000000189004 ) ) ;
#16532=ORIENTED_EDGE ( 'NONE', *, *, #26426, .T. ) ;
#16533=CARTESIAN_POINT ( 'NONE',  ( 22.72662675107780927, 7.272876594663812533, -1.425000000000078870 ) ) ;
#16534=CARTESIAN_POINT ( 'NONE',  ( 30.08242191457677706, 7.215531071606934965, 1.424999999999895239 ) ) ;
#16537=AXIS2_PLACEMENT_3D ( 'NONE', #2580, #12228, #16516 ) ;
#16539=CARTESIAN_POINT ( 'NONE',  ( 51.80000000000000426, 2.478823385132571090E-14, -4.100000000000173728 ) ) ;
#16541=AXIS2_PLACEMENT_3D ( 'NONE', #16795, #22323, #9674 ) ;
#16550=CARTESIAN_POINT ( 'NONE',  ( 31.90749320720292559, 7.645246318246651462, 2.049999999999888356 ) ) ;
#16554=CYLINDRICAL_SURFACE ( 'NONE', #11416, 0.09999999999999972800 ) ;
#16556=ORIENTED_EDGE ( 'NONE', *, *, #14820, .F. ) ;
#16571=AXIS2_PLACEMENT_3D ( 'NONE', #22434, #22600, #10235 ) ;
#16573=ORIENTED_EDGE ( 'NONE', *, *, #23952, .F. ) ;
#16576=CARTESIAN_POINT ( 'NONE',  ( 31.35411506839069062, 7.935106539330317510, -1.425000000000109068 ) ) ;
#16578=CARTESIAN_POINT ( 'NONE',  ( 53.66827364943468126, 4.678978782231800082, 2.049999999999812861 ) ) ;
#16580=CARTESIAN_POINT ( 'NONE',  ( 50.87477060347373481, 8.633605004118185988, -2.008578643762867433 ) ) ;
#16595=CARTESIAN_POINT ( 'NONE',  ( 53.61178743402152946, 7.592121589695717709, 1.856625336930636250 ) ) ;
#16602=CARTESIAN_POINT ( 'NONE',  ( 24.05318950685000701, 5.396204383593524057, 1.549999999999915890 ) ) ;
#16611=DIRECTION ( 'NONE',  ( 3.489354422748178582E-15, -1.218509414717996338E-16, 1.000000000000000000 ) ) ;
#16612=CARTESIAN_POINT ( 'NONE',  ( 52.69133855403836009, 4.542743498088711362, 1.570391066185332196 ) ) ;
#16624=LINE ( 'NONE', #26268, #27795 ) ;
#16638=B_SPLINE_CURVE_WITH_KNOTS ( 'NONE', 3,
 ( #26943, #17000, #17449, #2729, #24729, #29465, #19835, #29017, #22221, #9718 ),
 .UNSPECIFIED., .F., .F.,
 ( 4, 2, 2, 2, 4 ),
 ( 0.000000000000000000, 0.0001518620921315108662, 0.0002277931381972662993, 0.0002657586612301437176, 0.0003037241842630211902 ),
 .UNSPECIFIED. ) ;
#16654=ORIENTED_EDGE ( 'NONE', *, *, #541, .F. ) ;
#16657=CARTESIAN_POINT ( 'NONE',  ( 51.80000000000001847, 2.428612866367529932E-14, -1.808587333520743709E-13 ) ) ;
#16665=PLANE ( 'NONE',  #20607 ) ;
#16683=CYLINDRICAL_SURFACE ( 'NONE', #30705, 4.600000000000036948 ) ;
#16686=DIRECTION ( 'NONE',  ( 1.000000000000000000, 0.000000000000000000, -3.491481338843133355E-15 ) ) ;
#16688=DIRECTION ( 'NONE',  ( -3.489354422748178582E-15, 1.218509414717996338E-16, -1.000000000000000000 ) ) ;
#16695=CARTESIAN_POINT ( 'NONE',  ( 54.18857836506865056, 5.673639474816032369, -2.050000000000188116 ) ) ;
#16696=CARTESIAN_POINT ( 'NONE',  ( 51.70000000000000284, -3.609862487194767766, -1.947526779791158624 ) ) ;
#16697=AXIS2_PLACEMENT_3D ( 'NONE', #29910, #27857, #6168 ) ;
#16701=CARTESIAN_POINT ( 'NONE',  ( 22.58314801556725371, 7.622751244490532763, 1.424999999999921663 ) ) ;
#16708=CARTESIAN_POINT ( 'NONE',  ( 52.08333333333335702, 4.368973594129894167, 1.439468559502539824 ) ) ;
#16710=ORIENTED_EDGE ( 'NONE', *, *, #1829, .T. ) ;
#16720=VERTEX_POINT ( 'NONE', #3068 ) ;
#16725=CARTESIAN_POINT ( 'NONE',  ( 47.09453520915243985, 9.265918505097243241, 1.949999999999835865 ) ) ;
#16735=CARTESIAN_POINT ( 'NONE',  ( 53.25639650609797116, 8.250950595073881288, 2.049999999999814193 ) ) ;
#16737=CARTESIAN_POINT ( 'NONE',  ( 50.85906935218976344, 8.675599908283860628, -2.050000000000176570 ) ) ;
#16738=CARTESIAN_POINT ( 'NONE',  ( 31.17557021199490919, 8.263885728205480063, -1.575000000000108535 ) ) ;
#16743=DIRECTION ( 'NONE',  ( 9.754918421198724481E-16, -0.9601771338024399638, 0.2793919678926571892 ) ) ;
#16756=DIRECTION ( 'NONE',  ( -1.000000000000000000, -0.000000000000000000, 3.491481338843133355E-15 ) ) ;
#16757=DIRECTION ( 'NONE',  ( -3.489354422748178977E-15, 1.218509414717996338E-16, -1.000000000000000000 ) ) ;
#16763=CARTESIAN_POINT ( 'NONE',  ( 22.07280086217094350, 8.086143481909241260, 1.949999999999922906 ) ) ;
#16764=CARTESIAN_POINT ( 'NONE',  ( 53.44675224545779457, 5.128498479132437282, 1.627483882363299772 ) ) ;
#16765=CARTESIAN_POINT ( 'NONE',  ( 53.93368094605000351, 6.673923850743078034, 1.889910665294559422 ) ) ;
#16772=ADVANCED_FACE ( 'NONE', ( #24599 ), #22249, .T. ) ;
#16774=CARTESIAN_POINT ( 'NONE',  ( 50.87477060347373481, 8.633605004118187765, -1.950000000000176925 ) ) ;
#16793=DIRECTION ( 'NONE',  ( 1.000000000000000000, 0.000000000000000000, -3.469446951953611033E-15 ) ) ;
#16794=CARTESIAN_POINT ( 'NONE',  ( 22.37589498084251716, 6.912581374120083666, -1.950000000000077893 ) ) ;
#16795=CARTESIAN_POINT ( 'NONE',  ( 51.70000000000003126, -3.933368109459640660, 2.186004417992994497 ) ) ;
#16800=CIRCLE ( 'NONE', #26398, 0.1000000000000000472 ) ;
#16801=CARTESIAN_POINT ( 'NONE',  ( 47.38185894056287140, -4.256263374916362530, -1.450017276182623105 ) ) ;
#16807=UNCERTAINTY_MEASURE_WITH_UNIT (LENGTH_MEASURE( 1.000000000000000082E-05 ), #12517, 'distance_accuracy_value', 'NONE');
#16831=CARTESIAN_POINT ( 'NONE',  ( 54.23463818034553441, 5.946682447858800735, -2.050000000000189004 ) ) ;
#16832=CARTESIAN_POINT ( 'NONE',  ( 51.70000000000000995, -3.933368109459640660, -2.186004417993355098 ) ) ;
#16849=ORIENTED_EDGE ( 'NONE', *, *, #10977, .F. ) ;
#16852=ORIENTED_EDGE ( 'NONE', *, *, #13741, .T. ) ;
#16857=VERTEX_POINT ( 'NONE', #15579 ) ;
#16859=ORIENTED_EDGE ( 'NONE', *, *, #30332, .T. ) ;
#16862=ORIENTED_EDGE ( 'NONE', *, *, #29660, .T. ) ;
#16865=CARTESIAN_POINT ( 'NONE',  ( 32.27289361194385720, 7.909974131750026061, 2.049999999999887468 ) ) ;
#16876=CARTESIAN_POINT ( 'NONE',  ( 53.74478519188839698, 7.379842749953417602, 2.049999999999939426 ) ) ;
#16878=EDGE_LOOP ( 'NONE', ( #28698, #9265, #16532, #29374 ) ) ;
#16889=ORIENTED_EDGE ( 'NONE', *, *, #14247, .F. ) ;
#16892=CARTESIAN_POINT ( 'NONE',  ( 33.05069135236685440, 8.148093138862860130, 1.949999999999884270 ) ) ;
#16907=CARTESIAN_POINT ( 'NONE',  ( 54.28867365409861634, 5.640057820322912363, 1.949999999999809885 ) ) ;
#16910=CARTESIAN_POINT ( 'NONE',  ( 53.81457038914302871, 5.799118248596165870, 1.689328270749656191 ) ) ;
#16911=CARTESIAN_POINT ( 'NONE',  ( 53.91582462592153746, 6.672259099522125148, 1.484311102127795712 ) ) ;
#16921=CARTESIAN_POINT ( 'NONE',  ( 47.54826167791131297, -3.873874536552758041, -1.343508358799555991 ) ) ;
#16936=CARTESIAN_POINT ( 'NONE',  ( 51.80000000000001137, 6.475000000000062705, -2.050000000000180123 ) ) ;
#16938=VECTOR ( 'NONE', #1960, 1000.000000000000000 ) ;
#16943=DIRECTION ( 'NONE',  ( -3.051840300662039141E-15, -0.4857787595540328796, -0.8740818021021516948 ) ) ;
#16945=CARTESIAN_POINT ( 'NONE',  ( 33.37799870938437863, 8.120802762572234101, -1.950000000000116529 ) ) ;
#16967=CARTESIAN_POINT ( 'NONE',  ( 47.19861448675352023, -4.191665075176588928, 1.623492990430730032 ) ) ;
#16968=VECTOR ( 'NONE', #2598, 1000.000000000000000 ) ;
#16972=ORIENTED_EDGE ( 'NONE', *, *, #19931, .F. ) ;
#16981=CARTESIAN_POINT ( 'NONE',  ( 54.23473434925103476, 6.620089622897159742, -2.050000000000189004 ) ) ;
#16986=DIRECTION ( 'NONE',  ( -0.1208805777273843918, 0.9926670569371656150, 0.000000000000000000 ) ) ;
#17000=CARTESIAN_POINT ( 'NONE',  ( 51.80000000000003268, 3.850000000000017408, 1.627168804780626088 ) ) ;
#17003=CARTESIAN_POINT ( 'NONE',  ( 47.76318363328993399, -4.380055612571977619, 1.406160842577559800 ) ) ;
#17014=ORIENTED_EDGE ( 'NONE', *, *, #1526, .F. ) ;
#17025=CIRCLE ( 'NONE', #5887, 4.199999999999993072 ) ;
#17026=DIRECTION ( 'NONE',  ( -0.9993908270190957621, 0.03489949670250097613, 3.491481338843133355E-15 ) ) ;
#17042=CARTESIAN_POINT ( 'NONE',  ( 53.94440344817343913, 6.524635634306410914, 1.761196874214440378 ) ) ;
#17057=CARTESIAN_POINT ( 'NONE',  ( 22.79310476198749313, 6.591203646873187161, -2.050000000000079758 ) ) ;
#17068=CARTESIAN_POINT ( 'NONE',  ( 51.87416143049281914, 8.598705507415685290, -2.050000000000179678 ) ) ;
#17073=CARTESIAN_POINT ( 'NONE',  ( 27.27214205000343483, 5.011961650406415281, 1.549999999999904565 ) ) ;
#17091=CARTESIAN_POINT ( 'NONE',  ( 48.00000000000001421, -3.908336260473453727, -1.238913909466087482 ) ) ;
#17097=CARTESIAN_POINT ( 'NONE',  ( 47.09104525948218622, 9.165979422395331255, 1.949999999999836087 ) ) ;
#17098=CARTESIAN_POINT ( 'NONE',  ( 47.09453520915242564, 9.265918505097243241, -1.950000000000163380 ) ) ;
#17113=CARTESIAN_POINT ( 'NONE',  ( 27.42782126191618630, 5.342778649435317995, -1.950000000000095213 ) ) ;
#17116=CARTESIAN_POINT ( 'NONE',  ( 54.19386703870442545, 5.671865141453449333, -1.950000000000188694 ) ) ;
#17119=ORIENTED_EDGE ( 'NONE', *, *, #26122, .F. ) ;
#17125=DIRECTION ( 'NONE',  ( 0.000000000000000000, -0.2793919678926574668, -0.9601771338024398528 ) ) ;
#17128=ORIENTED_EDGE ( 'NONE', *, *, #3960, .F. ) ;
#17144=CARTESIAN_POINT ( 'NONE',  ( 48.00000000000002132, -3.936726248589973221, 1.145507068359725933 ) ) ;
#17148=CARTESIAN_POINT ( 'NONE',  ( 54.19030381964616083, 6.697848500921247172, -2.050000000000189004 ) ) ;
#17154=ORIENTED_EDGE ( 'NONE', *, *, #18349, .F. ) ;
#17157=CARTESIAN_POINT ( 'NONE',  ( 47.86735231835938009, -4.319730106884873244, -1.256953381662404334 ) ) ;
#17161=ORIENTED_EDGE ( 'NONE', *, *, #11359, .T. ) ;
#17162=PLANE ( 'NONE',  #11949 ) ;
#17177=CARTESIAN_POINT ( 'NONE',  ( 31.77414890219473165, 7.582826004857921909, 1.949999999999889377 ) ) ;
#17182=CARTESIAN_POINT ( 'NONE',  ( 51.87770073550463223, 8.700057942179277859, -2.050000000000180123 ) ) ;
#17195=VERTEX_POINT ( 'NONE', #24264 ) ;
#17200=FACE_OUTER_BOUND ( 'NONE', #12370, .T. ) ;
#17202=EDGE_CURVE ( 'NONE', #13278, #27612, #12221, .T. ) ;
#17206=DIRECTION ( 'NONE',  ( 3.384826294588897856E-15, 0.000000000000000000, 1.000000000000000000 ) ) ;
#17208=CARTESIAN_POINT ( 'NONE',  ( 27.84544208433268153, 5.444976785341570924, -2.050000000000357314 ) ) ;
#17213=CARTESIAN_POINT ( 'NONE',  ( 47.10000000000002274, 6.982261990806648555E-14, -1.632474749424821370E-13 ) ) ;
#17216=CARTESIAN_POINT ( 'NONE',  ( 51.39453088482484588, 4.389042235173731044, -2.050000000000179234 ) ) ;
#17226=CARTESIAN_POINT ( 'NONE',  ( 53.94287869493206244, 6.382073928939168361, 1.484311102127795490 ) ) ;
#17234=ORIENTED_EDGE ( 'NONE', *, *, #10790, .T. ) ;
#17240=CARTESIAN_POINT ( 'NONE',  ( 52.42875048912549119, 4.000253242763575301, 2.045760939463020733 ) ) ;
#17253=CARTESIAN_POINT ( 'NONE',  ( 23.81491379129848696, 5.755424080683373411, -1.950000000000082556 ) ) ;
#17254=DIRECTION ( 'NONE',  ( 0.000000000000000000, 0.000000000000000000, -1.000000000000000000 ) ) ;
#17258=CARTESIAN_POINT ( 'NONE',  ( 24.79176202108332205, 5.385922622694288897, 1.424999999999913669 ) ) ;
#17276=LINE ( 'NONE', #17422, #8136 ) ;
#17284=CARTESIAN_POINT ( 'NONE',  ( 52.10591853744707436, 8.701414215152928122, -2.050000000000181455 ) ) ;
#17301=DIRECTION ( 'NONE',  ( -0.9993908270190956511, 0.03489949670250096919, 3.491481338843132961E-15 ) ) ;
#17302=CARTESIAN_POINT ( 'NONE',  ( 47.73687070013482270, -4.312041630646834989, 1.282098934412685187 ) ) ;
#17304=DIRECTION ( 'NONE',  ( -1.000000000000000000, 0.000000000000000000, 3.491481338843133355E-15 ) ) ;
#17312=ORIENTED_EDGE ( 'NONE', *, *, #28787, .F. ) ;
#17318=CARTESIAN_POINT ( 'NONE',  ( 23.38809389355778023, 6.107120497888718802, 2.049999999999917222 ) ) ;
#17320=EDGE_CURVE ( 'NONE', #20124, #10732, #23060, .T. ) ;
#17341=DIRECTION ( 'NONE',  ( 0.03489949670250203084, 0.9993908270190957621, -3.673133589935336920E-30 ) ) ;
#17342=ADVANCED_FACE ( 'NONE', ( #18857 ), #31024, .F. ) ;
#17345=CARTESIAN_POINT ( 'NONE',  ( 54.02156746059516479, 6.375683097465850935, -1.975347834873397490 ) ) ;
#17349=CARTESIAN_POINT ( 'NONE',  ( 30.23587923389752419, 6.713699166094404092, -1.950000000000105871 ) ) ;
#17355=CARTESIAN_POINT ( 'NONE',  ( 51.68129744678915927, 4.333300462208747206, -1.550000000000180123 ) ) ;
#17366=CARTESIAN_POINT ( 'NONE',  ( 54.20407287615058323, 5.668441115105648187, 2.049999999999810196 ) ) ;
#17374=CARTESIAN_POINT ( 'NONE',  ( 47.09999999999999432, -3.609867133138429995, -1.947518732153282306 ) ) ;
#17376=ORIENTED_EDGE ( 'NONE', *, *, #25693, .T. ) ;
#17382=DIRECTION ( 'NONE',  ( -0.9993908270190956511, 0.03489949670250202390, 3.491481338843132961E-15 ) ) ;
#17396=EDGE_CURVE ( 'NONE', #14732, #125, #30632, .T. ) ;
#17413=CYLINDRICAL_SURFACE ( 'NONE', #11517, 0.09999999999999886757 ) ;
#17420=CARTESIAN_POINT ( 'NONE',  ( 54.19048439011715601, 6.697865729247673983, 2.049999999999811084 ) ) ;
#17422=CARTESIAN_POINT ( 'NONE',  ( 51.80000000000002558, -3.908336260473453727, 1.238913909465738872 ) ) ;
#17433=EDGE_CURVE ( 'NONE', #363, #30852, #30111, .T. ) ;
#17439=EDGE_CURVE ( 'NONE', #17195, #16857, #25380, .T. ) ;
#17449=CARTESIAN_POINT ( 'NONE',  ( 51.79433046211416070, 3.849974775422116746, 1.576777095043395471 ) ) ;
#17451=FACE_OUTER_BOUND ( 'NONE', #29014, .T. ) ;
#17452=CARTESIAN_POINT ( 'NONE',  ( 47.27826922991183523, -4.267091652301661320, 1.720255306494459235 ) ) ;
#17454=LINE ( 'NONE', #15235, #13955 ) ;
#17463=CARTESIAN_POINT ( 'NONE',  ( 31.71120695424772151, 7.553129896932145648, 1.949999999999888045 ) ) ;
#17471=CARTESIAN_POINT ( 'NONE',  ( 22.41225425035782237, 6.886225699534909594, 1.949999999999887823 ) ) ;
#17475=CARTESIAN_POINT ( 'NONE',  ( 51.29777716379115304, 3.891287491069770788, -2.050000000000178790 ) ) ;
#17488=DIRECTION ( 'NONE',  ( -0.7313537016191670181, -0.6819983600625022513, 2.468850131082252327E-15 ) ) ;
#17494=ORIENTED_EDGE ( 'NONE', *, *, #1526, .T. ) ;
#17495=ADVANCED_FACE ( 'NONE', ( #901 ), #10555, .T. ) ;
#17503=CARTESIAN_POINT ( 'NONE',  ( 51.41755241844363411, -4.256411467774983137, -1.449592950258013380 ) ) ;
#17509=CARTESIAN_POINT ( 'NONE',  ( 29.99460040655550941, 6.535150012678215603, -1.950000000000102984 ) ) ;
#17516=CARTESIAN_POINT ( 'NONE',  ( 52.02275531408256626, 3.834498708141866885, -2.050000000000181455 ) ) ;
#17518=EDGE_CURVE ( 'NONE', #26028, #14388, #9809, .T. ) ;
#17532=ORIENTED_EDGE ( 'NONE', *, *, #14395, .F. ) ;
#17535=CARTESIAN_POINT ( 'NONE',  ( 54.41366571437521316, 6.718673005292165712, 1.624999999999810374 ) ) ;
#17544=VERTEX_POINT ( 'NONE', #4731 ) ;
#17549=CARTESIAN_POINT ( 'NONE',  ( 52.92035180444707976, 4.185175181814600798, 2.047053903428833976 ) ) ;
#17567=AXIS2_PLACEMENT_3D ( 'NONE', #13419, #20602, #3636 ) ;
#17569=AXIS2_PLACEMENT_3D ( 'NONE', #16442, #23577, #9653 ) ;
#17571=AXIS2_PLACEMENT_3D ( 'NONE', #15551, #11100, #5893 ) ;
#17575=CARTESIAN_POINT ( 'NONE',  ( 24.78376069717984009, 5.502839434325734302, 2.049999999999912781 ) ) ;
#17590=DIRECTION ( 'NONE',  ( -0.9956821769042237813, -0.09282781153978682254, 3.493224332854920750E-15 ) ) ;
#17605=CARTESIAN_POINT ( 'NONE',  ( 51.60173421008559558, -3.901954665936026245, 1.539656138810567398 ) ) ;
#17607=CARTESIAN_POINT ( 'NONE',  ( 22.54717926605044198, 7.740376438784147162, -1.425000000000078204 ) ) ;
#17621=ORIENTED_EDGE ( 'NONE', *, *, #5129, .T. ) ;
#17623=CARTESIAN_POINT ( 'NONE',  ( 54.19386703870442545, 5.671865141453449333, -2.050000000000189004 ) ) ;
#17629=ADVANCED_FACE ( 'NONE', ( #6427 ), #29574, .T. ) ;
#17635=ORIENTED_EDGE ( 'NONE', *, *, #28366, .F. ) ;
#17640=CARTESIAN_POINT ( 'NONE',  ( 22.72181155690791954, 6.520914527883612699, 2.050000000000084199 ) ) ;
#17642=VECTOR ( 'NONE', #5439, 999.9999999999998863 ) ;
#17643=CARTESIAN_POINT ( 'NONE',  ( 50.87477060347373481, 8.633605004118187765, -1.550000000000176792 ) ) ;
#17645=CARTESIAN_POINT ( 'NONE',  ( 53.94065574304036659, 7.474792160838903854, -2.050000000000186784 ) ) ;
#17656=CARTESIAN_POINT ( 'NONE',  ( 54.19030381964616083, 6.697848500921247172, -2.050000000000189004 ) ) ;
#17671=CARTESIAN_POINT ( 'NONE',  ( 51.79423677987253427, 3.849974365564825529, -1.576055568942727358 ) ) ;
#17673=CARTESIAN_POINT ( 'NONE',  ( 25.68808851933666304, 5.234409799645237449, -1.950000000000088107 ) ) ;
#17677=B_SPLINE_CURVE_WITH_KNOTS ( 'NONE', 3,
 ( #15550, #20926, #18556, #25202, #10784, #20467, #18094, #8710, #18394, #28029 ),
 .UNSPECIFIED., .F., .F.,
 ( 4, 2, 2, 2, 4 ),
 ( 0.000000000000000000, 0.0003925703575136120483, 0.0007851407150272240966, 0.001177711072540836091, 0.001570281430054448193 ),
 .UNSPECIFIED. ) ;
#17682=CARTESIAN_POINT ( 'NONE',  ( 53.91678946233204783, 6.821600947619695710, -2.050000000000123723 ) ) ;
#17684=CARTESIAN_POINT ( 'NONE',  ( 47.12365020756617895, -3.859233156638960160, -1.644927388241157473 ) ) ;
#17693=CARTESIAN_POINT ( 'NONE',  ( 51.70000000000002416, 3.851905453475163110, 1.404572667215161053 ) ) ;
#17695=CARTESIAN_POINT ( 'NONE',  ( 54.28867365409860923, 5.640057820322912363, 1.624999999999810152 ) ) ;
#17698=ORIENTED_EDGE ( 'NONE', *, *, #5546, .T. ) ;
#17703=CARTESIAN_POINT ( 'NONE',  ( 51.80000000000001137, -3.637377585518695611, -2.099877210783217762 ) ) ;
#17707=AXIS2_PLACEMENT_3D ( 'NONE', #2666, #12303, #25434 ) ;
#17711=VERTEX_POINT ( 'NONE', #2292 ) ;
#17712=CARTESIAN_POINT ( 'NONE',  ( 52.43776296160012862, 4.002620649804632613, 2.045778211737469210 ) ) ;
#17715=VERTEX_POINT ( 'NONE', #16725 ) ;
#17740=CARTESIAN_POINT ( 'NONE',  ( 50.80000000000001847, -4.319730106884873244, -1.256953381662414770 ) ) ;
#17743=DIRECTION ( 'NONE',  ( -3.489354422748178582E-15, 1.218509414717996338E-16, -1.000000000000000000 ) ) ;
#17745=CARTESIAN_POINT ( 'NONE',  ( 30.51261366513615059, 7.487866468533194819, 1.424999999999893019 ) ) ;
#17746=ORIENTED_EDGE ( 'NONE', *, *, #7528, .F. ) ;
#17751=EDGE_CURVE ( 'NONE', #10732, #3631, #24906, .T. ) ;
#17752=DIRECTION ( 'NONE',  ( -1.000000000000000000, -0.000000000000000000, 3.491481338843133355E-15 ) ) ;
#17760=CARTESIAN_POINT ( 'NONE',  ( 51.80000000000001137, 8.600000000000108002, -1.950000000000180256 ) ) ;
#17764=CARTESIAN_POINT ( 'NONE',  ( 29.29107486424064177, 6.659593085418572755, -1.425000000000101963 ) ) ;
#17781=ORIENTED_EDGE ( 'NONE', *, *, #24512, .T. ) ;
#17789=ORIENTED_EDGE ( 'NONE', *, *, #23641, .F. ) ;
#17791=CARTESIAN_POINT ( 'NONE',  ( 52.01814763855281143, 4.368239464846260134, -1.441698456444288290 ) ) ;
#17794=ORIENTED_EDGE ( 'NONE', *, *, #30078, .F. ) ;
#17798=CARTESIAN_POINT ( 'NONE',  ( 25.06719628372391639, 5.330953183979298515, 1.949999999999910916 ) ) ;
#17814=CARTESIAN_POINT ( 'NONE',  ( 53.85175331755100814, 5.786643218348696216, 1.878002189130716149 ) ) ;
#17817=CARTESIAN_POINT ( 'NONE',  ( 51.88812122917388336, 8.998461838224887543, -1.950000000000180256 ) ) ;
#17820=DIRECTION ( 'NONE',  ( 3.491481338843133355E-15, -0.000000000000000000, 1.000000000000000000 ) ) ;
#17825=ORIENTED_EDGE ( 'NONE', *, *, #6537, .T. ) ;
#17826=CARTESIAN_POINT ( 'NONE',  ( 53.91582462592152325, 6.672259099522126036, -1.774223561664970861 ) ) ;
#17828=CARTESIAN_POINT ( 'NONE',  ( 51.77480685185290099, 3.850112906364226095, -1.502155480406633270 ) ) ;
#17830=CARTESIAN_POINT ( 'NONE',  ( 26.92903764427389035, 5.249711979587993405, -1.950000000000161604 ) ) ;
#17838=CARTESIAN_POINT ( 'NONE',  ( 47.00000000000000711, -3.550773357292059007, -2.049880134335985371 ) ) ;
#17842=CARTESIAN_POINT ( 'NONE',  ( 51.60243094284678023, -4.191177329985464439, 1.624749424009206411 ) ) ;
#17850=CARTESIAN_POINT ( 'NONE',  ( 54.36194271933292299, 6.362460388746521645, 2.049999999999810196 ) ) ;
#17851=ORIENTED_EDGE ( 'NONE', *, *, #17396, .F. ) ;
#17863=FACE_OUTER_BOUND ( 'NONE', #23581, .T. ) ;
#17864=CARTESIAN_POINT ( 'NONE',  ( 34.56702326949725546, 8.213851659285209550, 1.549999999999879696 ) ) ;
#17867=DIRECTION ( 'NONE',  ( 1.000000000000000000, 0.000000000000000000, -3.491481338843133750E-15 ) ) ;
#17881=CARTESIAN_POINT ( 'NONE',  ( 47.05963571244990362, 8.266527678078146479, -2.050000000000163691 ) ) ;
#17882=CARTESIAN_POINT ( 'NONE',  ( 22.40781231897555870, 7.073106863806386535, 2.049999999999922107 ) ) ;
#17889=FACE_OUTER_BOUND ( 'NONE', #26628, .T. ) ;
#17890=ORIENTED_EDGE ( 'NONE', *, *, #6018, .T. ) ;
#17896=DIRECTION ( 'NONE',  ( -0.03489949670247565611, -0.9993908270190966503, 0.000000000000000000 ) ) ;
#17903=CARTESIAN_POINT ( 'NONE',  ( 47.06312566212017146, 8.366466760780054912, 1.949999999999835865 ) ) ;
#17904=CARTESIAN_POINT ( 'NONE',  ( 53.71283936284424954, 7.813984279442741432, -2.050000000000187228 ) ) ;
#17909=ADVANCED_FACE ( 'NONE', ( #10976 ), #3843, .T. ) ;
#17912=ADVANCED_FACE ( 'NONE', ( #12868 ), #14409, .T. ) ;
#17926=CARTESIAN_POINT ( 'NONE',  ( 52.72388909185001893, 4.000582417204455510, 2.049999999999815969 ) ) ;
#17929=ADVANCED_FACE ( 'NONE', ( #11128 ), #854, .T. ) ;
#17933=CARTESIAN_POINT ( 'NONE',  ( 54.19386703870443966, 5.671865141453451109, 2.049999999999810640 ) ) ;
#17942=CARTESIAN_POINT ( 'NONE',  ( 22.18976255005305021, 7.481058471421467182, 2.049999999999922551 ) ) ;
#17948=AXIS2_PLACEMENT_3D ( 'NONE', #22265, #17820, #27456 ) ;
#17952=DIRECTION ( 'NONE',  ( -1.000000000000000000, -0.000000000000000000, 3.491481338843133355E-15 ) ) ;
#17964=ORIENTED_EDGE ( 'NONE', *, *, #8547, .T. ) ;
#17975=CARTESIAN_POINT ( 'NONE',  ( 47.00000000000002132, 6.982261990806648555E-14, -1.628983268085978048E-13 ) ) ;
#17983=AXIS2_PLACEMENT_3D ( 'NONE', #13592, #27865, #22963 ) ;
#17987=CARTESIAN_POINT ( 'NONE',  ( 47.19764788914726239, -3.901663320877392760, -1.540393549661939865 ) ) ;
#17991=CARTESIAN_POINT ( 'NONE',  ( 51.03825729975065428, -4.379902212273306006, 1.406632791261188897 ) ) ;
#17992=AXIS2_PLACEMENT_3D ( 'NONE', #18651, #15647, #3604 ) ;
#17999=ORIENTED_EDGE ( 'NONE', *, *, #119, .F. ) ;
#18001=CARTESIAN_POINT ( 'NONE',  ( 54.16352682579100986, 5.682044187412361502, 2.049999999999811084 ) ) ;
#18046=DIRECTION ( 'NONE',  ( -0.9480661539417394312, 0.3180732113053816867, 0.000000000000000000 ) ) ;
#18047=CARTESIAN_POINT ( 'NONE',  ( 34.56269065792917417, 8.313757757582560970, 2.049999999999879474 ) ) ;
#18048=ORIENTED_EDGE ( 'NONE', *, *, #30332, .F. ) ;
#18060=CARTESIAN_POINT ( 'NONE',  ( 26.19155409318043226, 5.638511060912941630, -1.425000000000091305 ) ) ;
#18063=CARTESIAN_POINT ( 'NONE',  ( 50.80000000000001847, -4.319730106884873244, -1.256953381662414770 ) ) ;
#18071=CARTESIAN_POINT ( 'NONE',  ( 53.32659268230732152, 4.996744265006703323, -1.614825610218436625 ) ) ;
#18076=CARTESIAN_POINT ( 'NONE',  ( 53.90340377275680339, 6.895264694547793560, -2.050000000000123723 ) ) ;
#18089=ORIENTED_EDGE ( 'NONE', *, *, #19713, .T. ) ;
#18094=CARTESIAN_POINT ( 'NONE',  ( 47.12416679051325730, -3.859603212985637466, -1.644059474114685893 ) ) ;
#18097=EDGE_CURVE ( 'NONE', #13195, #6282, #2267, .T. ) ;
#18098=CARTESIAN_POINT ( 'NONE',  ( 51.29912638713659589, 3.898228643449898723, 2.049999999999820410 ) ) ;
#18099=CARTESIAN_POINT ( 'NONE',  ( 22.04321716858593661, 7.679566743993218481, -1.550000000000076206 ) ) ;
#18101=VECTOR ( 'NONE', #21681, 1000.000000000000000 ) ;
#18102=EDGE_LOOP ( 'NONE', ( #27433, #27425, #8502 ) ) ;
#18109=CARTESIAN_POINT ( 'NONE',  ( 25.91283125986204183, 5.216860428245192693, 1.949999999999909583 ) ) ;
#18116=EDGE_CURVE ( 'NONE', #30783, #28370, #28590, .T. ) ;
#18132=DIRECTION ( 'NONE',  ( -0.9993908270190957621, 0.03489949670250106634, 3.490838185622846777E-15 ) ) ;
#18145=ORIENTED_EDGE ( 'NONE', *, *, #18280, .T. ) ;
#18146=CARTESIAN_POINT ( 'NONE',  ( 51.80000000000001137, -3.933368109459640660, -2.186004417993355098 ) ) ;
#18152=ORIENTED_EDGE ( 'NONE', *, *, #1460, .F. ) ;
#18157=ADVANCED_FACE ( 'NONE', ( #11272 ), #4156, .F. ) ;
#18174=CARTESIAN_POINT ( 'NONE',  ( 54.32946523776459458, 6.710822964229192777, -2.050000000000189004 ) ) ;
#18181=AXIS2_PLACEMENT_3D ( 'NONE', #30468, #30958, #8772 ) ;
#18184=EDGE_LOOP ( 'NONE', ( #17789, #22813 ) ) ;
#18185=CARTESIAN_POINT ( 'NONE',  ( 34.56269065792915995, 8.313757757582562746, -2.050000000000119726 ) ) ;
#18190=CARTESIAN_POINT ( 'NONE',  ( 50.80000000000002558, -4.319730106884873244, 1.256953381662059277 ) ) ;
#18196=CARTESIAN_POINT ( 'NONE',  ( 22.07280086217095061, 8.086143481909148889, 2.049999999999922995 ) ) ;
#18224=CARTESIAN_POINT ( 'NONE',  ( 51.41699094018468230, -4.256549615192540159, -1.449195206876658482 ) ) ;
#18228=PRODUCT_CONTEXT ( 'NONE', #10736, 'mechanical' ) ;
#18233=CARTESIAN_POINT ( 'NONE',  ( 54.23225718638637005, 5.947176913004134313, -2.050000000000189004 ) ) ;
#18240=CARTESIAN_POINT ( 'NONE',  ( 53.96125931204732495, 5.169815675097246377, -2.050000000000188116 ) ) ;
#18241=CARTESIAN_POINT ( 'NONE',  ( 31.35411506561226602, 7.935106537971987173, 1.424999999999891021 ) ) ;
#18244=EDGE_LOOP ( 'NONE', ( #8756, #16573, #16556, #31095 ) ) ;
#18257=CARTESIAN_POINT ( 'NONE',  ( 47.10000000000000853, 7.037371096768279372E-14, -4.500000000000199840 ) ) ;
#18269=CARTESIAN_POINT ( 'NONE',  ( 22.11060592828335203, 7.457498294695588115, -1.425000000000077094 ) ) ;
#18277=EDGE_CURVE ( 'NONE', #16857, #9403, #10384, .T. ) ;
#18280=EDGE_CURVE ( 'NONE', #4799, #24892, #12885, .T. ) ;
#18295=VERTEX_POINT ( 'NONE', #20307 ) ;
#18296=CARTESIAN_POINT ( 'NONE',  ( 22.00282357524660171, 7.757228885921728434, -2.049999999999808420 ) ) ;
#18302=CARTESIAN_POINT ( 'NONE',  ( 47.19713079078776019, -3.901416201057355426, 1.541017813822200155 ) ) ;
#18321=CARTESIAN_POINT ( 'NONE',  ( 51.67634979243387505, -3.859233156638911755, 1.644927388240807531 ) ) ;
#18324=CARTESIAN_POINT ( 'NONE',  ( 54.23463818034554862, 5.946682447858800735, 2.049999999999810640 ) ) ;
#18327=CARTESIAN_POINT ( 'NONE',  ( 51.80000000000001137, -3.700146292169718354, -1.985065161562939107 ) ) ;
#18329=ORIENTED_EDGE ( 'NONE', *, *, #18280, .F. ) ;
#18330=CARTESIAN_POINT ( 'NONE',  ( 31.73174553812004106, 7.673395716939830358, -2.050000000000110845 ) ) ;
#18331=LINE ( 'NONE', #13557, #19605 ) ;
#18342=FACE_OUTER_BOUND ( 'NONE', #11512, .T. ) ;
#18345=EDGE_CURVE ( 'NONE', #15816, #25173, #13896, .T. ) ;
#18349=EDGE_CURVE ( 'NONE', #25407, #13124, #20517, .T. ) ;
#18357=CYLINDRICAL_SURFACE ( 'NONE', #2091, 0.09999999999999850675 ) ;
#18361=ORIENTED_EDGE ( 'NONE', *, *, #2247, .F. ) ;
#18363=CARTESIAN_POINT ( 'NONE',  ( 29.29107486424065243, 6.659593085418572755, 1.424999999999897238 ) ) ;
#18380=DIRECTION ( 'NONE',  ( -0.9993908270190957621, 0.03489949670250100389, 3.492120980335537899E-15 ) ) ;
#18386=CARTESIAN_POINT ( 'NONE',  ( 52.38136139153902349, 3.988241223888660869, -2.045676639479365733 ) ) ;
#18394=CARTESIAN_POINT ( 'NONE',  ( 47.00000000000002132, -3.701043595308294076, -1.983423889356798142 ) ) ;
#18397=CARTESIAN_POINT ( 'NONE',  ( 52.18343291569984643, 8.689381540779885782, 2.049999999999818190 ) ) ;
#18406=CARTESIAN_POINT ( 'NONE',  ( 23.02975722382757695, 6.234282476769586800, 1.949999999999919131 ) ) ;
#18410=ORIENTED_EDGE ( 'NONE', *, *, #14822, .T. ) ;
#18449=CARTESIAN_POINT ( 'NONE',  ( 24.17629218427073923, 5.599093920977425753, -2.050000000000020695 ) ) ;
#18453=ORIENTED_EDGE ( 'NONE', *, *, #19319, .T. ) ;
#18461=CARTESIAN_POINT ( 'NONE',  ( 47.10000000000002984, -3.550773357292059007, 2.049880134335656745 ) ) ;
#18477=ORIENTED_EDGE ( 'NONE', *, *, #211, .T. ) ;
#18478=CARTESIAN_POINT ( 'NONE',  ( 54.16322038507461656, 5.604326647956827223, 2.049999999999811084 ) ) ;
#18489=CARTESIAN_POINT ( 'NONE',  ( 51.80000048029754822, 4.021162616303429971, -2.019962949071075542 ) ) ;
#18517=EDGE_LOOP ( 'NONE', ( #30196, #9330, #23228, #23483 ) ) ;
#18518=CIRCLE ( 'NONE', #6870, 4.600000000000036948 ) ;
#18533=CARTESIAN_POINT ( 'NONE',  ( 52.27848606442668711, 4.392737230661539094, -1.555162892461804613 ) ) ;
#18535=ADVANCED_FACE ( 'NONE', ( #12 ), #2687, .F. ) ;
#18544=CARTESIAN_POINT ( 'NONE',  ( 50.87477060347374902, 8.633605004118187765, 1.949999999999822320 ) ) ;
#18548=CARTESIAN_POINT ( 'NONE',  ( 47.88109723283228192, -4.387164036186663729, -1.383037136012811308 ) ) ;
#18556=CARTESIAN_POINT ( 'NONE',  ( 47.73697115155167126, -4.023893809447296910, -1.198232146805585874 ) ) ;
#18560=CARTESIAN_POINT ( 'NONE',  ( 53.21917409580260028, 8.083376426877340037, 2.049999999999814637 ) ) ;
#18568=EDGE_LOOP ( 'NONE', ( #15545, #16859, #15528, #9778 ) ) ;
#18576=CLOSED_SHELL ( 'NONE', ( #9644, #13735, #6354, #7421, #6219, #18535, #8407, #14669, #26220, #6917, #19260, #29976, #11153, #30634, #29921, #8088, #23555, #16403, #1642, #27343, #5352, #29351, #11918, #6183, #4732, #12266, #18157, #12194, #23381, #4311, #19137, #21474, #5507, #26839, #12463, #12742, #11174, #155, #26363, #7361, #28696, #12711, #6123, #17495, #30887, #19264, #14087, #16307, #24188, #5553, #1392, #17929, #11618, #8883, #22644, #28210, #11565, #19362, #157, #26011, #17342, #12129, #10164, #9054, #11621, #16436, #1226, #21193, #17629, #21466, #28293, #20247, #10531, #16772, #22648, #30236, #24768, #2683, #29135, #24514, #30081, #17912, #20610, #25619, #17909, #30338, #11334, #26643, #19047, #13680, #25334, #4855, #5057, #23760, #20878, #7848 ) ) ;
#18581=DIRECTION ( 'NONE',  ( 3.489354422748178582E-15, -1.218509414717996338E-16, 1.000000000000000000 ) ) ;
#18582=CARTESIAN_POINT ( 'NONE',  ( 30.02700392305999344, 6.560679691584628159, -1.425000000000105072 ) ) ;
#18587=CARTESIAN_POINT ( 'NONE',  ( 47.05963571244991783, 8.266527678078146479, 1.949999999999835865 ) ) ;
#18598=EDGE_CURVE ( 'NONE', #22328, #8007, #13976, .T. ) ;
#18614=DIRECTION ( 'NONE',  ( 3.489354422748178582E-15, -1.218509414717996338E-16, 1.000000000000000000 ) ) ;
#18638=CARTESIAN_POINT ( 'NONE',  ( 51.06223082645568923, -3.930699233196520481, 1.170919866330858650 ) ) ;
#18639=ORIENTED_EDGE ( 'NONE', *, *, #13848, .F. ) ;
#18640=CARTESIAN_POINT ( 'NONE',  ( 54.23267447929808327, 6.619944661321486734, 2.049999999999810640 ) ) ;
#18651=CARTESIAN_POINT ( 'NONE',  ( 41.48619405472009447, -151.3359592902261852, -1.550000000000163469 ) ) ;
#18665=VERTEX_POINT ( 'NONE', #20420 ) ;
#18673=VERTEX_POINT ( 'NONE', #27689 ) ;
#18681=TOROIDAL_SURFACE ( 'NONE', #5017, 4.199999999999993072, 0.1000000000000000056 ) ;
#18685=ORIENTED_EDGE ( 'NONE', *, *, #11955, .F. ) ;
#18694=ORIENTED_EDGE ( 'NONE', *, *, #24855, .F. ) ;
#18700=DIRECTION ( 'NONE',  ( 3.083952846180964840E-15, 0.000000000000000000, 1.000000000000000000 ) ) ;
#18712=ORIENTED_EDGE ( 'NONE', *, *, #29868, .T. ) ;
#18749=CARTESIAN_POINT ( 'NONE',  ( 51.80000000000002558, 6.475000000000061817, 1.949999999999818767 ) ) ;
#18754=ORIENTED_EDGE ( 'NONE', *, *, #30491, .T. ) ;
#18763=ORIENTED_EDGE ( 'NONE', *, *, #29868, .F. ) ;
#18766=CYLINDRICAL_SURFACE ( 'NONE', #5326, 4.099999999999992539 ) ;
#18791=VECTOR ( 'NONE', #28324, 1000.000000000000000 ) ;
#18797=CARTESIAN_POINT ( 'NONE',  ( 53.71392934491858995, 7.814769211952036443, 2.049999999999812417 ) ) ;
#18800=CARTESIAN_POINT ( 'NONE',  ( 51.06494979651333210, -4.023708852620672793, -1.198807875231533426 ) ) ;
#18809=ORIENTED_EDGE ( 'NONE', *, *, #11756, .F. ) ;
#18833=CARTESIAN_POINT ( 'NONE',  ( 51.87673771347597551, 8.672480599449025718, 2.049999999999819522 ) ) ;
#18843=EDGE_LOOP ( 'NONE', ( #29264, #15573, #30228, #22885 ) ) ;
#18846=CARTESIAN_POINT ( 'NONE',  ( 50.35762544161296006, 8.151359338959888845, 1.949999999999825206 ) ) ;
#18857=FACE_OUTER_BOUND ( 'NONE', #11372, .T. ) ;
#18868=AXIS2_PLACEMENT_3D ( 'NONE', #7186, #28878, #12242 ) ;
#18887=EDGE_CURVE ( 'NONE', #8527, #14388, #14049, .T. ) ;
#18889=CARTESIAN_POINT ( 'NONE',  ( 24.34823467037698919, 5.521868380698613521, -1.425000000000085087 ) ) ;
#18892=EDGE_CURVE ( 'NONE', #16720, #15457, #18518, .T. ) ;
#18907=CARTESIAN_POINT ( 'NONE',  ( 54.22843442268823821, 6.361173098464514730, -2.050000000000188116 ) ) ;
#18910=CARTESIAN_POINT ( 'NONE',  ( 22.54717926605049172, 7.740376438784041468, 1.424999999999921219 ) ) ;
#18912=CARTESIAN_POINT ( 'NONE',  ( 29.69543387591359362, 6.938696499881336521, 1.424999999999896572 ) ) ;
#18914=ORIENTED_EDGE ( 'NONE', *, *, #22419, .F. ) ;
#18923=DIRECTION ( 'NONE',  ( -0.9926670569371678354, -0.1208805777273652682, -2.408208294782601816E-14 ) ) ;
#18925=CARTESIAN_POINT ( 'NONE',  ( 32.30803788188344328, 7.816246126570704611, 1.949999999999824096 ) ) ;
#18938=CARTESIAN_POINT ( 'NONE',  ( 47.10000000000003695, 2.428612866367529932E-14, 4.199999999999827871 ) ) ;
#18949=ORIENTED_EDGE ( 'NONE', *, *, #11356, .F. ) ;
#18950=CARTESIAN_POINT ( 'NONE',  ( 52.09213388422778479, 8.599999999993011457, 2.049999999999818190 ) ) ;
#18959=DIRECTION ( 'NONE',  ( -3.489354422748178582E-15, 1.218509414717996338E-16, -1.000000000000000000 ) ) ;
#18975=VECTOR ( 'NONE', #15103, 999.9999999999998863 ) ;
#18980=CARTESIAN_POINT ( 'NONE',  ( 21.97322666366011035, 8.076925076899302169, -7.622595309165997977E-14 ) ) ;
#19005=CARTESIAN_POINT ( 'NONE',  ( 54.31409749668478071, 6.709390224138189751, -2.050000000000189004 ) ) ;
#19013=FACE_OUTER_BOUND ( 'NONE', #18184, .T. ) ;
#19014=DIRECTION ( 'NONE',  ( 1.000000000000000000, 0.000000000000000000, -3.491481338843133750E-15 ) ) ;
#19018=LINE ( 'NONE', #30729, #10937 ) ;
#19028=VERTEX_POINT ( 'NONE', #16907 ) ;
#19036=EDGE_LOOP ( 'NONE', ( #16175, #26232, #19491, #20425 ) ) ;
#19041=CARTESIAN_POINT ( 'NONE',  ( 51.41795137217811629, -3.967700393345039878, -1.365904513877001403 ) ) ;
#19044=CIRCLE ( 'NONE', #13944, 2.625000000001612044 ) ;
#19047=ADVANCED_FACE ( 'NONE', ( #24340 ), #9437, .T. ) ;
#19062=ORIENTED_EDGE ( 'NONE', *, *, #15289, .T. ) ;
#19063=CARTESIAN_POINT ( 'NONE',  ( 52.08333333333334991, 4.368973594129894167, -1.439468559502902645 ) ) ;
#19064=CARTESIAN_POINT ( 'NONE',  ( 54.19028661868582475, 6.697846887293304796, 2.049999999999810640 ) ) ;
#19068=CARTESIAN_POINT ( 'NONE',  ( 47.05963571244991783, 8.266527678078146479, 1.549999999999835953 ) ) ;
#19073=CARTESIAN_POINT ( 'NONE',  ( 47.73537254841801314, -4.023728077055556795, 1.198744011644558682 ) ) ;
#19074=CARTESIAN_POINT ( 'NONE',  ( 24.57460841532291340, 5.893272594507614315, 1.424999999999914335 ) ) ;
#19082=LINE ( 'NONE', #14622, #30838 ) ;
#19085=CARTESIAN_POINT ( 'NONE',  ( 50.80000000000002558, -4.031600731908413948, 1.173113608511496375 ) ) ;
#19120=CARTESIAN_POINT ( 'NONE',  ( 51.41858953131476540, -3.967542327744261410, -1.366354831956597460 ) ) ;
#19121=EDGE_CURVE ( 'NONE', #21850, #28904, #19044, .T. ) ;
#19127=LINE ( 'NONE', #7080, #27694 ) ;
#19133=FACE_OUTER_BOUND ( 'NONE', #14741, .T. ) ;
#19136=CARTESIAN_POINT ( 'NONE',  ( 47.10000000000002984, -4.020776289669855785, 2.234582293948414122 ) ) ;
#19137=ADVANCED_FACE ( 'NONE', ( #20387 ), #1197, .F. ) ;
#19142=CARTESIAN_POINT ( 'NONE',  ( 47.00000000000002132, 6.982261990806648555E-14, -1.628983268085978048E-13 ) ) ;
#19153=CARTESIAN_POINT ( 'NONE',  ( 53.81464057712624793, 5.799094425976102585, -1.689602626210267466 ) ) ;
#19154=ORIENTED_EDGE ( 'NONE', *, *, #5046, .T. ) ;
#19161=EDGE_CURVE ( 'NONE', #10675, #6667, #16461, .T. ) ;
#19181=CARTESIAN_POINT ( 'NONE',  ( 52.05000000000001137, 4.616741406585203933, -2.050000000000181011 ) ) ;
#19182=CARTESIAN_POINT ( 'NONE',  ( 26.81612439946666626, 5.236792088878508444, -1.950000000000093880 ) ) ;
#19189=CARTESIAN_POINT ( 'NONE',  ( 47.12385499560041779, -4.149773407328906316, -1.728861777176172509 ) ) ;
#19190=CARTESIAN_POINT ( 'NONE',  ( 50.80000000000002558, -3.908336260473453727, 1.238913909465742202 ) ) ;
#19195=DIRECTION ( 'NONE',  ( 0.03489949670250097613, 0.9993908270190957621, 2.465190328815662439E-32 ) ) ;
#19203=FACE_OUTER_BOUND ( 'NONE', #6853, .T. ) ;
#19205=CIRCLE ( 'NONE', #8060, 0.09999999999999992228 ) ;
#19209=CARTESIAN_POINT ( 'NONE',  ( 50.80000000000001847, -4.031600731908413948, -1.173113608511851869 ) ) ;
#19211=ORIENTED_EDGE ( 'NONE', *, *, #18887, .F. ) ;
#19216=DIRECTION ( 'NONE',  ( 3.023770467182126270E-15, -0.4999707644721522182, 0.8660422822663637055 ) ) ;
#19221=DIRECTION ( 'NONE',  ( 3.304235192336781034E-15, 0.000000000000000000, 1.000000000000000000 ) ) ;
#19223=DIRECTION ( 'NONE',  ( -1.000000000000000000, -0.000000000000000000, 3.491481338843133355E-15 ) ) ;
#19244=VERTEX_POINT ( 'NONE', #6122 ) ;
#19251=CARTESIAN_POINT ( 'NONE',  ( 31.73163254175109671, 7.673342709000030126, 2.049999999999888800 ) ) ;
#19260=ADVANCED_FACE ( 'NONE', ( #30637 ), #1514, .T. ) ;
#19264=ADVANCED_FACE ( 'NONE', ( #24115 ), #2351, .T. ) ;
#19267=CARTESIAN_POINT ( 'NONE',  ( 53.94440344817330413, 6.524635634306426901, 2.049999999999811529 ) ) ;
#19281=CARTESIAN_POINT ( 'NONE',  ( 29.25706191173316739, 5.994885333997869381, 1.949999999999897371 ) ) ;
#19282=ORIENTED_EDGE ( 'NONE', *, *, #17320, .T. ) ;
#19284=VERTEX_POINT ( 'NONE', #21178 ) ;
#19302=CARTESIAN_POINT ( 'NONE',  ( 53.91582462592152325, 6.672259099522126036, -1.484311132272649436 ) ) ;
#19307=CARTESIAN_POINT ( 'NONE',  ( 47.07708546080149148, 8.766223091587903582, -1.550000000000163469 ) ) ;
#19309=CARTESIAN_POINT ( 'NONE',  ( 47.21358082890262864, -3.755449232595078346, -1.648679025009969878 ) ) ;
#19315=ORIENTED_EDGE ( 'NONE', *, *, #27210, .T. ) ;
#19319=EDGE_CURVE ( 'NONE', #20522, #133, #8910, .T. ) ;
#19323=DIRECTION ( 'NONE',  ( -0.4772254810013855097, 0.8787808829753844808, 1.772289120718281137E-15 ) ) ;
#19331=CARTESIAN_POINT ( 'NONE',  ( 30.12780005191093480, 6.637137500361657949, -1.950000000000104539 ) ) ;
#19341=CIRCLE ( 'NONE', #3633, 159.7997717543496776 ) ;
#19352=CARTESIAN_POINT ( 'NONE',  ( 51.89161117884418672, 9.098400920928359170, -2.050000000000180123 ) ) ;
#19362=ADVANCED_FACE ( 'NONE', ( #3188 ), #19374, .T. ) ;
#19366=FACE_OUTER_BOUND ( 'NONE', #13004, .T. ) ;
#19367=DIRECTION ( 'NONE',  ( 0.9993908270190958731, -0.03489949670249358621, -4.336808689942082423E-15 ) ) ;
#19369=DIRECTION ( 'NONE',  ( -0.9926670569371645048, -0.1208805777273925935, 3.449037773238375127E-15 ) ) ;
#19374=PLANE ( 'NONE',  #29126 ) ;
#19380=CARTESIAN_POINT ( 'NONE',  ( 47.00000000000002842, -4.020776289669855785, 2.234582293948414122 ) ) ;
#19398=CARTESIAN_POINT ( 'NONE',  ( 29.19109589768859792, 6.114704649262250769, 2.049999999999898126 ) ) ;
#19401=CARTESIAN_POINT ( 'NONE',  ( 51.65273894882757588, 3.822289909571943145, -2.050000000000175682 ) ) ;
#19410=CARTESIAN_POINT ( 'NONE',  ( 53.21917409580247238, 8.083376426877231680, 1.902110155464532104 ) ) ;
#19416=VERTEX_POINT ( 'NONE', #12231 ) ;
#19419=CARTESIAN_POINT ( 'NONE',  ( 47.09104525948222886, 9.165979422395331255, -1.950000000000163380 ) ) ;
#19426=CARTESIAN_POINT ( 'NONE',  ( 31.30720621464601905, 7.411182539856417506, -1.950000000000108535 ) ) ;
#19436=CARTESIAN_POINT ( 'NONE',  ( 52.98236138753809854, 8.264679131573773319, -2.050000000000184119 ) ) ;
#19437=B_SPLINE_CURVE_WITH_KNOTS ( 'NONE', 3,
 ( #23941, #26314, #21421, #26155, #26620, #19041, #9551, #24095, #12214, #19209 ),
 .UNSPECIFIED., .F., .F.,
 ( 4, 2, 2, 2, 4 ),
 ( 0.000000000000000000, 0.0003926182454497113513, 0.0007852364908994227026, 0.001177854736349134108, 0.001570472981798845405 ),
 .UNSPECIFIED. ) ;
#19441=VECTOR ( 'NONE', #14359, 1000.000000000000000 ) ;
#19445=EDGE_CURVE ( 'NONE', #29912, #6282, #5660, .T. ) ;
#19448=CARTESIAN_POINT ( 'NONE',  ( 53.94293340116774260, 6.381487143331855627, -2.142504121165067499E-08 ) ) ;
#19456=CARTESIAN_POINT ( 'NONE',  ( 47.88186413446628364, -3.908336260473453727, -1.238913909466087926 ) ) ;
#19477=CARTESIAN_POINT ( 'NONE',  ( 30.62824136006083720, 6.974337361240579014, -1.950000000000106759 ) ) ;
#19489=CARTESIAN_POINT ( 'NONE',  ( 48.00000000000002842, -3.657334280697315698, 2.105684202162165342 ) ) ;
#19491=ORIENTED_EDGE ( 'NONE', *, *, #15289, .F. ) ;
#19497=ORIENTED_EDGE ( 'NONE', *, *, #29717, .F. ) ;
#19508=( LENGTH_UNIT ( ) NAMED_UNIT ( * ) SI_UNIT ( .MILLI., .METRE. ) );
#19509=AXIS2_PLACEMENT_3D ( 'NONE', #30611, #17867, #1634 ) ;
#19513=CARTESIAN_POINT ( 'NONE',  ( 53.25639650609795694, 8.250950595073881288, -2.050000000000185452 ) ) ;
#19530=( BOUNDED_SURFACE ( )  B_SPLINE_SURFACE ( 3, 2, ( 
 ( #30016, #25279, #8641 ),
 ( #20853, #4203, #23069 ),
 ( #11321, #18638, #25748 ),
 ( #25580, #16252, #21007 ),
 ( #1366, #30645, #8958 ),
 ( #13547, #8496, #23230 ),
 ( #30482, #6594, #18321 ),
 ( #22914, #15780, #25429 ),
 ( #3592, #6273, #15919 ),
 ( #8785, #1518, #3899 ) ),
 .UNSPECIFIED., .F., .F., .F. ) 
 B_SPLINE_SURFACE_WITH_KNOTS ( ( 4, 2, 2, 2, 4 ),
 ( 3, 3 ),
 ( -5.421010862427522170E-20, 0.0003537438758377288439, 0.0007074877516754576878, 0.001061231627513186532, 0.001414975503350915376 ),
 ( 0.000000000000000000, 1.000000000000000000 ),
 .UNSPECIFIED. ) 
 GEOMETRIC_REPRESENTATION_ITEM ( )  RATIONAL_B_SPLINE_SURFACE ( (
 ( 1.000000000000000000, 0.7154752000627009334, 1.000000000000000000),
 ( 1.000000000000000000, 0.7154106121891214976, 1.000000000000000000),
 ( 1.000000000000000000, 0.7173719856077137580, 1.000000000000000000),
 ( 1.000000000000000000, 0.7229186815317750758, 1.000000000000000000),
 ( 1.000000000000000000, 0.7264660769275549379, 1.000000000000000000),
 ( 1.000000000000000000, 0.7305267549316539766, 1.000000000000000000),
 ( 1.000000000000000000, 0.7309418327392975812, 1.000000000000000000),
 ( 1.000000000000000000, 0.7246992783963228657, 1.000000000000000000),
 ( 1.000000000000000000, 0.7179850693090684688, 1.000000000000000000),
 ( 1.000000000000000000, 0.7071067811865482389, 1.000000000000000000) ) ) 
 REPRESENTATION_ITEM ( '' )  SURFACE ( )  );
#19532=AXIS2_PLACEMENT_3D ( 'NONE', #13801, #23487, #20358 ) ;
#19536=CARTESIAN_POINT ( 'NONE',  ( 41.48619405472010868, -151.3359592902261852, 1.549999999999835953 ) ) ;
#19537=CARTESIAN_POINT ( 'NONE',  ( 47.49114655384919104, -4.380199991372831114, 1.408811060053114739 ) ) ;
#19555=DIRECTION ( 'NONE',  ( 3.491481338843133355E-15, 0.000000000000000000, 1.000000000000000000 ) ) ;
#19556=CARTESIAN_POINT ( 'NONE',  ( 27.54696499482877314, 5.363421040582749377, 1.949999999999838307 ) ) ;
#19584=CARTESIAN_POINT ( 'NONE',  ( 54.23679421920402177, 6.620234584472831862, 2.049999999999810640 ) ) ;
#19595=CARTESIAN_POINT ( 'NONE',  ( 28.66473729876425125, 5.839050301630731354, -2.050000000000099298 ) ) ;
#19604=CARTESIAN_POINT ( 'NONE',  ( 51.87767605783385960, 8.699351266148436679, -2.050000000000180123 ) ) ;
#19605=VECTOR ( 'NONE', #13709, 1000.000000000000000 ) ;
#19607=CARTESIAN_POINT ( 'NONE',  ( 34.56702326949725546, 8.213851659285209550, 1.549999999999879696 ) ) ;
#19614=CARTESIAN_POINT ( 'NONE',  ( 47.00000000000001421, -3.637377585518695611, -2.099877210783201331 ) ) ;
#19617=CARTESIAN_POINT ( 'NONE',  ( 54.12874039445436836, 6.030813710072695066, 2.034055266290029085 ) ) ;
#19629=CARTESIAN_POINT ( 'NONE',  ( 52.28361797084581042, 3.966539589492596107, 2.045539107969434056 ) ) ;
#19636=DIRECTION ( 'NONE',  ( -0.9993908270190956511, 0.03489949670250202390, 3.491481338843132961E-15 ) ) ;
#19637=LINE ( 'NONE', #2049, #10652 ) ;
#19640=CIRCLE ( 'NONE', #5977, 0.1000000000000006578 ) ;
#19652=DIRECTION ( 'NONE',  ( -1.000000000000000000, 0.000000000000000000, 3.491481338843133355E-15 ) ) ;
#19674=CARTESIAN_POINT ( 'NONE',  ( 54.23701917430468455, 5.946187982713466269, -2.050000000000189004 ) ) ;
#19695=CARTESIAN_POINT ( 'NONE',  ( 52.91818227938544794, 4.100069807933122590, 0.1744202563123046223 ) ) ;
#19696=CARTESIAN_POINT ( 'NONE',  ( 47.00000000000002842, -3.933368109459640660, 2.186004417993010485 ) ) ;
#19707=CARTESIAN_POINT ( 'NONE',  ( 51.82264168681148675, 4.510085190442490344, 0.9145483697865447459 ) ) ;
#19713=EDGE_CURVE ( 'NONE', #15558, #9996, #27135, .T. ) ;
#19714=CARTESIAN_POINT ( 'NONE',  ( 23.33428888328873185, 6.022557148079767941, 2.050000000000117506 ) ) ;
#19742=ORIENTED_EDGE ( 'NONE', *, *, #15906, .F. ) ;
#19743=CARTESIAN_POINT ( 'NONE',  ( 54.00141249824493883, 6.058257955356691760, -1.948923759896386443 ) ) ;
#19747=CARTESIAN_POINT ( 'NONE',  ( 30.67843166873835870, 7.122989987860104399, -2.050000000000106404 ) ) ;
#19750=EDGE_CURVE ( 'NONE', #26613, #29801, #25610, .T. ) ;
#19756=CARTESIAN_POINT ( 'NONE',  ( 53.05088594538231916, 4.168914605591084843, -2.050000000000185008 ) ) ;
#19764=CARTESIAN_POINT ( 'NONE',  ( 53.81464057712625504, 5.799094425976108802, -0.8364387603671682436 ) ) ;
#19804=CIRCLE ( 'NONE', #27366, 0.1000000000000002554 ) ;
#19808=ORIENTED_EDGE ( 'NONE', *, *, #26186, .T. ) ;
#19819=CARTESIAN_POINT ( 'NONE',  ( 51.74540690333466841, 3.818766532315405193, -2.050000000000175682 ) ) ;
#19826=B_SPLINE_CURVE_WITH_KNOTS ( 'NONE', 3,
 ( #6713, #16376, #25721, #15320, #10581, #20257 ),
 .UNSPECIFIED., .F., .F.,
 ( 4, 2, 4 ),
 ( 0.000000000000000000, 0.4999999999999995559, 1.000000000000000000 ),
 .UNSPECIFIED. ) ;
#19835=CARTESIAN_POINT ( 'NONE',  ( 51.74175063877302705, 3.850631602819848620, 1.433098087438243295 ) ) ;
#19837=CARTESIAN_POINT ( 'NONE',  ( 52.29551448703413996, 3.895969970751527178, -1.277875341319584246 ) ) ;
#19883=CARTESIAN_POINT ( 'NONE',  ( 51.35579717334661609, -4.328226263800980078, -1.560066312055160775 ) ) ;
#19888=CARTESIAN_POINT ( 'NONE',  ( 34.56269065792915995, 8.313757757582562746, -2.050000000000119726 ) ) ;
#19893=CARTESIAN_POINT ( 'NONE',  ( 54.34016439512040364, 6.711820450561372553, 2.049999999999808420 ) ) ;
#19897=CARTESIAN_POINT ( 'NONE',  ( 53.82285890661302119, 4.901445667019300068, -2.050000000000187672 ) ) ;
#19898=CARTESIAN_POINT ( 'NONE',  ( 48.00000000000001421, -3.908336260473454615, -1.238913909466087926 ) ) ;
#19911=CARTESIAN_POINT ( 'NONE',  ( 54.28867365409859502, 5.640057820322912363, -1.625000000000180744 ) ) ;
#19917=CARTESIAN_POINT ( 'NONE',  ( 53.34494210428218963, 4.987020249080358347, 1.614082030464476292 ) ) ;
#19920=DIRECTION ( 'NONE',  ( -3.489354422748178188E-15, 1.218509414717996091E-16, -1.000000000000000000 ) ) ;
#19929=AXIS2_PLACEMENT_3D ( 'NONE', #23627, #21104, #4454 ) ;
#19931=EDGE_CURVE ( 'NONE', #26160, #19416, #12763, .T. ) ;
#19945=EDGE_CURVE ( 'NONE', #5179, #21368, #29831, .T. ) ;
#19951=AXIS2_PLACEMENT_3D ( 'NONE', #12477, #24508, #22166 ) ;
#19957=CARTESIAN_POINT ( 'NONE',  ( 47.02510416483082167, -3.758927087870047146, 1.866445954014450903 ) ) ;
#19970=CARTESIAN_POINT ( 'NONE',  ( 51.75611399313549299, 4.330462468343535321, -2.050000000000496758 ) ) ;
#19973=CARTESIAN_POINT ( 'NONE',  ( 51.30607925897589183, -3.992076856964202669, 1.294425493480717115 ) ) ;
#19975=CARTESIAN_POINT ( 'NONE',  ( 31.35411506832756601, 7.935106539446550755, -1.425000000000109068 ) ) ;
#19983=ORIENTED_EDGE ( 'NONE', *, *, #18277, .T. ) ;
#19987=PLANE ( 'NONE',  #5535 ) ;
#19988=CARTESIAN_POINT ( 'NONE',  ( 47.38244758155640568, -4.256411467774985802, 1.449592950257672985 ) ) ;
#19991=CARTESIAN_POINT ( 'NONE',  ( 27.27214205000342062, 5.011961650406415281, -1.550000000000094857 ) ) ;
#19993=VECTOR ( 'NONE', #22786, 1000.000000000000000 ) ;
#19995=B_SPLINE_CURVE_WITH_KNOTS ( 'NONE', 3,
 ( #25417, #23218, #16242, #27805, #11167, #3720 ),
 .UNSPECIFIED., .F., .F.,
 ( 4, 2, 4 ),
 ( 2.716379216518720479E-07, 0.0002832190672503200860, 0.0005661664965789883243 ),
 .UNSPECIFIED. ) ;
#20001=CARTESIAN_POINT ( 'NONE',  ( 29.14728015088713420, 5.974878709855460102, 1.949999999999897815 ) ) ;
#20002=EDGE_CURVE ( 'NONE', #7829, #15664, #22992, .T. ) ;
#20006=VERTEX_POINT ( 'NONE', #25066 ) ;
#20007=CARTESIAN_POINT ( 'NONE',  ( 51.80000000000001137, 3.987918699320235572, -2.032049940491799322 ) ) ;
#20009=CARTESIAN_POINT ( 'NONE',  ( 26.92903764425156510, 5.249711979699990927, 2.050000000000040679 ) ) ;
#20011=AXIS2_PLACEMENT_3D ( 'NONE', #12233, #53, #196 ) ;
#20013=CARTESIAN_POINT ( 'NONE',  ( 54.24037840390754184, 6.535103219670295616, -2.050000000000189004 ) ) ;
#20043=CARTESIAN_POINT ( 'NONE',  ( 54.19008868793212486, 6.697828837789025158, -2.050000000000189004 ) ) ;
#20048=DIRECTION ( 'NONE',  ( 3.491481338843133750E-15, 0.000000000000000000, 1.000000000000000000 ) ) ;
#20051=CARTESIAN_POINT ( 'NONE',  ( 30.23587923126627786, 6.713699170113216930, -2.050000000000235190 ) ) ;
#20061=CARTESIAN_POINT ( 'NONE',  ( 54.23831472968566203, 6.535030234825930151, -2.050000000000189004 ) ) ;
#20062=AXIS2_PLACEMENT_3D ( 'NONE', #25895, #1360, #23375 ) ;
#20078=CARTESIAN_POINT ( 'NONE',  ( 54.41366571437522737, 6.718673005292171041, -0.9750000000001826095 ) ) ;
#20085=CARTESIAN_POINT ( 'NONE',  ( 51.52258228595268719, -3.791878011401587312, -1.561538262852857351 ) ) ;
#20086=CIRCLE ( 'NONE', #6419, 4.099999999999992539 ) ;
#20089=CIRCLE ( 'NONE', #26154, 0.09999999999999972800 ) ;
#20100=AXIS2_PLACEMENT_3D ( 'NONE', #20616, #30246, #5876 ) ;
#20111=CIRCLE ( 'NONE', #14022, 0.09999999999999972800 ) ;
#20124=VERTEX_POINT ( 'NONE', #30593 ) ;
#20129=ORIENTED_EDGE ( 'NONE', *, *, #10188, .F. ) ;
#20130=EDGE_LOOP ( 'NONE', ( #30792, #23715, #17119, #29191 ) ) ;
#20131=CARTESIAN_POINT ( 'NONE',  ( 47.07708546080149858, 8.766223091587903582, 1.549999999999835953 ) ) ;
#20148=CARTESIAN_POINT ( 'NONE',  ( 51.46757676178951613, 4.376162276235349147, -2.050000000000179234 ) ) ;
#20176=CARTESIAN_POINT ( 'NONE',  ( 52.05081297082752911, 4.366207722110991618, -1.447839973523495027 ) ) ;
#20182=AXIS2_PLACEMENT_3D ( 'NONE', #11696, #4092, #2031 ) ;
#20183=CARTESIAN_POINT ( 'NONE',  ( 24.17629218427016013, 5.599093920977841421, 2.049999999999914557 ) ) ;
#20205=ORIENTED_EDGE ( 'NONE', *, *, #9159, .F. ) ;
#20206=DIRECTION ( 'NONE',  ( -1.000000000000000000, -0.000000000000000000, 3.491481338843133355E-15 ) ) ;
#20213=CARTESIAN_POINT ( 'NONE',  ( 54.12879229448595453, 6.030824283042129252, -2.034063242164690255 ) ) ;
#20217=CARTESIAN_POINT ( 'NONE',  ( 27.84544208489333172, 5.444976783748663784, -1.950000000000065459 ) ) ;
#20226=CARTESIAN_POINT ( 'NONE',  ( 47.21114320858165314, -3.753732476607509749, 1.652583012570356669 ) ) ;
#20227=CARTESIAN_POINT ( 'NONE',  ( 47.38200087219854595, -3.967692247893680690, -1.365930198224970749 ) ) ;
#20231=CARTESIAN_POINT ( 'NONE',  ( 29.12648003328355983, 5.963603948890924045, -1.950000000000100320 ) ) ;
#20238=CARTESIAN_POINT ( 'NONE',  ( 54.44703553012594455, 6.360744381977848860, 0.9749999999998122391 ) ) ;
#20247=ADVANCED_FACE ( 'NONE', ( #14759 ), #29591, .T. ) ;
#20253=CARTESIAN_POINT ( 'NONE',  ( 54.41366571437522026, 6.718673005292167488, 1.949999999999809663 ) ) ;
#20257=CARTESIAN_POINT ( 'NONE',  ( 53.91574522233626965, 6.672251602764244893, -1.774295313897662485 ) ) ;
#20270=EDGE_CURVE ( 'NONE', #18295, #4290, #26649, .T. ) ;
#20275=CARTESIAN_POINT ( 'NONE',  ( 27.51012318650851896, 5.457609198730995814, 2.049999999999903011 ) ) ;
#20280=CARTESIAN_POINT ( 'NONE',  ( 47.10000000000002984, -3.550773357292059007, 2.049880134335656745 ) ) ;
#20285=ORIENTED_EDGE ( 'NONE', *, *, #21867, .T. ) ;
#20287=CARTESIAN_POINT ( 'NONE',  ( 23.27131915274573615, 6.595123925190214287, -1.425000000000080869 ) ) ;
#20288=ORIENTED_EDGE ( 'NONE', *, *, #19445, .F. ) ;
#20290=CYLINDRICAL_SURFACE ( 'NONE', #3905, 0.1000000000000001721 ) ;
#20294=EDGE_CURVE ( 'NONE', #5230, #16210, #23327, .T. ) ;
#20302=CARTESIAN_POINT ( 'NONE',  ( 54.23267447929806906, 6.619944661321486734, -2.050000000000189004 ) ) ;
#20305=CARTESIAN_POINT ( 'NONE',  ( 41.48619405472009447, -151.3359592902261852, -1.550000000000163469 ) ) ;
#20306=DIRECTION ( 'NONE',  ( -0.9993908270190957621, 0.03489949670250097613, 3.491481338843133355E-15 ) ) ;
#20307=CARTESIAN_POINT ( 'NONE',  ( 47.09104525948223596, 9.165979422395388099, -2.050000000000163691 ) ) ;
#20321=CARTESIAN_POINT ( 'NONE',  ( 51.29777716379116725, 3.891287491069770343, 2.049999999999820410 ) ) ;
#20325=CARTESIAN_POINT ( 'NONE',  ( 51.80000000000003979, 6.982261990806648555E-14, 4.499999999999857003 ) ) ;
#20338=CARTESIAN_POINT ( 'NONE',  ( 26.61920844898531868, 5.219578738934654183, 1.949999999999841860 ) ) ;
#20347=DIRECTION ( 'NONE',  ( -0.6819983600624907050, 0.7313537016191778983, 2.168404344971033323E-15 ) ) ;
#20352=CARTESIAN_POINT ( 'NONE',  ( 54.15673930838963912, 5.684321142249388892, 2.049999999999811529 ) ) ;
#20358=DIRECTION ( 'NONE',  ( -1.000000000000000000, 0.000000000000000000, 3.491481338843132961E-15 ) ) ;
#20369=CARTESIAN_POINT ( 'NONE',  ( 54.22156662858499487, 6.014361416436350360, -2.050000000000191225 ) ) ;
#20373=CARTESIAN_POINT ( 'NONE',  ( 23.13461596521335650, 6.279931474728896568, -2.050000000000080647 ) ) ;
#20379=CARTESIAN_POINT ( 'NONE',  ( 47.00000000000002842, -3.550773357292058563, 2.049880134335657189 ) ) ;
#20387=FACE_OUTER_BOUND ( 'NONE', #12249, .T. ) ;
#20391=CARTESIAN_POINT ( 'NONE',  ( 54.18344080464222401, 5.675363110172368053, 2.049999999999807532 ) ) ;
#20407=ORIENTED_EDGE ( 'NONE', *, *, #5661, .F. ) ;
#20420=CARTESIAN_POINT ( 'NONE',  ( 47.00000000000000711, 2.480048031931718505E-14, -4.200000000000156497 ) ) ;
#20424=CARTESIAN_POINT ( 'NONE',  ( 22.08710231755535958, 7.931663834300023197, 2.049999999999922995 ) ) ;
#20425=ORIENTED_EDGE ( 'NONE', *, *, #18598, .T. ) ;
#20436=CARTESIAN_POINT ( 'NONE',  ( 30.51261366513613993, 7.487866468533194819, -1.425000000000106404 ) ) ;
#20448=CARTESIAN_POINT ( 'NONE',  ( 53.66376481541391996, 4.683274397263343047, -2.050000000000186784 ) ) ;
#20458=CARTESIAN_POINT ( 'NONE',  ( 52.79212554374781519, 4.124817749204305883, -2.046663969066548905 ) ) ;
#20467=CARTESIAN_POINT ( 'NONE',  ( 47.19826578991445842, -3.901954665936025801, -1.539656138810913788 ) ) ;
#20472=CARTESIAN_POINT ( 'NONE',  ( 53.05468381831884273, 8.377149132718326285, 2.049999999999815081 ) ) ;
#20481=CARTESIAN_POINT ( 'NONE',  ( 52.00295751487188767, 4.370849658658843673, -1.433798655470523986 ) ) ;
#20505=ORIENTED_EDGE ( 'NONE', *, *, #7528, .T. ) ;
#20517=CIRCLE ( 'NONE', #11379, 159.6997717543496833 ) ;
#20521=DIRECTION ( 'NONE',  ( 3.083952846180964840E-15, 0.000000000000000000, 1.000000000000000000 ) ) ;
#20522=VERTEX_POINT ( 'NONE', #25817 ) ;
#20523=CARTESIAN_POINT ( 'NONE',  ( 25.06719628372713160, 5.330953183978783372, -1.950000000000088107 ) ) ;
#20525=CARTESIAN_POINT ( 'NONE',  ( 47.10000000000003695, -3.609862487194767322, 1.947526779790813123 ) ) ;
#20529=CARTESIAN_POINT ( 'NONE',  ( 47.00000000000002842, -3.637377585518695611, 2.099877210782872705 ) ) ;
#20535=DIRECTION ( 'NONE',  ( -3.489354422748178977E-15, 1.218509414717996338E-16, -1.000000000000000000 ) ) ;
#20545=CARTESIAN_POINT ( 'NONE',  ( 54.44772160268976791, 6.353385485843105585, 1.624999999999810374 ) ) ;
#20552=CARTESIAN_POINT ( 'NONE',  ( 51.75611399313425665, 4.330462468336024884, 1.549999999999819300 ) ) ;
#20557=DIRECTION ( 'NONE',  ( 3.489354422748178582E-15, -1.218509414717996338E-16, 1.000000000000000000 ) ) ;
#20559=AXIS2_PLACEMENT_3D ( 'NONE', #18938, #28580, #6892 ) ;
#20573=ORIENTED_EDGE ( 'NONE', *, *, #23358, .T. ) ;
#20594=CIRCLE ( 'NONE', #11464, 0.09999999999999992228 ) ;
#20598=CIRCLE ( 'NONE', #28674, 160.1997717543138720 ) ;
#20602=DIRECTION ( 'NONE',  ( -3.489354422748178582E-15, 1.218509414717996338E-16, -1.000000000000000000 ) ) ;
#20606=CARTESIAN_POINT ( 'NONE',  ( 53.31624996668935523, 4.986115460562799306, -1.613809080173747912 ) ) ;
#20607=AXIS2_PLACEMENT_3D ( 'NONE', #19352, #14414, #3862 ) ;
#20610=ADVANCED_FACE ( 'NONE', ( #31035 ), #5071, .T. ) ;
#20613=CARTESIAN_POINT ( 'NONE',  ( 53.34494210428216121, 4.987020249080381440, -2.050000000000185896 ) ) ;
#20616=CARTESIAN_POINT ( 'NONE',  ( 47.10000000000002274, 6.982261990806648555E-14, -1.632474749424821370E-13 ) ) ;
#20628=AXIS2_PLACEMENT_3D ( 'NONE', #15317, #8344, #8509 ) ;
#20629=DIRECTION ( 'NONE',  ( -0.9993908270190956511, 0.03489949670250096919, 3.491481338843132961E-15 ) ) ;
#20641=CARTESIAN_POINT ( 'NONE',  ( 48.00000000000001421, -4.387164041431065975, -1.383037119376926194 ) ) ;
#20648=EDGE_LOOP ( 'NONE', ( #12343, #665, #16862 ) ) ;
#20666=CARTESIAN_POINT ( 'NONE',  ( 53.14855870271264138, 8.298021504495151746, -2.050000000000184563 ) ) ;
#20672=CARTESIAN_POINT ( 'NONE',  ( 51.80000000000001137, 3.850000000000016520, -2.050000000000180123 ) ) ;
#20682=ORIENTED_EDGE ( 'NONE', *, *, #27975, .T. ) ;
#20685=CARTESIAN_POINT ( 'NONE',  ( 22.32354329421558958, 7.018810582754777982, -2.050000000000010036 ) ) ;
#20688=DIRECTION ( 'NONE',  ( -1.000000000000000000, -0.000000000000000000, 3.491481338843133355E-15 ) ) ;
#20694=CARTESIAN_POINT ( 'NONE',  ( 48.00000000000001421, -3.937842575352406005, 1.145831896685653328 ) ) ;
#20702=VECTOR ( 'NONE', #25458, 1000.000000000000000 ) ;
#20704=ORIENTED_EDGE ( 'NONE', *, *, #3963, .F. ) ;
#20705=CARTESIAN_POINT ( 'NONE',  ( 54.16356081880782369, 5.682032782862182607, -2.050000000000188116 ) ) ;
#20709=CARTESIAN_POINT ( 'NONE',  ( 51.80000000000002558, 8.700000000000107647, 2.049999999999819522 ) ) ;
#20717=CARTESIAN_POINT ( 'NONE',  ( 30.93632708544912902, 7.271619894357248093, -2.050000000000106848 ) ) ;
#20723=FACE_OUTER_BOUND ( 'NONE', #24575, .T. ) ;
#20736=CARTESIAN_POINT ( 'NONE',  ( 54.41366571437520605, 6.718673005292168376, -1.950000000000180256 ) ) ;
#20740=CIRCLE ( 'NONE', #2541, 0.09999999999999850675 ) ;
#20744=CARTESIAN_POINT ( 'NONE',  ( 51.80000000000001137, -4.387164041431065975, -1.383037119376939739 ) ) ;
#20746=DIRECTION ( 'NONE',  ( 3.491481338843133355E-15, 0.000000000000000000, 1.000000000000000000 ) ) ;
#20753=CARTESIAN_POINT ( 'NONE',  ( 26.19155409318044292, 5.638511060912941630, 1.424999999999907896 ) ) ;
#20754=DIRECTION ( 'NONE',  ( 0.9993908270190957621, -0.03489949670250202390, -3.491481338843133355E-15 ) ) ;
#20767=DIRECTION ( 'NONE',  ( 3.489354422748178582E-15, -1.218509414717996338E-16, 1.000000000000000000 ) ) ;
#20781=CARTESIAN_POINT ( 'NONE',  ( 51.87767605783387381, 8.699351266148434902, 2.049999999999819522 ) ) ;
#20792=CARTESIAN_POINT ( 'NONE',  ( 21.98769535799031161, 7.920638968848361827, 1.949999999999923794 ) ) ;
#20794=EDGE_LOOP ( 'NONE', ( #16303, #27124, #17128, #25755 ) ) ;
#20796=ORIENTED_EDGE ( 'NONE', *, *, #30159, .F. ) ;
#20816=CYLINDRICAL_SURFACE ( 'NONE', #1637, 2.125000000000043521 ) ;
#20822=CARTESIAN_POINT ( 'NONE',  ( 51.80000000000001137, -3.994701997234045177, -2.069753729861391722 ) ) ;
#20828=CARTESIAN_POINT ( 'NONE',  ( 23.38809389355835933, 6.107120497888152144, -2.050000000000081091 ) ) ;
#20836=CARTESIAN_POINT ( 'NONE',  ( 47.49328262214483232, -3.991926107141724245, 1.294864543653815314 ) ) ;
#20842=CARTESIAN_POINT ( 'NONE',  ( 51.69999998375428163, -4.079529477378105007, 2.128865254696994391 ) ) ;
#20845=DIRECTION ( 'NONE',  ( 3.489354422748178582E-15, -1.218509414717996338E-16, 1.000000000000000000 ) ) ;
#20853=CARTESIAN_POINT ( 'NONE',  ( 50.91843332348674522, -3.908336253171006636, 1.238913932502388571 ) ) ;
#20856=CARTESIAN_POINT ( 'NONE',  ( 53.66601923242430416, 4.681126589747570677, 2.049999999999812861 ) ) ;
#20858=DIRECTION ( 'NONE',  ( 3.489354422748178582E-15, -1.218509414717996338E-16, 1.000000000000000000 ) ) ;
#20859=CARTESIAN_POINT ( 'NONE',  ( 51.03845481666589734, -3.901365292554824560, -1.261477279112157568 ) ) ;
#20868=CARTESIAN_POINT ( 'NONE',  ( 48.00000000000001421, -3.657334280697314810, -2.105684202162501073 ) ) ;
#20869=VERTEX_POINT ( 'NONE', #22947 ) ;
#20878=ADVANCED_FACE ( 'NONE', ( #1236 ), #10897, .F. ) ;
#20880=CARTESIAN_POINT ( 'NONE',  ( 51.70000000000002416, 6.982261990806648555E-14, -1.793082891011605378E-13 ) ) ;
#20883=CARTESIAN_POINT ( 'NONE',  ( 52.27846493713558829, 4.392730452021146981, 1.555162895512434806 ) ) ;
#20902=CARTESIAN_POINT ( 'NONE',  ( 53.26700867189011745, 4.937278075622002937, -1.609149601427315890 ) ) ;
#20919=CARTESIAN_POINT ( 'NONE',  ( 47.00000000000000711, -3.933368109459638884, -2.186004417993338667 ) ) ;
#20926=CARTESIAN_POINT ( 'NONE',  ( 47.86726225955752767, -4.031600731908414836, -1.173113608511841655 ) ) ;
#20929=CARTESIAN_POINT ( 'NONE',  ( 53.05367528747408556, 8.375580747031632356, 2.049999999999815081 ) ) ;
#20932=ORIENTED_EDGE ( 'NONE', *, *, #9667, .T. ) ;
#20937=ORIENTED_EDGE ( 'NONE', *, *, #24517, .T. ) ;
#20941=ORIENTED_EDGE ( 'NONE', *, *, #20270, .F. ) ;
#20948=CARTESIAN_POINT ( 'NONE',  ( 51.80000000000002558, 4.286401202180091907, 1.833837317107078313 ) ) ;
#20951=LINE ( 'NONE', #29971, #13987 ) ;
#20978=CARTESIAN_POINT ( 'NONE',  ( 23.93127868632186050, 5.811091648296249801, -2.050000000000082867 ) ) ;
#21005=ORIENTED_EDGE ( 'NONE', *, *, #2248, .F. ) ;
#21007=CARTESIAN_POINT ( 'NONE',  ( 51.30663577364959593, -3.991980709735059918, 1.294710393269015603 ) ) ;
#21009=CARTESIAN_POINT ( 'NONE',  ( 53.87894805006524734, 4.971284855691957993, 2.049999999999811973 ) ) ;
#21015=ORIENTED_EDGE ( 'NONE', *, *, #14820, .T. ) ;
#21031=AXIS2_PLACEMENT_3D ( 'NONE', #15167, #3134, #27500 ) ;
#21043=( GEOMETRIC_REPRESENTATION_CONTEXT ( 3 ) GLOBAL_UNCERTAINTY_ASSIGNED_CONTEXT ( ( #12647 ) ) GLOBAL_UNIT_ASSIGNED_CONTEXT ( ( #8744, #3857, #1623 ) ) REPRESENTATION_CONTEXT ( 'NONE', 'WORKASPACE' ) );
#21046=CARTESIAN_POINT ( 'NONE',  ( 51.80000000000001847, 2.428612866367529932E-14, -1.808587333520743709E-13 ) ) ;
#21059=DIRECTION ( 'NONE',  ( 0.000000000000000000, 0.000000000000000000, -1.000000000000000000 ) ) ;
#21069=CARTESIAN_POINT ( 'NONE',  ( 53.38896854193014008, 5.061769990941914266, -1.621051239797380195 ) ) ;
#21080=DIRECTION ( 'NONE',  ( 3.352440544655105674E-15, 0.2793919678926571892, 0.9601771338024399638 ) ) ;
#21089=CARTESIAN_POINT ( 'NONE',  ( 47.49107765765781153, -4.380148595134368605, -1.408962902656728744 ) ) ;
#21093=ORIENTED_EDGE ( 'NONE', *, *, #14805, .F. ) ;
#21104=DIRECTION ( 'NONE',  ( 0.03489949670250203084, 0.9993908270190957621, -3.673133589935336920E-30 ) ) ;
#21105=EDGE_LOOP ( 'NONE', ( #20932, #201, #3693 ) ) ;
#21121=CIRCLE ( 'NONE', #9981, 4.199999999999993072 ) ;
#21126=CARTESIAN_POINT ( 'NONE',  ( 22.25735896772342315, 7.137076052088946909, -1.425000000000077538 ) ) ;
#21131=CIRCLE ( 'NONE', #7469, 0.09999999999999982514 ) ;
#21145=CARTESIAN_POINT ( 'NONE',  ( 22.54717926605044198, 7.740376438784147162, -1.425000000000078204 ) ) ;
#21157=CIRCLE ( 'NONE', #25176, 159.6997717543496833 ) ;
#21164=FACE_OUTER_BOUND ( 'NONE', #6129, .T. ) ;
#21166=ORIENTED_EDGE ( 'NONE', *, *, #26426, .F. ) ;
#21178=CARTESIAN_POINT ( 'NONE',  ( 48.00000000000001421, -3.908336260473453727, -1.238913909466087482 ) ) ;
#21185=CARTESIAN_POINT ( 'NONE',  ( 52.10572631149718603, 8.700000001568275465, 2.049999999999818190 ) ) ;
#21188=DIRECTION ( 'NONE',  ( 0.03489949670250097613, 0.9993908270190957621, 0.000000000000000000 ) ) ;
#21189=CARTESIAN_POINT ( 'NONE',  ( 50.91898013251472577, -3.908336255397554915, -1.238913925478770661 ) ) ;
#21193=ADVANCED_FACE ( 'NONE', ( #30181 ), #19530, .T. ) ;
#21198=ORIENTED_EDGE ( 'NONE', *, *, #10472, .T. ) ;
#21199=CARTESIAN_POINT ( 'NONE',  ( 53.35811189124944320, 7.919971434358604512, 1.887106088948682592 ) ) ;
#21224=ORIENTED_EDGE ( 'NONE', *, *, #14395, .T. ) ;
#21229=CARTESIAN_POINT ( 'NONE',  ( 51.67554083669129739, -4.150097527438617817, -1.728039211945292530 ) ) ;
#21251=DIRECTION ( 'NONE',  ( 3.489354422748178582E-15, -1.218509414717996338E-16, 1.000000000000000000 ) ) ;
#21253=CARTESIAN_POINT ( 'NONE',  ( 47.86761800069044881, -4.417905785811086616, -1.285520522240110930 ) ) ;
#21260=B_SPLINE_CURVE_WITH_KNOTS ( 'NONE', 3,
 ( #16708, #5121, #4802, #24432, #10039, #23977, #2743, #12389, #22079, #14462, #19707, #14154, #23828, #2118, #9413, #11781, #2272, #11937, #21624, #31260, #29809, #20481, #17791, #20176, #8122, #30104 ),
 .UNSPECIFIED., .F., .F.,
 ( 4, 2, 2, 2, 2, 2, 2, 2, 2, 2, 2, 2, 4 ),
 ( -0.001582486880272674767, -0.001533040430800264656, -0.001483593981327854545, -0.001384701082383033889, -0.001186915284493391927, -0.0007913436887141038836, -2.004971555299647767E-07, 0.0007909426944030439541, 0.001186514290182330480, 0.001384300088071973092, 0.001483192987016789411, 0.001532639436489198221, 0.001582085885961606597 ),
 .UNSPECIFIED. ) ;
#21273=EDGE_CURVE ( 'NONE', #27565, #9758, #4363, .T. ) ;
#21285=CARTESIAN_POINT ( 'NONE',  ( 22.20257169554297150, 7.242789023567405060, -1.425000000000076872 ) ) ;
#21297=CARTESIAN_POINT ( 'NONE',  ( 53.14824221617038802, 8.298223012065058413, 2.049999999999815081 ) ) ;
#21302=VECTOR ( 'NONE', #7976, 1000.000000000000114 ) ;
#21317=CYLINDRICAL_SURFACE ( 'NONE', #21792, 0.1000000000000000472 ) ;
#21340=CARTESIAN_POINT ( 'NONE',  ( 54.23225718638638426, 5.947176913004134313, 2.049999999999810640 ) ) ;
#21354=CARTESIAN_POINT ( 'NONE',  ( 52.35021482935074744, 8.543783160579959457, 1.945426946893610953 ) ) ;
#21356=CARTESIAN_POINT ( 'NONE',  ( 48.00000000000002842, -4.387164041431067751, 1.383037119376590685 ) ) ;
#21357=AXIS2_PLACEMENT_3D ( 'NONE', #11161, #16236, #13994 ) ;
#21361=VECTOR ( 'NONE', #27288, 1000.000000000000114 ) ;
#21366=DIRECTION ( 'NONE',  ( -1.000000000000000000, -0.000000000000000000, 3.491481338843133355E-15 ) ) ;
#21368=VERTEX_POINT ( 'NONE', #17623 ) ;
#21369=CARTESIAN_POINT ( 'NONE',  ( 51.80000000000002558, 6.475000000000061817, 1.949999999999818767 ) ) ;
#21382=CYLINDRICAL_SURFACE ( 'NONE', #10097, 159.6997717543496833 ) ;
#21388=DIRECTION ( 'NONE',  ( -1.000000000000000000, -0.000000000000000000, 3.491481338843133355E-15 ) ) ;
#21402=CARTESIAN_POINT ( 'NONE',  ( 47.21146949041553142, -4.227727696248180678, -1.816297733665433567 ) ) ;
#21421=CARTESIAN_POINT ( 'NONE',  ( 51.77489583516923233, -3.758927087870047146, -1.866445954014795516 ) ) ;
#21423=EDGE_CURVE ( 'NONE', #7964, #16445, #30839, .T. ) ;
#21427=CARTESIAN_POINT ( 'NONE',  ( 51.80000000000002558, 4.350000000000017408, 1.550321101314541927 ) ) ;
#21430=DIRECTION ( 'NONE',  ( -1.000000000000000000, -0.000000000000000000, 3.491481338843133355E-15 ) ) ;
#21433=DIRECTION ( 'NONE',  ( 3.384826294588897856E-15, 1.776356839400250465E-15, 1.000000000000000000 ) ) ;
#21445=CARTESIAN_POINT ( 'NONE',  ( 54.37322582291520234, 5.989334736793181513, -2.026384253567227400 ) ) ;
#21448=CARTESIAN_POINT ( 'NONE',  ( 22.72662675107781993, 7.272876594663812533, 1.424999999999920330 ) ) ;
#21450=CARTESIAN_POINT ( 'NONE',  ( 51.67569715750386905, -4.150085526745833420, 1.728112049830016206 ) ) ;
#21466=ADVANCED_FACE ( 'NONE', ( #4284 ), #23455, .T. ) ;
#21474=ADVANCED_FACE ( 'NONE', ( #30410 ), #25504, .F. ) ;
#21479=CARTESIAN_POINT ( 'NONE',  ( 51.80000000000002558, 4.350000000000017408, 1.495827530165114050 ) ) ;
#21480=VECTOR ( 'NONE', #10265, 1000.000000000000000 ) ;
#21482=VECTOR ( 'NONE', #16611, 1000.000000000000000 ) ;
#21518=CARTESIAN_POINT ( 'NONE',  ( 53.90752842026361691, 6.075960936770284704, -7.641258220787705557E-08 ) ) ;
#21519=ORIENTED_EDGE ( 'NONE', *, *, #24581, .T. ) ;
#21522=VECTOR ( 'NONE', #25136, 1000.000000000000000 ) ;
#21523=CARTESIAN_POINT ( 'NONE',  ( 51.03947097432633484, -4.379874851678565939, -1.406750166670766689 ) ) ;
#21524=CARTESIAN_POINT ( 'NONE',  ( 41.48619405471885102, -151.3359592902621955, 1.949999999999835865 ) ) ;
#21525=B_SPLINE_SURFACE_WITH_KNOTS ( 'NONE', 3, 1, ( 
 ( #31294, #7545 ),
 ( #5005, #16892 ),
 ( #19426, #29071 ),
 ( #12139, #24011 ),
 ( #2776, #19281 ),
 ( #26847, #24326 ),
 ( #14662, #26711 ),
 ( #2943, #2313 ),
 ( #24177, #5155 ) ),
 .UNSPECIFIED., .F., .F., .F.,
 ( 4, 1, 1, 1, 1, 1, 4 ),
 ( 2, 2 ),
 ( 0.000000000000000000, 0.08990530927501938496, 0.2069505209790863942, 0.2957249676700259844, 0.5865340158044511920, 0.7553074047937105018, 0.9940797213269729760 ),
 ( 0.000000000000000000, 1.000000000000000000 ),
 .UNSPECIFIED. ) ;
#21529=LINE ( 'NONE', #28482, #3525 ) ;
#21532=VERTEX_POINT ( 'NONE', #15850 ) ;
#21552=CARTESIAN_POINT ( 'NONE',  ( 50.83686442967773900, 8.734989671305513070, 2.049999999999822631 ) ) ;
#21556=AXIS2_PLACEMENT_3D ( 'NONE', #29425, #24520, #2997 ) ;
#21557=CARTESIAN_POINT ( 'NONE',  ( 47.73526966676922001, -4.311876499822751896, -1.282612398564092704 ) ) ;
#21563=FACE_OUTER_BOUND ( 'NONE', #16444, .T. ) ;
#21588=AXIS2_PLACEMENT_3D ( 'NONE', #6083, #10672, #8139 ) ;
#21599=CARTESIAN_POINT ( 'NONE',  ( 51.76858160943182696, 4.130187818440810510, -1.964805969893994586 ) ) ;
#21600=CARTESIAN_POINT ( 'NONE',  ( 47.09104525948219333, 9.165979422395388099, 2.049999999999835953 ) ) ;
#21603=VERTEX_POINT ( 'NONE', #28985 ) ;
#21605=CARTESIAN_POINT ( 'NONE',  ( 52.41144973999026746, 8.636710922408726177, 2.049999999999818190 ) ) ;
#21610=CARTESIAN_POINT ( 'NONE',  ( 54.21132576206891684, 6.699808777935940540, -2.050000000000189004 ) ) ;
#21612=CARTESIAN_POINT ( 'NONE',  ( 51.03629145313043125, -3.908336260473452839, -1.238913909466098362 ) ) ;
#21616=CARTESIAN_POINT ( 'NONE',  ( 23.27131915274574325, 6.595123925190213399, 1.424999999999919220 ) ) ;
#21619=AXIS2_PLACEMENT_3D ( 'NONE', #2096, #16686, #31064 ) ;
#21624=CARTESIAN_POINT ( 'NONE',  ( 51.89870775422352267, 4.414556427217972256, -1.294251603339130918 ) ) ;
#21627=ORIENTED_EDGE ( 'NONE', *, *, #19161, .T. ) ;
#21633=CARTESIAN_POINT ( 'NONE',  ( 28.70703846264724390, 5.747922415052714840, 2.049999999999641442 ) ) ;
#21640=DIRECTION ( 'NONE',  ( 3.384826294588897856E-15, 0.000000000000000000, 1.000000000000000000 ) ) ;
#21650=CARTESIAN_POINT ( 'NONE',  ( 52.54946733419073723, 4.465216787881786331, 2.049999999999816414 ) ) ;
#21660=FACE_OUTER_BOUND ( 'NONE', #20794, .T. ) ;
#21673=EDGE_LOOP ( 'NONE', ( #13334, #28838, #1756, #14737, #26384 ) ) ;
#21681=DIRECTION ( 'NONE',  ( 3.489354422748178582E-15, -1.218509414717996338E-16, 1.000000000000000000 ) ) ;
#21687=LINE ( 'NONE', #4703, #19441 ) ;
#21689=CARTESIAN_POINT ( 'NONE',  ( 53.94320330750939974, 6.378592095722332544, 0.8960560279709253173 ) ) ;
#21715=DIRECTION ( 'NONE',  ( 1.000000000000000000, 0.000000000000000000, -3.491481338843133355E-15 ) ) ;
#21716=CARTESIAN_POINT ( 'NONE',  ( 31.41368619715721877, 7.411258020427958115, -1.950000000000107869 ) ) ;
#21719=CARTESIAN_POINT ( 'NONE',  ( 52.35020563828505402, 8.543786098496177317, -1.945426797535727781 ) ) ;
#21723=LINE ( 'NONE', #26597, #1852 ) ;
#21745=ORIENTED_EDGE ( 'NONE', *, *, #25922, .F. ) ;
#21747=ORIENTED_EDGE ( 'NONE', *, *, #24969, .T. ) ;
#21750=AXIS2_PLACEMENT_3D ( 'NONE', #10318, #5110, #21920 ) ;
#21752=CARTESIAN_POINT ( 'NONE',  ( 53.90311770664829538, 7.548181632372875427, -2.050000000000187228 ) ) ;
#21759=B_SPLINE_CURVE_WITH_KNOTS ( 'NONE', 3,
 ( #4849, #12281, #2781, #14670 ),
 .UNSPECIFIED., .F., .F.,
 ( 4, 4 ),
 ( 0.000000000000000000, 0.0002896903389214072148 ),
 .UNSPECIFIED. ) ;
#21766=( BOUNDED_SURFACE ( )  B_SPLINE_SURFACE ( 3, 2, ( 
 ( #18461, #20379, #20529 ),
 ( #25563, #15618, #27799 ),
 ( #10549, #11162, #893 ),
 ( #20226, #6420, #5791 ),
 ( #15446, #30162, #18302 ),
 ( #8168, #3429, #29854 ),
 ( #24936, #25414, #20836 ),
 ( #1343, #3716, #6113 ),
 ( #10696, #22750, #30001 ),
 ( #8481, #20694, #30319 ) ),
 .UNSPECIFIED., .F., .F., .F. ) 
 B_SPLINE_SURFACE_WITH_KNOTS ( ( 4, 2, 2, 2, 4 ),
 ( 3, 3 ),
 ( -1.029992063861229212E-18, 0.0003537660104434874790, 0.0007075320208869760423, 0.001061298031330464714, 0.001415064041773953169 ),
 ( 0.000000000000000000, 1.000000000000000000 ),
 .UNSPECIFIED. ) 
 GEOMETRIC_REPRESENTATION_ITEM ( )  RATIONAL_B_SPLINE_SURFACE ( (
 ( 1.000000000000000000, 0.7071067811865467956, 1.000000000000000000),
 ( 1.000000000000000000, 0.7179295922952573239, 1.000000000000000000),
 ( 1.000000000000000000, 0.7246425758715731025, 1.000000000000000000),
 ( 1.000000000000000000, 0.7309548279203579302, 1.000000000000000000),
 ( 1.000000000000000000, 0.7305336397965990214, 1.000000000000000000),
 ( 1.000000000000000000, 0.7264835597184705618, 1.000000000000000000),
 ( 1.000000000000000000, 0.7229248932001940409, 1.000000000000000000),
 ( 1.000000000000000000, 0.7174039707112246367, 1.000000000000000000),
 ( 1.000000000000000000, 0.7154085637335746428, 1.000000000000000000),
 ( 1.000000000000000000, 0.7154752000627009334, 1.000000000000000000) ) ) 
 REPRESENTATION_ITEM ( '' )  SURFACE ( )  );
#21767=CARTESIAN_POINT ( 'NONE',  ( 51.89801475736550884, 4.350000000000017408, -1.495827530165608987 ) ) ;
#21768=CARTESIAN_POINT ( 'NONE',  ( 47.00000000000002132, -3.995252422878563969, -2.068710474281869605 ) ) ;
#21782=EDGE_LOOP ( 'NONE', ( #12050, #23003, #7166, #18329 ) ) ;
#21789=CARTESIAN_POINT ( 'NONE',  ( 51.87416143049283335, 8.598705507415685290, -1.950000000000180256 ) ) ;
#21790=CARTESIAN_POINT ( 'NONE',  ( 27.84544208433369405, 5.444976785341556713, 2.050000000000031353 ) ) ;
#21792=AXIS2_PLACEMENT_3D ( 'NONE', #1338, #20688, #6107 ) ;
#21803=CARTESIAN_POINT ( 'NONE',  ( 53.29207122288457299, 4.934008984266823994, 2.049999999999814193 ) ) ;
#21813=ORIENTED_EDGE ( 'NONE', *, *, #4785, .T. ) ;
#21816=FACE_OUTER_BOUND ( 'NONE', #14621, .T. ) ;
#21828=CARTESIAN_POINT ( 'NONE',  ( 54.23625105546377512, 6.534957249981562022, -2.050000000000189004 ) ) ;
#21837=B_SPLINE_CURVE_WITH_KNOTS ( 'NONE', 3,
 ( #26008, #16211, #4317, #6859 ),
 .UNSPECIFIED., .F., .F.,
 ( 4, 4 ),
 ( 0.6030138259287500802, 0.6725631453485761968 ),
 .UNSPECIFIED. ) ;
#21846=ORIENTED_EDGE ( 'NONE', *, *, #27126, .T. ) ;
#21848=CARTESIAN_POINT ( 'NONE',  ( 51.25952958126881498, -4.349936135048432462, -1.496764967787034717 ) ) ;
#21849=DIRECTION ( 'NONE',  ( -0.9993908270190956511, 0.03489949670250096919, 3.491481338843132961E-15 ) ) ;
#21850=VERTEX_POINT ( 'NONE', #24993 ) ;
#21853=CIRCLE ( 'NONE', #8170, 0.09999999999999850675 ) ;
#21867=EDGE_CURVE ( 'NONE', #12847, #4765, #10449, .T. ) ;
#21868=CARTESIAN_POINT ( 'NONE',  ( 51.80000000000001847, 6.982261990806648555E-14, -1.796574372350448449E-13 ) ) ;
#21872=CARTESIAN_POINT ( 'NONE',  ( 53.41816162339292617, 7.853362761740803499, -1.880937203427523574 ) ) ;
#21874=CARTESIAN_POINT ( 'NONE',  ( 50.31971926781693583, 8.252744006147214151, -2.050000000000174794 ) ) ;
#21889=AXIS2_PLACEMENT_3D ( 'NONE', #14175, #4196, #9281 ) ;
#21903=CARTESIAN_POINT ( 'NONE',  ( 53.88135321025246327, 4.969568719840013138, -2.050000000000188560 ) ) ;
#21905=DIRECTION ( 'NONE',  ( 0.9993908270190956511, -0.03489949670250096919, -3.491481338843132961E-15 ) ) ;
#21915=EDGE_CURVE ( 'NONE', #6782, #8007, #29266, .T. ) ;
#21920=DIRECTION ( 'NONE',  ( -0.9993908270190956511, 0.03489949670250096919, 3.491481338843132961E-15 ) ) ;
#21921=CARTESIAN_POINT ( 'NONE',  ( 22.06071280439821081, 8.185410187602871090, 1.949999999999922906 ) ) ;
#21936=CARTESIAN_POINT ( 'NONE',  ( 32.54904120526451550, 8.004085848662246150, 2.049999999999885691 ) ) ;
#21940=CARTESIAN_POINT ( 'NONE',  ( 53.05468381831882851, 8.377149132718326285, -2.050000000000184563 ) ) ;
#21958=ORIENTED_EDGE ( 'NONE', *, *, #7486, .F. ) ;
#21963=CARTESIAN_POINT ( 'NONE',  ( 33.39233489564305302, 8.222108905995247241, -2.050000000000115730 ) ) ;
#21971=CARTESIAN_POINT ( 'NONE',  ( 53.94440344817342492, 6.524635634306411802, -1.761196874214848052 ) ) ;
#21993=CARTESIAN_POINT ( 'NONE',  ( 34.56269065792915995, 8.313757757582562746, -1.950000000000119860 ) ) ;
#22007=DIRECTION ( 'NONE',  ( 3.016910393003118404E-15, 0.000000000000000000, 1.000000000000000000 ) ) ;
#22009=CARTESIAN_POINT ( 'NONE',  ( 22.08866779209807873, 7.467293579578107909, -1.950000000000077005 ) ) ;
#22017=CARTESIAN_POINT ( 'NONE',  ( 23.49584529083620765, 5.910990189302488318, 1.424999999999918554 ) ) ;
#22019=CARTESIAN_POINT ( 'NONE',  ( 51.80000000000001847, 2.428612866367529932E-14, -1.808587333520743709E-13 ) ) ;
#22020=ORIENTED_EDGE ( 'NONE', *, *, #11056, .T. ) ;
#22021=CARTESIAN_POINT ( 'NONE',  ( 51.80000000000001137, 4.287867059355201071, -1.832567882403405068 ) ) ;
#22026=ORIENTED_EDGE ( 'NONE', *, *, #5182, .F. ) ;
#22040=EDGE_CURVE ( 'NONE', #22071, #17711, #7576, .T. ) ;
#22047=VECTOR ( 'NONE', #1544, 1000.000000000000114 ) ;
#22051=FACE_OUTER_BOUND ( 'NONE', #23354, .T. ) ;
#22064=DIRECTION ( 'NONE',  ( -3.489354422748178188E-15, 1.218509414717996091E-16, -1.000000000000000000 ) ) ;
#22065=FACE_OUTER_BOUND ( 'NONE', #23150, .T. ) ;
#22071=VERTEX_POINT ( 'NONE', #16774 ) ;
#22079=CARTESIAN_POINT ( 'NONE',  ( 51.87915152462694124, 4.432914534380794080, 1.230195908850218123 ) ) ;
#22082=AXIS2_PLACEMENT_3D ( 'NONE', #18749, #16688, #26175 ) ;
#22086=CARTESIAN_POINT ( 'NONE',  ( 33.40812713681398805, 8.122903765862725223, 2.049999999999884803 ) ) ;
#22090=AXIS2_PLACEMENT_3D ( 'NONE', #11168, #1191, #13364 ) ;
#22107=TOROIDAL_SURFACE ( 'NONE', #20100, 4.500000000000037303, 0.1000000000000000056 ) ;
#22112=AXIS2_PLACEMENT_3D ( 'NONE', #11018, #6421, #16083 ) ;
#22120=CARTESIAN_POINT ( 'NONE',  ( 51.80000000000001847, 2.428612866367529932E-14, -1.808587333520743709E-13 ) ) ;
#22122=CARTESIAN_POINT ( 'NONE',  ( 34.56702326949724835, 8.213851659285211326, -1.950000000000119860 ) ) ;
#22130=CARTESIAN_POINT ( 'NONE',  ( 54.17887612135720588, 6.867997567695679706, -2.050000000000189004 ) ) ;
#22133=DIRECTION ( 'NONE',  ( 0.03489949670250097613, 0.9993908270190957621, 0.000000000000000000 ) ) ;
#22143=DIRECTION ( 'NONE',  ( 0.9957419851084058360, 0.09218405009746234724, -4.336808689941986970E-15 ) ) ;
#22151=CARTESIAN_POINT ( 'NONE',  ( 50.92088486138060688, -4.387164041431067751, 1.383037119376580470 ) ) ;
#22157=CARTESIAN_POINT ( 'NONE',  ( 52.44060252733988392, 4.003370659767288231, 2.045783712298512746 ) ) ;
#22166=DIRECTION ( 'NONE',  ( -0.9993908270190956511, 0.03489949670250089980, 3.491481338843132961E-15 ) ) ;
#22171=DIRECTION ( 'NONE',  ( -1.000000000000000000, -0.000000000000000000, 3.491481338843133355E-15 ) ) ;
#22177=CARTESIAN_POINT ( 'NONE',  ( 27.10659297677966961, 5.279073180725294634, 1.424999999999906564 ) ) ;
#22193=CARTESIAN_POINT ( 'NONE',  ( 47.12400663174540938, -3.859587729118648447, 1.644141655454772977 ) ) ;
#22194=ORIENTED_EDGE ( 'NONE', *, *, #1099, .F. ) ;
#22211=DIRECTION ( 'NONE',  ( 1.000000000000000000, 0.000000000000000000, -3.491481338843133355E-15 ) ) ;
#22221=CARTESIAN_POINT ( 'NONE',  ( 51.71305322616575495, 3.851407826495535591, 1.405937361346973224 ) ) ;
#22231=EDGE_LOOP ( 'NONE', ( #12136, #10755, #27429, #7342 ) ) ;
#22237=CARTESIAN_POINT ( 'NONE',  ( 33.82794497195008887, 8.157778427462202941, 1.949999999999882050 ) ) ;
#22243=DIRECTION ( 'NONE',  ( -1.000000000000000000, -0.000000000000000000, 3.491481338843133355E-15 ) ) ;
#22249=CYLINDRICAL_SURFACE ( 'NONE', #11439, 0.1000000000000000472 ) ;
#22256=LINE ( 'NONE', #9747, #26601 ) ;
#22264=VERTEX_POINT ( 'NONE', #10574 ) ;
#22265=CARTESIAN_POINT ( 'NONE',  ( 51.80000000000001137, 6.475000000000062705, -2.050000000000180123 ) ) ;
#22271=CARTESIAN_POINT ( 'NONE',  ( 51.25562636158013419, -4.350642226022881864, -1.494686490729537409 ) ) ;
#22276=CARTESIAN_POINT ( 'NONE',  ( 27.52339381994850953, 5.460762561607475085, -2.050000000000095746 ) ) ;
#22282=CARTESIAN_POINT ( 'NONE',  ( 54.17703590114059153, 6.867671797591380134, -2.050000000000188560 ) ) ;
#22284=CARTESIAN_POINT ( 'NONE',  ( 47.02542275843954656, -3.759243154119187302, -1.865745259404487655 ) ) ;
#22296=CARTESIAN_POINT ( 'NONE',  ( 54.41366571437522026, 6.718673005292168376, 0.9749999999998122391 ) ) ;
#22313=CARTESIAN_POINT ( 'NONE',  ( 50.35762544161296006, 8.151359338959888845, 1.949999999999825206 ) ) ;
#22317=FACE_OUTER_BOUND ( 'NONE', #30481, .T. ) ;
#22323=DIRECTION ( 'NONE',  ( 3.051840300662039536E-15, 0.4857787595540328796, 0.8740818021021518058 ) ) ;
#22328=VERTEX_POINT ( 'NONE', #27664 ) ;
#22350=CARTESIAN_POINT ( 'NONE',  ( 51.38825337055898501, 3.875334094704443899, -2.050000000000178790 ) ) ;
#22363=ORIENTED_EDGE ( 'NONE', *, *, #26168, .F. ) ;
#22366=CARTESIAN_POINT ( 'NONE',  ( 47.00000000000001421, -3.933368109459638884, -2.186004417993339111 ) ) ;
#22367=DIRECTION ( 'NONE',  ( 1.000000000000000000, 0.000000000000000000, -3.491481338843133355E-15 ) ) ;
#22368=CARTESIAN_POINT ( 'NONE',  ( 52.36968054666201056, 3.911638213474379011, -1.229829597898885130 ) ) ;
#22374=LINE ( 'NONE', #13016, #8345 ) ;
#22380=CARTESIAN_POINT ( 'NONE',  ( 29.90503599876537777, 6.470972976943354382, 1.949999999999894040 ) ) ;
#22393=CIRCLE ( 'NONE', #29444, 4.600000000000036948 ) ;
#22394=CARTESIAN_POINT ( 'NONE',  ( 51.80000000000001137, -4.291790910095606648, -1.352971095042662553 ) ) ;
#22403=EDGE_LOOP ( 'NONE', ( #30755, #19983, #15887, #28560 ) ) ;
#22407=FACE_OUTER_BOUND ( 'NONE', #12518, .T. ) ;
#22413=VERTEX_POINT ( 'NONE', #16260 ) ;
#22417=ORIENTED_EDGE ( 'NONE', *, *, #5241, .F. ) ;
#22418=CARTESIAN_POINT ( 'NONE',  ( 25.99900894223008763, 5.212247165294384921, -1.950000000000091438 ) ) ;
#22419=EDGE_CURVE ( 'NONE', #9403, #28571, #10868, .T. ) ;
#22422=ORIENTED_EDGE ( 'NONE', *, *, #24476, .T. ) ;
#22426=CARTESIAN_POINT ( 'NONE',  ( 51.65313719492860400, 3.829415913202794286, -2.050000000000180123 ) ) ;
#22428=CARTESIAN_POINT ( 'NONE',  ( 47.76297833550881222, -3.901511898670463108, -1.261029562208496824 ) ) ;
#22434=CARTESIAN_POINT ( 'NONE',  ( 51.80000000000001847, 2.428612866367529932E-14, -1.808587333520743709E-13 ) ) ;
#22439=CARTESIAN_POINT ( 'NONE',  ( 54.28770169842803028, 6.706929334265034903, 2.049999999999810196 ) ) ;
#22447=FACE_OUTER_BOUND ( 'NONE', #21673, .T. ) ;
#22449=EDGE_CURVE ( 'NONE', #5154, #21603, #27747, .T. ) ;
#22463=CARTESIAN_POINT ( 'NONE',  ( 51.80000000000001137, 6.475000000000062705, -1.950000000000180256 ) ) ;
#22473=CARTESIAN_POINT ( 'NONE',  ( 22.11595495846478343, 7.781273941107792247, 2.049999999999922107 ) ) ;
#22487=ORIENTED_EDGE ( 'NONE', *, *, #30491, .F. ) ;
#22506=DIRECTION ( 'NONE',  ( 0.000000000000000000, 0.000000000000000000, -1.000000000000000000 ) ) ;
#22519=ORIENTED_EDGE ( 'NONE', *, *, #10477, .F. ) ;
#22529=CARTESIAN_POINT ( 'NONE',  ( 47.10000000000000853, -4.020776289669854009, -2.234582293948742748 ) ) ;
#22531=CARTESIAN_POINT ( 'NONE',  ( 26.83497762440962120, 5.238776824946374866, 1.949999999999906031 ) ) ;
#22537=CIRCLE ( 'NONE', #21031, 0.1000000000000000472 ) ;
#22539=CARTESIAN_POINT ( 'NONE',  ( 24.76493886329451399, 5.404133871416378021, 1.949999999999914468 ) ) ;
#22551=DIRECTION ( 'NONE',  ( -3.352440544655105674E-15, 0.2793919678926571892, -0.9601771338024399638 ) ) ;
#22573=VECTOR ( 'NONE', #6542, 1000.000000000000114 ) ;
#22575=CARTESIAN_POINT ( 'NONE',  ( 50.91833842830035906, -4.387164033828486076, -1.383037143493254240 ) ) ;
#22581=CARTESIAN_POINT ( 'NONE',  ( 30.98482657477733682, 7.184130536712149073, -2.050000000000107292 ) ) ;
#22589=FACE_OUTER_BOUND ( 'NONE', #24214, .T. ) ;
#22600=DIRECTION ( 'NONE',  ( -1.000000000000000000, -0.000000000000000000, 3.491481338843133355E-15 ) ) ;
#22601=CIRCLE ( 'NONE', #8927, 2.525000000001609290 ) ;
#22606=CARTESIAN_POINT ( 'NONE',  ( 54.40859248998804532, 6.718200026737121355, 1.988253682540942258 ) ) ;
#22612=B_SPLINE_CURVE_WITH_KNOTS ( 'NONE', 3,
 ( #2547, #29287, #29128, #24235, #29427, #4908, #307, #31201, #9529, #19190 ),
 .UNSPECIFIED., .F., .F.,
 ( 4, 2, 2, 2, 4 ),
 ( 0.000000000000000000, 0.0003520942986628438666, 0.0007041885973256877332, 0.001056282895988531600, 0.001408377194651375466 ),
 .UNSPECIFIED. ) ;
#22627=LINE ( 'NONE', #12626, #11493 ) ;
#22644=ADVANCED_FACE ( 'NONE', ( #10366 ), #14172, .T. ) ;
#22648=ADVANCED_FACE ( 'NONE', ( #24924 ), #6194, .T. ) ;
#22675=CARTESIAN_POINT ( 'NONE',  ( 52.91918222397608673, 8.304852724747799897, -1.919164453910518375 ) ) ;
#22685=CARTESIAN_POINT ( 'NONE',  ( 51.70000000000003837, 2.428612866367529932E-14, 4.099999999999812239 ) ) ;
#22689=EDGE_LOOP ( 'NONE', ( #30965, #15512, #13463, #26048 ) ) ;
#22695=ORIENTED_EDGE ( 'NONE', *, *, #3100, .F. ) ;
#22696=CARTESIAN_POINT ( 'NONE',  ( 54.21471704787897750, 5.862036637490150248, 2.049999999999810640 ) ) ;
#22711=CARTESIAN_POINT ( 'NONE',  ( 21.97322666366011035, 8.076925076899389211, 1.949999999999923128 ) ) ;
#22713=( GEOMETRIC_REPRESENTATION_CONTEXT ( 3 ) GLOBAL_UNCERTAINTY_ASSIGNED_CONTEXT ( ( #16807 ) ) GLOBAL_UNIT_ASSIGNED_CONTEXT ( ( #12517, #12351, #7308 ) ) REPRESENTATION_CONTEXT ( 'NONE', 'WORKASPACE' ) );
#22727=CARTESIAN_POINT ( 'NONE',  ( 53.25930982050607554, 8.220062413181228322, -2.050000000000184563 ) ) ;
#22730=AXIS2_PLACEMENT_3D ( 'NONE', #3518, #5892, #8865 ) ;
#22732=ORIENTED_EDGE ( 'NONE', *, *, #23940, .T. ) ;
#22733=CYLINDRICAL_SURFACE ( 'NONE', #17948, 2.625000000001612044 ) ;
#22737=CARTESIAN_POINT ( 'NONE',  ( 47.73715617352264218, -4.312058781922654127, 1.282041952413738306 ) ) ;
#22740=CARTESIAN_POINT ( 'NONE',  ( 53.82818350034567345, 5.794550817852396563, -1.819853284099130608 ) ) ;
#22744=CARTESIAN_POINT ( 'NONE',  ( 22.09542497196754951, 7.445411295443247646, -1.950000000000144285 ) ) ;
#22745=CARTESIAN_POINT ( 'NONE',  ( 50.80000000000001847, -4.003661535119149129, -1.169131321892095565 ) ) ;
#22750=CARTESIAN_POINT ( 'NONE',  ( 47.86807216729960146, -3.937842570012147103, 1.145831914963004960 ) ) ;
#22751=PRODUCT_DEFINITION_FORMATION_WITH_SPECIFIED_SOURCE ( 'ANY', '', #7773, .NOT_KNOWN. ) ;
#22759=CARTESIAN_POINT ( 'NONE',  ( 51.06473033323084820, -4.311876499822710151, 1.282612398563742095 ) ) ;
#22764=ORIENTED_EDGE ( 'NONE', *, *, #17320, .F. ) ;
#22767=CARTESIAN_POINT ( 'NONE',  ( 54.27127970009382096, 6.003218211144689676, 2.049999999999811084 ) ) ;
#22782=CARTESIAN_POINT ( 'NONE',  ( 51.80000000000002558, 6.475000000000061817, 2.049999999999819522 ) ) ;
#22786=DIRECTION ( 'NONE',  ( -1.000000000000000000, -0.000000000000000000, 3.491481338843133355E-15 ) ) ;
#22791=AXIS2_PLACEMENT_3D ( 'NONE', #26717, #255, #2947 ) ;
#22806=CARTESIAN_POINT ( 'NONE',  ( 29.92080114924054968, 6.605317672619497316, 2.049999999999895461 ) ) ;
#22813=ORIENTED_EDGE ( 'NONE', *, *, #6582, .F. ) ;
#22825=EDGE_CURVE ( 'NONE', #28370, #12339, #30782, .T. ) ;
#22829=CARTESIAN_POINT ( 'NONE',  ( 54.16188382698977222, 6.950389949135505674, -2.050000000000188560 ) ) ;
#22833=CARTESIAN_POINT ( 'NONE',  ( 51.80000000000001137, 4.350000000000017408, -2.050000000000180123 ) ) ;
#22836=DIRECTION ( 'NONE',  ( 3.491481338843133355E-15, -0.000000000000000000, 1.000000000000000000 ) ) ;
#22846=CARTESIAN_POINT ( 'NONE',  ( 53.93792434297150606, 7.473468098462469733, 2.049999999999811973 ) ) ;
#22849=CARTESIAN_POINT ( 'NONE',  ( 21.97286177946902797, 8.089633431579400735, -1.950000000000075895 ) ) ;
#22856=CARTESIAN_POINT ( 'NONE',  ( 50.35762544161294585, 8.151359338959888845, -1.950000000000174927 ) ) ;
#22859=VERTEX_POINT ( 'NONE', #11779 ) ;
#22870=CARTESIAN_POINT ( 'NONE',  ( 50.80657076746749112, 8.706740374280103723, 1.949999999999822764 ) ) ;
#22874=CARTESIAN_POINT ( 'NONE',  ( 51.80000000000001137, 6.475000000000062705, -2.050000000000180123 ) ) ;
#22885=ORIENTED_EDGE ( 'NONE', *, *, #9811, .T. ) ;
#22890=CARTESIAN_POINT ( 'NONE',  ( 51.72405698199537483, 3.851083960639936077, -1.414090016722021614 ) ) ;
#22902=CARTESIAN_POINT ( 'NONE',  ( 51.80000000000002558, 3.949999999998452971, 1.949999999999818767 ) ) ;
#22911=CARTESIAN_POINT ( 'NONE',  ( 54.28867365409866608, 5.640057820322917692, -1.843143693225357538E-13 ) ) ;
#22914=CARTESIAN_POINT ( 'NONE',  ( 51.67711951922819225, -3.662677325876138035, 1.845585774149405944 ) ) ;
#22927=FACE_OUTER_BOUND ( 'NONE', #20130, .T. ) ;
#22928=ORIENTED_EDGE ( 'NONE', *, *, #18116, .F. ) ;
#22947=CARTESIAN_POINT ( 'NONE',  ( 51.70000000000000995, 7.038595743567426471E-14, -4.600000000000215472 ) ) ;
#22952=CARTESIAN_POINT ( 'NONE',  ( 53.96142581635486124, 5.170113101904351360, 2.049999999999811529 ) ) ;
#22956=EDGE_CURVE ( 'NONE', #19244, #9597, #7353, .T. ) ;
#22957=CARTESIAN_POINT ( 'NONE',  ( 24.57460841532291695, 5.893272594507614315, 1.424999999999913447 ) ) ;
#22963=DIRECTION ( 'NONE',  ( 0.000000000000000000, 0.2793919678926571337, 0.9601771338024398528 ) ) ;
#22964=( NAMED_UNIT ( * ) PLANE_ANGLE_UNIT ( ) SI_UNIT ( $, .RADIAN. ) );
#22968=CARTESIAN_POINT ( 'NONE',  ( 53.16217804548191594, 8.131925109091586279, -1.902110155464870944 ) ) ;
#22979=CARTESIAN_POINT ( 'NONE',  ( 53.43485098824196911, 4.477779790996729403, -2.048706274183198506 ) ) ;
#22990=CARTESIAN_POINT ( 'NONE',  ( 54.17887612135722009, 6.867997567695679706, 2.049999999999811973 ) ) ;
#22992=B_SPLINE_CURVE_WITH_KNOTS ( 'NONE', 3,
 ( #20352, #12873, #8141, #17814, #27451, #15419 ),
 .UNSPECIFIED., .F., .F.,
 ( 4, 2, 4 ),
 ( 3.337428612691802767E-06, 0.0002849599470117442990, 0.0005665824654107963184 ),
 .UNSPECIFIED. ) ;
#22993=ORIENTED_EDGE ( 'NONE', *, *, #6018, .F. ) ;
#22997=ORIENTED_EDGE ( 'NONE', *, *, #10698, .F. ) ;
#23003=ORIENTED_EDGE ( 'NONE', *, *, #3201, .T. ) ;
#23006=ORIENTED_EDGE ( 'NONE', *, *, #2711, .F. ) ;
#23009=CARTESIAN_POINT ( 'NONE',  ( 50.80000000000002558, -3.908336260473453727, 1.238913909465742202 ) ) ;
#23010=CARTESIAN_POINT ( 'NONE',  ( 23.09424125814508244, 6.161968159343408580, -1.425000000000080647 ) ) ;
#23022=CARTESIAN_POINT ( 'NONE',  ( 53.96623127887670535, 7.375919661206682854, -2.050000000000187228 ) ) ;
#23033=CARTESIAN_POINT ( 'NONE',  ( 47.10000000000000853, 2.479435708532144956E-14, -4.100000000000157740 ) ) ;
#23035=ORIENTED_EDGE ( 'NONE', *, *, #5092, .T. ) ;
#23041=VERTEX_POINT ( 'NONE', #17933 ) ;
#23042=CARTESIAN_POINT ( 'NONE',  ( 25.69798005928776874, 5.334073409756094009, -2.050000000000088640 ) ) ;
#23056=CARTESIAN_POINT ( 'NONE',  ( 51.80000000000003268, -3.933368109459640660, 2.186004417992994053 ) ) ;
#23060=CIRCLE ( 'NONE', #24071, 4.500000000000037303 ) ;
#23062=DIRECTION ( 'NONE',  ( 1.000000000000000000, 0.000000000000000000, -3.491481338843133355E-15 ) ) ;
#23069=CARTESIAN_POINT ( 'NONE',  ( 50.93159257904724058, -4.031600731367472434, 1.173113608354092730 ) ) ;
#23071=COLOUR_RGB ( '', 0.31764706, 0.68627451, 0.89019608) ;
#23072=CARTESIAN_POINT ( 'NONE',  ( 51.80000000000002558, 8.600000000000108002, 1.949999999999818767 ) ) ;
#23078=CARTESIAN_POINT ( 'NONE',  ( 29.93623257617671030, 6.616414062163364029, -2.050000000000104183 ) ) ;
#23079=EDGE_CURVE ( 'NONE', #6282, #20869, #22393, .T. ) ;
#23104=AXIS2_PLACEMENT_3D ( 'NONE', #29369, #17341, #26987 ) ;
#23112=CIRCLE ( 'NONE', #15000, 0.1000000000000000472 ) ;
#23119=VERTEX_POINT ( 'NONE', #3983 ) ;
#23147=CARTESIAN_POINT ( 'NONE',  ( 52.54176024732381478, 4.030513272393515756, -2.045987183813463783 ) ) ;
#23150=EDGE_LOOP ( 'NONE', ( #5300, #26228, #14179, #4872 ) ) ;
#23158=CARTESIAN_POINT ( 'NONE',  ( 53.60009913848112717, 4.619321414059948339, 2.049999999999812861 ) ) ;
#23167=CARTESIAN_POINT ( 'NONE',  ( 47.43974768990582902, -4.327031471043519595, -1.563408443049195018 ) ) ;
#23179=CARTESIAN_POINT ( 'NONE',  ( 25.71580480958624193, 5.235626398479810817, -1.425000000000088862 ) ) ;
#23183=PLANE ( 'NONE',  #5407 ) ;
#23196=ORIENTED_EDGE ( 'NONE', *, *, #28366, .T. ) ;
#23203=CARTESIAN_POINT ( 'NONE',  ( 51.69999999079093556, -4.079797993893543584, -2.128382101831790330 ) ) ;
#23213=DIRECTION ( 'NONE',  ( 3.489354422748178582E-15, -1.218509414717996338E-16, 1.000000000000000000 ) ) ;
#23218=CARTESIAN_POINT ( 'NONE',  ( 53.81456879268866800, 5.799118509429035839, -1.784594539754255749 ) ) ;
#23222=LINE ( 'NONE', #1357, #29118 ) ;
#23227=CARTESIAN_POINT ( 'NONE',  ( 54.11187982984932887, 5.509389740176599659, -2.050000000000188560 ) ) ;
#23228=ORIENTED_EDGE ( 'NONE', *, *, #30506, .F. ) ;
#23230=CARTESIAN_POINT ( 'NONE',  ( 51.60235211085279161, -3.901663320877444718, 1.540393549661617456 ) ) ;
#23232=CARTESIAN_POINT ( 'NONE',  ( 53.55869261961985472, 7.702978059423599255, 1.861455469535095331 ) ) ;
#23239=CARTESIAN_POINT ( 'NONE',  ( 24.21343478405543692, 5.692107421281859203, -2.050000000000083755 ) ) ;
#23258=EDGE_CURVE ( 'NONE', #15457, #28051, #15804, .T. ) ;
#23262=CARTESIAN_POINT ( 'NONE',  ( 53.31625799375803609, 4.986123645165291940, 1.613809813132785820 ) ) ;
#23264=ORIENTED_EDGE ( 'NONE', *, *, #22956, .T. ) ;
#23275=SPHERICAL_SURFACE ( 'NONE', #485, 0.1000000000000000056 ) ;
#23288=DIRECTION ( 'NONE',  ( 0.03489949670247565611, 0.9993908270190966503, 0.000000000000000000 ) ) ;
#23297=LINE ( 'NONE', #3966, #15977 ) ;
#23307=CARTESIAN_POINT ( 'NONE',  ( 53.05088594538233338, 4.168914605591084843, 2.049999999999814637 ) ) ;
#23309=VERTEX_POINT ( 'NONE', #2674 ) ;
#23323=CARTESIAN_POINT ( 'NONE',  ( 26.87602198329691916, 5.247164978609347052, -1.425000000000093747 ) ) ;
#23327=B_SPLINE_CURVE_WITH_KNOTS ( 'NONE', 3,
 ( #24418, #21767, #2728, #19063 ),
 .UNSPECIFIED., .F., .F.,
 ( 4, 4 ),
 ( 0.000000000000000000, 0.0002896601805182694557 ),
 .UNSPECIFIED. ) ;
#23336=CARTESIAN_POINT ( 'NONE',  ( 53.91574522233626965, 6.672251602764244893, -1.774295313897662485 ) ) ;
#23341=SURFACE_STYLE_FILL_AREA ( #25708 ) ;
#23348=CARTESIAN_POINT ( 'NONE',  ( 51.67698846994527173, -4.134673935618214280, -2.019140663350203369 ) ) ;
#23354=EDGE_LOOP ( 'NONE', ( #22363, #5989, #30416, #22695 ) ) ;
#23355=CARTESIAN_POINT ( 'NONE',  ( 24.21299357973748201, 5.692280404210901423, -2.050000000000084199 ) ) ;
#23358=EDGE_CURVE ( 'NONE', #24179, #17195, #1130, .T. ) ;
#23371=CARTESIAN_POINT ( 'NONE',  ( 51.67614500439950831, -4.149773407329040431, 1.728861777175572101 ) ) ;
#23373=AXIS2_PLACEMENT_3D ( 'NONE', #14474, #17026, #24146 ) ;
#23375=DIRECTION ( 'NONE',  ( -0.9993908270190957621, 0.03489949670250100389, 3.491481338843133355E-15 ) ) ;
#23376=VERTEX_POINT ( 'NONE', #21479 ) ;
#23381=ADVANCED_FACE ( 'NONE', ( #10737 ), #4357, .F. ) ;
#23382=CARTESIAN_POINT ( 'NONE',  ( 54.23473434925104897, 6.620089622897159742, 2.049999999999810640 ) ) ;
#23386=ORIENTED_EDGE ( 'NONE', *, *, #19161, .F. ) ;
#23396=VERTEX_POINT ( 'NONE', #26215 ) ;
#23400=CARTESIAN_POINT ( 'NONE',  ( 47.27530108852192114, -4.265589706924724389, 1.723997649431065149 ) ) ;
#23405=VECTOR ( 'NONE', #14991, 1000.000000000000000 ) ;
#23410=EDGE_CURVE ( 'NONE', #26766, #10675, #26047, .T. ) ;
#23412=CARTESIAN_POINT ( 'NONE',  ( 53.30600611140961576, 4.975802279707719045, 1.612825013952412956 ) ) ;
#23419=LINE ( 'NONE', #20744, #18791 ) ;
#23434=DIRECTION ( 'NONE',  ( 0.9480661539417378769, -0.3180732113053867383, -3.310155284476359054E-15 ) ) ;
#23455=CYLINDRICAL_SURFACE ( 'NONE', #6265, 0.1000000000000000472 ) ;
#23483=ORIENTED_EDGE ( 'NONE', *, *, #8840, .F. ) ;
#23487=DIRECTION ( 'NONE',  ( -3.491481338843133355E-15, 0.000000000000000000, -1.000000000000000000 ) ) ;
#23489=LINE ( 'NONE', #21145, #730 ) ;
#23492=EDGE_LOOP ( 'NONE', ( #12505, #11195, #26222, #5331 ) ) ;
#23498=FACE_OUTER_BOUND ( 'NONE', #5868, .T. ) ;
#23533=CARTESIAN_POINT ( 'NONE',  ( 51.80000000000003268, 8.600000000000104450, 2.049999999999819522 ) ) ;
#23544=CARTESIAN_POINT ( 'NONE',  ( 22.06071280439819660, 8.185410187602871090, -1.950000000000076339 ) ) ;
#23548=CARTESIAN_POINT ( 'NONE',  ( 53.45668161578581845, 7.806773462440032674, 1.876589663053878088 ) ) ;
#23549=B_SPLINE_CURVE_WITH_KNOTS ( 'NONE', 3,
 ( #9040, #2068, #11882, #9358 ),
 .UNSPECIFIED., .F., .F.,
 ( 4, 4 ),
 ( 0.000000000000000000, 1.000000000000000000 ),
 .UNSPECIFIED. ) ;
#23555=ADVANCED_FACE ( 'NONE', ( #546 ), #31268, .T. ) ;
#23560=CARTESIAN_POINT ( 'NONE',  ( 41.48619405472010158, -151.3359592902261852, -1.425000000000163691 ) ) ;
#23569=DIRECTION ( 'NONE',  ( -1.000000000000000000, 0.000000000000000000, 3.491481338843133355E-15 ) ) ;
#23577=DIRECTION ( 'NONE',  ( -3.491481338843133355E-15, 0.000000000000000000, -1.000000000000000000 ) ) ;
#23581=EDGE_LOOP ( 'NONE', ( #4066, #3766, #20682, #1339, #6819, #5152, #2152, #30516, #3405, #10132 ) ) ;
#23594=( BOUNDED_SURFACE ( )  B_SPLINE_SURFACE ( 3, 2, ( 
 ( #200, #7782, #10031 ),
 ( #27265, #659, #29468 ),
 ( #17003, #5583, #17302 ),
 ( #2888, #19537, #10319 ),
 ( #3194, #9862, #19988 ),
 ( #17452, #7955, #24878 ),
 ( #24422, #7332, #29183 ),
 ( #5421, #12836, #2732 ),
 ( #58, #12377, #27101 ),
 ( #362, #19380, #19696 ) ),
 .UNSPECIFIED., .F., .F., .F. ) 
 B_SPLINE_SURFACE_WITH_KNOTS ( ( 4, 2, 2, 2, 4 ),
 ( 3, 3 ),
 ( -4.878909776184769953E-18, 0.0003534454412679785659, 0.0007068908825359620108, 0.001060336323803945293, 0.001413781765071928792 ),
 ( 0.000000000000000000, 1.000000000000000000 ),
 .UNSPECIFIED. ) 
 GEOMETRIC_REPRESENTATION_ITEM ( )  RATIONAL_B_SPLINE_SURFACE ( (
 ( 1.000000000000000000, 0.6992058987801026415, 1.000000000000000000),
 ( 1.000000000000000000, 0.6992660572539753927, 1.000000000000000000),
 ( 1.000000000000000000, 0.6974033530214182042, 1.000000000000000000),
 ( 1.000000000000000000, 0.6920435876590419477, 1.000000000000000000),
 ( 1.000000000000000000, 0.6885661196048414867, 1.000000000000000000),
 ( 1.000000000000000000, 0.6845372766838363487, 1.000000000000000000),
 ( 1.000000000000000000, 0.6841195446900723010, 1.000000000000000000),
 ( 1.000000000000000000, 0.6902705495933709745, 1.000000000000000000),
 ( 1.000000000000000000, 0.6968978290759786365, 1.000000000000000000),
 ( 1.000000000000000000, 0.7071067811865482389, 1.000000000000000000) ) ) 
 REPRESENTATION_ITEM ( '' )  SURFACE ( )  );
#23612=EDGE_CURVE ( 'NONE', #3631, #30600, #12269, .T. ) ;
#23613=CARTESIAN_POINT ( 'NONE',  ( 48.00000000000001421, -4.387164041431065087, -1.383037119376925528 ) ) ;
#23620=CARTESIAN_POINT ( 'NONE',  ( 48.00000000000001421, -4.031600731908413948, -1.173113608511841877 ) ) ;
#23627=CARTESIAN_POINT ( 'NONE',  ( 47.05963571244990362, 8.266527678078146479, -2.050000000000163691 ) ) ;
#23634=VECTOR ( 'NONE', #20858, 1000.000000000000000 ) ;
#23638=EDGE_LOOP ( 'NONE', ( #30949, #9728, #26142, #28261 ) ) ;
#23641=EDGE_CURVE ( 'NONE', #16210, #1060, #3278, .T. ) ;
#23648=CARTESIAN_POINT ( 'NONE',  ( 30.21341079104191607, 6.695592610073554773, -1.425000000000104849 ) ) ;
#23651=B_SPLINE_CURVE_WITH_KNOTS ( 'NONE', 3,
 ( #64, #29189, #11775, #21450, #29028, #31080, #28729, #14300, #7337, #26342 ),
 .UNSPECIFIED., .F., .F.,
 ( 4, 2, 2, 2, 4 ),
 ( 8.673617379884035472E-19, 0.0003923434276460365509, 0.0007846868552920722344, 0.001177030282938107972, 0.001569373710584143601 ),
 .UNSPECIFIED. ) ;
#23663=CARTESIAN_POINT ( 'NONE',  ( 52.14970241235015891, 8.689026183520638824, 2.049999999999819078 ) ) ;
#23680=CYLINDRICAL_SURFACE ( 'NONE', #24794, 0.09999999999999982514 ) ;
#23700=DIRECTION ( 'NONE',  ( 3.489354422748178582E-15, -1.218509414717996338E-16, 1.000000000000000000 ) ) ;
#23706=CARTESIAN_POINT ( 'NONE',  ( 51.75611399313550720, 4.330462468343535321, 2.050000000000262279 ) ) ;
#23712=CARTESIAN_POINT ( 'NONE',  ( 23.38852972788364326, 6.106843900651806933, -2.050000000000079758 ) ) ;
#23715=ORIENTED_EDGE ( 'NONE', *, *, #3963, .T. ) ;
#23718=EDGE_LOOP ( 'NONE', ( #30071, #10538, #550, #4486 ) ) ;
#23732=AXIS2_PLACEMENT_3D ( 'NONE', #19181, #14240, #16793 ) ;
#23743=ORIENTED_EDGE ( 'NONE', *, *, #24282, .F. ) ;
#23757=FACE_OUTER_BOUND ( 'NONE', #20648, .T. ) ;
#23760=ADVANCED_FACE ( 'NONE', ( #16061 ), #20816, .F. ) ;
#23775=ORIENTED_EDGE ( 'NONE', *, *, #27991, .F. ) ;
#23776=DIRECTION ( 'NONE',  ( 3.491481338843133355E-15, 0.000000000000000000, 1.000000000000000000 ) ) ;
#23803=CARTESIAN_POINT ( 'NONE',  ( 51.71860689488131868, 4.174878657598904752, -1.931421652553907187 ) ) ;
#23804=B_SPLINE_CURVE_WITH_KNOTS ( 'NONE', 3,
 ( #28546, #23663, #21605, #1954, #11614, #21297, #30926, #9572, #6856, #16523, #26180, #14135, #23810, #26334, #31071, #9396, #19064 ),
 .UNSPECIFIED., .F., .F.,
 ( 4, 2, 2, 2, 2, 1, 2, 2, 4 ),
 ( 0.000000000000000000, 0.1147774566006787567, 0.1721661849010180101, 0.2295549132013572635, 0.2869436415016964892, 0.3443323698020356871, 0.3730267339522053693, 0.4017210981023749961, 0.4591098264027145270 ),
 .UNSPECIFIED. ) ;
#23810=CARTESIAN_POINT ( 'NONE',  ( 54.02661639416933781, 7.247660624457942014, 2.049999999999812417 ) ) ;
#23814=CARTESIAN_POINT ( 'NONE',  ( 54.42157971047652865, 6.359826807111529590, -2.020139939762307879 ) ) ;
#23828=CARTESIAN_POINT ( 'NONE',  ( 51.80056195330648450, 4.599988466687112698, 0.2643113378676240077 ) ) ;
#23833=CARTESIAN_POINT ( 'NONE',  ( 27.81683722849680507, 5.540920426341900296, 2.049999999999902567 ) ) ;
#23834=ORIENTED_EDGE ( 'NONE', *, *, #3436, .T. ) ;
#23835=ORIENTED_EDGE ( 'NONE', *, *, #29957, .T. ) ;
#23851=EDGE_LOOP ( 'NONE', ( #5463, #7789, #27669, #22764 ) ) ;
#23878=CARTESIAN_POINT ( 'NONE',  ( 30.31473038486000249, 6.776227631128586282, 1.549999999999894129 ) ) ;
#23881=DIRECTION ( 'NONE',  ( -3.491481338843133355E-15, 0.000000000000000000, -1.000000000000000000 ) ) ;
#23883=DIRECTION ( 'NONE',  ( -0.9993908270190958731, 0.03489949670249913732, 3.435095992031088928E-15 ) ) ;
#23885=CARTESIAN_POINT ( 'NONE',  ( 53.94314916079858335, 6.379172879799750007, -1.774223561664970861 ) ) ;
#23887=EDGE_CURVE ( 'NONE', #19028, #15276, #23926, .T. ) ;
#23891=CARTESIAN_POINT ( 'NONE',  ( 51.52469891147812575, -4.265589706924725277, -1.723997649431408430 ) ) ;
#23898=ORIENTED_EDGE ( 'NONE', *, *, #19121, .F. ) ;
#23901=CARTESIAN_POINT ( 'NONE',  ( 51.80000000000002558, -3.701043595308292300, 1.983423889356453751 ) ) ;
#23908=ORIENTED_EDGE ( 'NONE', *, *, #11165, .F. ) ;
#23911=DIRECTION ( 'NONE',  ( 0.7313537016191670181, 0.6819983600625022513, -2.468850131082252327E-15 ) ) ;
#23924=( BOUNDED_SURFACE ( )  B_SPLINE_SURFACE ( 3, 2, ( 
 ( #28828, #28673, #20919 ),
 ( #13917, #28195, #2063 ),
 ( #9201, #6809, #13757 ),
 ( #21402, #16471, #19189 ),
 ( #31030, #11400, #26130 ),
 ( #6504, #7140, #16801 ),
 ( #1580, #21089, #30549 ),
 ( #11876, #8857, #21557 ),
 ( #18548, #21253, #30883 ),
 ( #23613, #6989, #16164 ) ),
 .UNSPECIFIED., .F., .F., .F. ) 
 B_SPLINE_SURFACE_WITH_KNOTS ( ( 4, 2, 2, 2, 4 ),
 ( 3, 3 ),
 ( -5.421010862427522170E-20, 0.0003534648051082250452, 0.0007069296102164500904, 0.001060394415324675136, 0.001413859220432900181 ),
 ( 0.000000000000000000, 1.000000000000000000 ),
 .UNSPECIFIED. ) 
 GEOMETRIC_REPRESENTATION_ITEM ( )  RATIONAL_B_SPLINE_SURFACE ( (
 ( 1.000000000000000000, 0.7071067811865467956, 1.000000000000000000),
 ( 1.000000000000000000, 0.6969521241105990361, 1.000000000000000000),
 ( 1.000000000000000000, 0.6903264600368322901, 1.000000000000000000),
 ( 1.000000000000000000, 0.6841066566211814193, 1.000000000000000000),
 ( 1.000000000000000000, 0.6845305055655173110, 1.000000000000000000),
 ( 1.000000000000000000, 0.6885489555120742899, 1.000000000000000000),
 ( 1.000000000000000000, 0.6920376555000889995, 1.000000000000000000),
 ( 1.000000000000000000, 0.6973723772405847621, 1.000000000000000000),
 ( 1.000000000000000000, 0.6992679762638227547, 1.000000000000000000),
 ( 1.000000000000000000, 0.6992058987801016423, 1.000000000000000000) ) ) 
 REPRESENTATION_ITEM ( '' )  SURFACE ( )  );
#23926=CIRCLE ( 'NONE', #18868, 2.625000000001612044 ) ;
#23931=ORIENTED_EDGE ( 'NONE', *, *, #10687, .F. ) ;
#23933=EDGE_LOOP ( 'NONE', ( #10824, #12397, #1378, #14945, #23835, #12738, #22020, #27774, #14806, #1499, #579, #31211 ) ) ;
#23935=CARTESIAN_POINT ( 'NONE',  ( 51.80000048029783244, 4.021162535479849254, 2.019963026417355589 ) ) ;
#23940=EDGE_CURVE ( 'NONE', #22859, #27565, #14926, .T. ) ;
#23941=CARTESIAN_POINT ( 'NONE',  ( 51.80000000000001137, -3.637377585518695611, -2.099877210783217318 ) ) ;
#23946=DIRECTION ( 'NONE',  ( 0.000000000000000000, -0.8740818021021516948, -0.4857787595540328796 ) ) ;
#23952=EDGE_CURVE ( 'NONE', #17544, #125, #23651, .T. ) ;
#23955=CARTESIAN_POINT ( 'NONE',  ( 50.35762544161294585, 8.151359338959888845, -1.550000000000175016 ) ) ;
#23964=DIRECTION ( 'NONE',  ( 3.489354422748178582E-15, -1.218509414717996338E-16, 1.000000000000000000 ) ) ;
#23965=CARTESIAN_POINT ( 'NONE',  ( 54.28362896329676346, 5.641750298212469872, -1.990863909997389714 ) ) ;
#23971=CARTESIAN_POINT ( 'NONE',  ( 30.89639353599806881, 7.705332861457931948, 1.424999999999892575 ) ) ;
#23977=CARTESIAN_POINT ( 'NONE',  ( 51.96339880813594192, 4.380689046771754747, 1.403568635141169807 ) ) ;
#23981=CARTESIAN_POINT ( 'NONE',  ( 51.87765138016307986, 8.698644590117595499, -1.950000000000180256 ) ) ;
#23982=CARTESIAN_POINT ( 'NONE',  ( 30.93618511144813610, 7.271541257249599433, 2.049999999999891465 ) ) ;
#24000=ORIENTED_EDGE ( 'NONE', *, *, #4637, .T. ) ;
#24003=CARTESIAN_POINT ( 'NONE',  ( 54.16553928697277343, 6.951169537962178069, 2.049999999999812861 ) ) ;
#24006=VERTEX_POINT ( 'NONE', #20325 ) ;
#24009=CARTESIAN_POINT ( 'NONE',  ( 22.11607288752048461, 7.780659299909677529, -2.050000000000077094 ) ) ;
#24010=ORIENTED_EDGE ( 'NONE', *, *, #14114, .F. ) ;
#24011=CARTESIAN_POINT ( 'NONE',  ( 30.31473038486000249, 6.776227631128586282, 1.949999999999893818 ) ) ;
#24033=CARTESIAN_POINT ( 'NONE',  ( 53.81464057712626925, 5.799094425976097256, -7.641258220787705557E-08 ) ) ;
#24039=CARTESIAN_POINT ( 'NONE',  ( 50.92089186451759275, -4.387164041431066863, -1.383037119376936630 ) ) ;
#24060=CARTESIAN_POINT ( 'NONE',  ( 48.00000000000001421, -3.937842575352406005, -1.145831896685989282 ) ) ;
#24071=AXIS2_PLACEMENT_3D ( 'NONE', #6804, #16156, #18700 ) ;
#24073=EDGE_CURVE ( 'NONE', #19244, #18673, #22374, .T. ) ;
#24093=B_SPLINE_CURVE_WITH_KNOTS ( 'NONE', 3,
 ( #12168, #26261, #1880, #4568, #23891, #4875, #21848, #21523, #24039, #24205 ),
 .UNSPECIFIED., .F., .F.,
 ( 4, 2, 2, 2, 4 ),
 ( 0.000000000000000000, 0.0003601004132760234544, 0.0007202008265520462582, 0.001080301239828069170, 0.001440401653104092300 ),
 .UNSPECIFIED. ) ;
#24095=CARTESIAN_POINT ( 'NONE',  ( 51.06462745158204086, -4.023728077055554131, -1.198744011644903518 ) ) ;
#24101=TOROIDAL_SURFACE ( 'NONE', #22082, 2.525000000001608846, 0.1000000000000000056 ) ;
#24107=CARTESIAN_POINT ( 'NONE',  ( 50.80000000000001847, -3.908336260473453727, -1.238913909466097474 ) ) ;
#24115=FACE_OUTER_BOUND ( 'NONE', #22231, .T. ) ;
#24120=CARTESIAN_POINT ( 'NONE',  ( 48.00000000000001421, -4.319730106884873244, -1.256953381662404778 ) ) ;
#24123=LINE ( 'NONE', #14295, #28255 ) ;
#24124=CARTESIAN_POINT ( 'NONE',  ( 54.33836953411530146, 6.362880879443651772, -2.050000000000188560 ) ) ;
#24126=CARTESIAN_POINT ( 'NONE',  ( 51.70000000000000995, -3.550773357292059007, -2.049880134336001802 ) ) ;
#24127=AXIS2_PLACEMENT_3D ( 'NONE', #15467, #13702, #13089 ) ;
#24140=CARTESIAN_POINT ( 'NONE',  ( 47.09453520915242564, 9.265918505097243241, -2.050000000000163691 ) ) ;
#24143=CARTESIAN_POINT ( 'NONE',  ( 28.66473729876423704, 5.839050301631238504, 2.049999999999899902 ) ) ;
#24146=DIRECTION ( 'NONE',  ( 0.000000000000000000, 0.000000000000000000, 1.000000000000000000 ) ) ;
#24161=CARTESIAN_POINT ( 'NONE',  ( 51.97945110550971037, 4.337541896208930048, 1.549654688285104331 ) ) ;
#24174=EDGE_LOOP ( 'NONE', ( #18410, #29025, #18685, #11694 ) ) ;
#24177=CARTESIAN_POINT ( 'NONE',  ( 21.97322666366009614, 8.076925076899403422, -1.950000000000076117 ) ) ;
#24179=VERTEX_POINT ( 'NONE', #22849 ) ;
#24183=CARTESIAN_POINT ( 'NONE',  ( 53.37675057098704912, 7.899674929380397614, 1.885230776086536109 ) ) ;
#24188=ADVANCED_FACE ( 'NONE', ( #3820 ), #27544, .T. ) ;
#24196=B_SPLINE_CURVE_WITH_KNOTS ( 'NONE', 3,
 ( #20736, #1870, #8998, #11540, #1693, #25777 ),
 .UNSPECIFIED., .F., .F.,
 ( 4, 2, 4 ),
 ( 0.000000000000000000, 0.5000000000000000000, 1.000000000000000000 ),
 .UNSPECIFIED. ) ;
#24200=CARTESIAN_POINT ( 'NONE',  ( 53.90826771765248537, 6.078164526406591328, -1.689602626210267466 ) ) ;
#24205=CARTESIAN_POINT ( 'NONE',  ( 50.80000000000001137, -4.387164041431065975, -1.383037119376935742 ) ) ;
#24214=EDGE_LOOP ( 'NONE', ( #10139, #22194, #3215, #22417 ) ) ;
#24216=DIRECTION ( 'NONE',  ( 3.016910393003118404E-15, 0.000000000000000000, 1.000000000000000000 ) ) ;
#24220=VECTOR ( 'NONE', #8743, 1000.000000000000000 ) ;
#24228=CARTESIAN_POINT ( 'NONE',  ( 51.73328143279136526, 4.175271471638091647, 1.930573136446042337 ) ) ;
#24229=CARTESIAN_POINT ( 'NONE',  ( 50.87477060347373481, 8.633605004118187765, -2.050000000000176570 ) ) ;
#24232=CARTESIAN_POINT ( 'NONE',  ( 53.36557156485857689, 7.911885792138814821, -1.886359577549349797 ) ) ;
#24235=CARTESIAN_POINT ( 'NONE',  ( 51.58641917109738984, -3.755449232595080122, 1.648679025009623267 ) ) ;
#24255=PRESENTATION_STYLE_ASSIGNMENT (( #14593 ) ) ;
#24262=CARTESIAN_POINT ( 'NONE',  ( 52.41206581543986687, 8.644163850305695007, -2.050000000000182343 ) ) ;
#24264=CARTESIAN_POINT ( 'NONE',  ( 21.97322666366010324, 8.076925076899300393, -1.950000000000076117 ) ) ;
#24272=CARTESIAN_POINT ( 'NONE',  ( 47.00000000000002132, 2.428612866367529932E-14, -1.640996229256273308E-13 ) ) ;
#24273=EDGE_LOOP ( 'NONE', ( #14112, #30781, #23898, #16654, #7374 ) ) ;
#24282=EDGE_CURVE ( 'NONE', #25126, #107, #3217, .T. ) ;
#24284=CARTESIAN_POINT ( 'NONE',  ( 22.54717926605044909, 7.740376438784151603, 1.424999999999921663 ) ) ;
#24291=DIRECTION ( 'NONE',  ( 9.754918421198724481E-16, -0.9601771338024399638, 0.2793919678926571892 ) ) ;
#24293=EDGE_LOOP ( 'NONE', ( #24963, #6926, #9619, #20205 ) ) ;
#24295=CARTESIAN_POINT ( 'NONE',  ( 51.80000048712015115, 3.919471099442191520, -2.045252491637605807 ) ) ;
#24296=CARTESIAN_POINT ( 'NONE',  ( 30.67843166873835159, 7.122989987860218974, 2.049999999999892353 ) ) ;
#24311=CARTESIAN_POINT ( 'NONE',  ( 53.60047708782985865, 7.640852521089519733, 1.861455469535095331 ) ) ;
#24317=CARTESIAN_POINT ( 'NONE',  ( 52.11563210330035645, 3.836792880204552336, 2.049999999999818190 ) ) ;
#24326=CARTESIAN_POINT ( 'NONE',  ( 27.27214205000343483, 5.011961650406414392, 1.949999999999904254 ) ) ;
#24328=CARTESIAN_POINT ( 'NONE',  ( 30.93618511144916994, 7.271541257249353407, -2.050000000000106848 ) ) ;
#24335=CARTESIAN_POINT ( 'NONE',  ( 53.78456803694539445, 5.661108390837276794, -1.682988280464833286 ) ) ;
#24336=SPHERICAL_SURFACE ( 'NONE', #9930, 0.1000000000000000056 ) ;
#24340=FACE_OUTER_BOUND ( 'NONE', #24273, .T. ) ;
#24342=ORIENTED_EDGE ( 'NONE', *, *, #10851, .F. ) ;
#24345=CARTESIAN_POINT ( 'NONE',  ( 53.90734097010463444, 6.075402212724766216, 1.402257142663977607 ) ) ;
#24352=CARTESIAN_POINT ( 'NONE',  ( 50.80000000000002558, -4.387164041431067751, 1.383037119376580693 ) ) ;
#24370=ORIENTED_EDGE ( 'NONE', *, *, #329, .T. ) ;
#24389=DIRECTION ( 'NONE',  ( 0.7313537016191670181, 0.6819983600625023623, -2.468850131082252722E-15 ) ) ;
#24394=LINE ( 'NONE', #17420, #13493 ) ;
#24418=CARTESIAN_POINT ( 'NONE',  ( 51.80000000000001137, 4.350000000000017408, -1.495827530165608321 ) ) ;
#24422=CARTESIAN_POINT ( 'NONE',  ( 47.21160823903058912, -4.227734780419093674, 1.816236823409400847 ) ) ;
#24426=ORIENTED_EDGE ( 'NONE', *, *, #4637, .F. ) ;
#24432=CARTESIAN_POINT ( 'NONE',  ( 52.01765327766486280, 4.368296548649880151, 1.441525720016375134 ) ) ;
#24439=CARTESIAN_POINT ( 'NONE',  ( 26.91641317417657220, 5.349067879198667441, 2.049999999999906564 ) ) ;
#24440=ORIENTED_EDGE ( 'NONE', *, *, #6268, .F. ) ;
#24443=CARTESIAN_POINT ( 'NONE',  ( 53.81464057712624793, 5.799094425976102585, -2.050000000000187228 ) ) ;
#24451=CARTESIAN_POINT ( 'NONE',  ( 52.82099478266074755, 4.588601447596447613, 1.578939844535152570 ) ) ;
#24456=ORIENTED_EDGE ( 'NONE', *, *, #16041, .F. ) ;
#24463=CARTESIAN_POINT ( 'NONE',  ( 53.81450004168215173, 5.799141575175360330, -1.730551853729838774 ) ) ;
#24467=CARTESIAN_POINT ( 'NONE',  ( 27.54696499484732186, 5.363421040470059076, -2.050000000000028244 ) ) ;
#24475=CARTESIAN_POINT ( 'NONE',  ( 53.60227722476024326, 4.617096236911465645, -2.050000000000186784 ) ) ;
#24476=EDGE_CURVE ( 'NONE', #26160, #8007, #19826, .T. ) ;
#24486=CARTESIAN_POINT ( 'NONE',  ( 54.22158129257385184, 6.014404448109268664, 2.049999999999810640 ) ) ;
#24499=CARTESIAN_POINT ( 'NONE',  ( 53.02535680938098039, 4.241071265092343445, 2.047386379460785388 ) ) ;
#24508=DIRECTION ( 'NONE',  ( -3.489354422748178582E-15, 1.218509414717996338E-16, -1.000000000000000000 ) ) ;
#24512=EDGE_CURVE ( 'NONE', #6647, #10074, #30594, .T. ) ;
#24514=ADVANCED_FACE ( 'NONE', ( #23498 ), #18766, .F. ) ;
#24516=CARTESIAN_POINT ( 'NONE',  ( 24.67796800286685510, 5.428620075164593217, -1.950000000000086109 ) ) ;
#24517=EDGE_CURVE ( 'NONE', #7259, #30552, #9098, .T. ) ;
#24520=DIRECTION ( 'NONE',  ( -1.000000000000000000, -0.000000000000000000, 3.491481338843133355E-15 ) ) ;
#24523=CARTESIAN_POINT ( 'NONE',  ( 30.21341079104190186, 6.695592610073531681, 1.424999999999893907 ) ) ;
#24524=ORIENTED_EDGE ( 'NONE', *, *, #15658, .F. ) ;
#24554=AXIS2_PLACEMENT_3D ( 'NONE', #13909, #20767, #18380 ) ;
#24564=DIRECTION ( 'NONE',  ( 0.9993908270191184107, -0.03489949670185085034, -3.491481338843133355E-15 ) ) ;
#24568=CARTESIAN_POINT ( 'NONE',  ( 52.79462163297414889, 4.045128697758171299, -0.6895311692810858206 ) ) ;
#24572=CIRCLE ( 'NONE', #10919, 0.1000000000000002554 ) ;
#24575=EDGE_LOOP ( 'NONE', ( #172, #9652, #6182, #18639, #31174, #13235 ) ) ;
#24581=EDGE_CURVE ( 'NONE', #6667, #15786, #11470, .T. ) ;
#24589=VECTOR ( 'NONE', #11311, 1000.000000000000000 ) ;
#24593=VECTOR ( 'NONE', #22836, 1000.000000000000000 ) ;
#24599=FACE_OUTER_BOUND ( 'NONE', #26524, .T. ) ;
#24600=CARTESIAN_POINT ( 'NONE',  ( 47.05963571244990362, 8.266527678078146479, -1.950000000000163380 ) ) ;
#24610=CARTESIAN_POINT ( 'NONE',  ( 53.78456803694540866, 5.661108390837275905, 1.682988280464426722 ) ) ;
#24613=AXIS2_PLACEMENT_3D ( 'NONE', #24682, #609, #17254 ) ;
#24614=ORIENTED_EDGE ( 'NONE', *, *, #2294, .T. ) ;
#24621=ORIENTED_EDGE ( 'NONE', *, *, #19945, .F. ) ;
#24623=CARTESIAN_POINT ( 'NONE',  ( 51.06423821941617547, -4.410640387330812651, -1.311048612305549144 ) ) ;
#24628=CARTESIAN_POINT ( 'NONE',  ( 32.54904120526650502, 8.004085848662747082, -2.050000000000113065 ) ) ;
#24636=DIRECTION ( 'NONE',  ( -1.000000000000000000, -0.000000000000000000, 3.491481338843133355E-15 ) ) ;
#24638=CARTESIAN_POINT ( 'NONE',  ( 53.29207122288457299, 4.934008984266801789, -1.614082030464848438 ) ) ;
#24652=CARTESIAN_POINT ( 'NONE',  ( 54.31977788970097265, 6.362876281374246545, 2.049999999999810196 ) ) ;
#24653=ORIENTED_EDGE ( 'NONE', *, *, #10977, .T. ) ;
#24658=CARTESIAN_POINT ( 'NONE',  ( 51.73499623029054106, 4.165486553371512635, 1.939055223349886781 ) ) ;
#24662=B_SPLINE_CURVE_WITH_KNOTS ( 'NONE', 3,
 ( #4241, #3939, #9171, #13580, #18833, #1552 ),
 .UNSPECIFIED., .F., .F.,
 ( 4, 2, 4 ),
 ( 0.000000000000000000, 0.5000000000000000000, 1.000000000000000000 ),
 .UNSPECIFIED. ) ;
#24665=EDGE_CURVE ( 'NONE', #25954, #26805, #19437, .T. ) ;
#24682=CARTESIAN_POINT ( 'NONE',  ( 50.80000000000002558, -4.003661535119149129, 1.269131321891740383 ) ) ;
#24713=CARTESIAN_POINT ( 'NONE',  ( 52.41226287506259496, 8.644902628253648302, -2.050000000000182343 ) ) ;
#24719=CARTESIAN_POINT ( 'NONE',  ( 28.63101374161907842, 6.274379892050022001, -1.425000000000099742 ) ) ;
#24729=CARTESIAN_POINT ( 'NONE',  ( 51.76681525450422328, 3.850182003052834201, 1.478406873915413922 ) ) ;
#24732=FACE_OUTER_BOUND ( 'NONE', #583, .T. ) ;
#24735=DIRECTION ( 'NONE',  ( 3.491481338843133355E-15, 0.000000000000000000, 1.000000000000000000 ) ) ;
#24745=ORIENTED_EDGE ( 'NONE', *, *, #10790, .F. ) ;
#24747=CARTESIAN_POINT ( 'NONE',  ( 31.44149084649588133, 7.421688627196123100, 1.949999999999888933 ) ) ;
#24753=CARTESIAN_POINT ( 'NONE',  ( 22.07280086217094350, 8.086143481909239483, 2.049999999999922551 ) ) ;
#24756=CARTESIAN_POINT ( 'NONE',  ( 53.82754651211526919, 4.897847608402549291, -2.050000000000188560 ) ) ;
#24768=ADVANCED_FACE ( 'NONE', ( #1111 ), #8385, .T. ) ;
#24771=AXIS2_PLACEMENT_3D ( 'NONE', #17975, #29994, #20521 ) ;
#24776=CYLINDRICAL_SURFACE ( 'NONE', #11009, 1.000000000000000000 ) ;
#24780=CARTESIAN_POINT ( 'NONE',  ( 54.10834201130843013, 6.369203044738526387, -2.033313965204277540 ) ) ;
#24786=CARTESIAN_POINT ( 'NONE',  ( 33.98208436309533198, 8.188484713946708737, -2.050000000000247624 ) ) ;
#24792=CARTESIAN_POINT ( 'NONE',  ( 53.31680359303814498, 8.198234760421843959, -2.050000000000185452 ) ) ;
#24793=CARTESIAN_POINT ( 'NONE',  ( 47.88156667651360010, -3.908336253171002639, -1.238913932502745618 ) ) ;
#24794=AXIS2_PLACEMENT_3D ( 'NONE', #23981, #14467, #1796 ) ;
#24795=CARTESIAN_POINT ( 'NONE',  ( 47.10000000000002274, 6.982261990806648555E-14, -1.632474749424821370E-13 ) ) ;
#24803=CARTESIAN_POINT ( 'NONE',  ( 53.94314916079858335, 6.379172879799750007, -1.774223561664970861 ) ) ;
#24805=CARTESIAN_POINT ( 'NONE',  ( 54.44724579918531049, 6.358489010972262712, -1.963089969304977700 ) ) ;
#24808=EDGE_LOOP ( 'NONE', ( #6437, #13562, #5087, #29603, #10353, #17161 ) ) ;
#24809=CARTESIAN_POINT ( 'NONE',  ( 53.94136487687685388, 6.599443998687462454, 1.761196874214440378 ) ) ;
#24811=FACE_OUTER_BOUND ( 'NONE', #15781, .T. ) ;
#24818=CARTESIAN_POINT ( 'NONE',  ( 52.23459832779079903, 3.957147914211791573, 2.045484236922850307 ) ) ;
#24829=ORIENTED_EDGE ( 'NONE', *, *, #329, .F. ) ;
#24838=ORIENTED_EDGE ( 'NONE', *, *, #28785, .F. ) ;
#24847=CARTESIAN_POINT ( 'NONE',  ( 47.00000000000002842, -3.637377585518695611, 2.099877210782872261 ) ) ;
#24855=EDGE_CURVE ( 'NONE', #12841, #11041, #30356, .T. ) ;
#24858=CARTESIAN_POINT ( 'NONE',  ( 53.81176349924869129, 5.730864617276226980, -1.682988280464833286 ) ) ;
#24862=CIRCLE ( 'NONE', #15268, 159.7997717543496776 ) ;
#24878=CARTESIAN_POINT ( 'NONE',  ( 47.19807692573832725, -4.191416138886288500, 1.624134901684293419 ) ) ;
#24887=DIRECTION ( 'NONE',  ( 0.000000000000000000, 0.000000000000000000, -1.000000000000000000 ) ) ;
#24890=CARTESIAN_POINT ( 'NONE',  ( 27.44806845810027340, 5.340582161072727985, 1.949999999999904476 ) ) ;
#24892=VERTEX_POINT ( 'NONE', #26276 ) ;
#24896=CARTESIAN_POINT ( 'NONE',  ( 21.97322666366011035, 8.076925076899389211, 2.049999999999926104 ) ) ;
#24897=ORIENTED_EDGE ( 'NONE', *, *, #21273, .T. ) ;
#24905=DIRECTION ( 'NONE',  ( 3.083952846180964840E-15, -1.776356839400251254E-15, 1.000000000000000000 ) ) ;
#24906=LINE ( 'NONE', #29662, #18975 ) ;
#24920=CARTESIAN_POINT ( 'NONE',  ( 50.80000000000001847, 0.2793919678926817807, -0.9601771338026184877 ) ) ;
#24924=FACE_OUTER_BOUND ( 'NONE', #13387, .T. ) ;
#24928=CARTESIAN_POINT ( 'NONE',  ( 30.98482657347591029, 7.184130539199417242, -1.950000000000108091 ) ) ;
#24936=CARTESIAN_POINT ( 'NONE',  ( 47.54395435973425066, -3.873096995916273766, 1.345769568645033942 ) ) ;
#24944=CARTESIAN_POINT ( 'NONE',  ( 50.34192419032897448, 8.193354243125561709, -2.050000000000174794 ) ) ;
#24945=ORIENTED_EDGE ( 'NONE', *, *, #23258, .T. ) ;
#24948=CARTESIAN_POINT ( 'NONE',  ( 54.22606526463520993, 5.661062737973960424, 2.046523307115193369 ) ) ;
#24950=B_SPLINE_CURVE_WITH_KNOTS ( 'NONE', 3,
 ( #17607, #6044, #1263, #647, #10475, #10306, #25189, #24719, #17764, #1122, #29781, #27405, #15365, #10770, #19975 ),
 .UNSPECIFIED., .F., .F.,
 ( 4, 1, 1, 1, 1, 1, 1, 1, 1, 1, 1, 1, 4 ),
 ( 0.03200690811994900270, 0.06212998257909596589, 0.1242599651581919318, 0.2485199303163838636, 0.3727798954745757953, 0.4970398606327676716, 0.6212998257909596589, 0.6834298083700556248, 0.7455597909491513686, 0.8076897735282473345, 0.8387547648177954285, 0.8698197561073433004, 0.8953196949773711832 ),
 .UNSPECIFIED. ) ;
#24954=CARTESIAN_POINT ( 'NONE',  ( 51.79118766240952709, 4.088244304910976012, 1.991034353352840958 ) ) ;
#24956=CARTESIAN_POINT ( 'NONE',  ( 51.60286920921249987, -3.901416201057245292, -1.541017813822733062 ) ) ;
#24961=CARTESIAN_POINT ( 'NONE',  ( 52.99773473688004088, 4.225724694811284543, 2.047297911660232117 ) ) ;
#24962=CARTESIAN_POINT ( 'NONE',  ( 51.80000048712015115, 3.919471099442191520, -2.045252491637605807 ) ) ;
#24963=ORIENTED_EDGE ( 'NONE', *, *, #24517, .F. ) ;
#24967=EDGE_CURVE ( 'NONE', #15457, #4799, #5039, .T. ) ;
#24969=EDGE_CURVE ( 'NONE', #26664, #26160, #9338, .T. ) ;
#24993=CARTESIAN_POINT ( 'NONE',  ( 51.80000000000001137, 3.850000000000016520, -1.950000000000180256 ) ) ;
#25008=B_SPLINE_CURVE_WITH_KNOTS ( 'NONE', 3,
 ( #11925, #21612, #26656, #28725, #9576, #11619, #16696, #24126 ),
 .UNSPECIFIED., .F., .F.,
 ( 4, 2, 2, 4 ),
 ( 0.000000000000000000, 0.0007042195513453415210, 0.001056329327018012227, 0.001408439102690683042 ),
 .UNSPECIFIED. ) ;
#25019=CARTESIAN_POINT ( 'NONE',  ( 52.23456635604563303, 3.957142910676406888, -2.045484142945491524 ) ) ;
#25030=CARTESIAN_POINT ( 'NONE',  ( 54.13139471328951657, 5.522381836601891081, 2.049999999999811084 ) ) ;
#25033=EDGE_LOOP ( 'NONE', ( #15420, #14796, #30732 ) ) ;
#25051=CARTESIAN_POINT ( 'NONE',  ( 22.68548117337035563, 6.704541182151904977, 2.049999999999919886 ) ) ;
#25066=CARTESIAN_POINT ( 'NONE',  ( 21.97322666366011745, 8.076925076899298617, 1.949999999999923128 ) ) ;
#25070=AXIS2_PLACEMENT_3D ( 'NONE', #1824, #8780, #30330 ) ;
#25075=CARTESIAN_POINT ( 'NONE',  ( 47.10000000000002274, 2.428612866367529932E-14, -1.644487710595116631E-13 ) ) ;
#25088=CARTESIAN_POINT ( 'NONE',  ( 23.33428888328930739, 6.022557148079468625, -2.050000000000081979 ) ) ;
#25090=EDGE_CURVE ( 'NONE', #15786, #28571, #2988, .T. ) ;
#25100=AXIS2_PLACEMENT_3D ( 'NONE', #3271, #25115, #1621 ) ;
#25105=CARTESIAN_POINT ( 'NONE',  ( 51.35632695591942820, -4.328087698693943608, 1.560456010858371378 ) ) ;
#25108=CARTESIAN_POINT ( 'NONE',  ( 41.48619405471883681, -151.3359592902622239, -2.050000000000163691 ) ) ;
#25113=ORIENTED_EDGE ( 'NONE', *, *, #22040, .F. ) ;
#25115=DIRECTION ( 'NONE',  ( -1.000000000000000000, -0.000000000000000000, 3.491481338843133355E-15 ) ) ;
#25116=CARTESIAN_POINT ( 'NONE',  ( 54.44772159691260072, 6.353385547808748868, -1.625000000000181188 ) ) ;
#25124=CARTESIAN_POINT ( 'NONE',  ( 51.69999998495889315, -3.608564799421289493, -1.949774616186548570 ) ) ;
#25126=VERTEX_POINT ( 'NONE', #25446 ) ;
#25128=AXIS2_PLACEMENT_3D ( 'NONE', #6915, #4368, #14017 ) ;
#25136=DIRECTION ( 'NONE',  ( 3.489354422748178582E-15, -1.218509414717996338E-16, 1.000000000000000000 ) ) ;
#25158=CARTESIAN_POINT ( 'NONE',  ( 25.99326321321243327, 5.312800855510418252, 2.049999999999909228 ) ) ;
#25173=VERTEX_POINT ( 'NONE', #18196 ) ;
#25176=AXIS2_PLACEMENT_3D ( 'NONE', #30360, #28310, #8988 ) ;
#25180=CARTESIAN_POINT ( 'NONE',  ( 53.44675344197725053, 5.128499738955621723, -1.627484327855545532 ) ) ;
#25182=( NAMED_UNIT ( * ) SI_UNIT ( $, .STERADIAN. ) SOLID_ANGLE_UNIT ( ) );
#25186=CARTESIAN_POINT ( 'NONE',  ( 51.74555621289471929, 3.825902093565871631, -2.050000000000180123 ) ) ;
#25189=CARTESIAN_POINT ( 'NONE',  ( 27.62808879389201522, 5.849836810644521989, -1.425000000000096412 ) ) ;
#25202=CARTESIAN_POINT ( 'NONE',  ( 47.49392074102413375, -3.992076856964202669, -1.294425493481064393 ) ) ;
#25205=CARTESIAN_POINT ( 'NONE',  ( 54.13382992866386445, 5.521407779354434275, 2.049999999999811084 ) ) ;
#25211=CARTESIAN_POINT ( 'NONE',  ( 47.20943027200282671, -4.226153977860457545, -1.819915812912896502 ) ) ;
#25218=EDGE_LOOP ( 'NONE', ( #5781, #18361, #844, #5631, #20573 ) ) ;
#25219=CARTESIAN_POINT ( 'NONE',  ( 50.80000000000001847, -4.003661535119149129, -1.269131321892095654 ) ) ;
#25229=B_SPLINE_CURVE_WITH_KNOTS ( 'NONE', 3,
 ( #7252, #17374, #14993, #19309, #28944, #137, #16921, #9788, #19456, #17091 ),
 .UNSPECIFIED., .F., .F.,
 ( 4, 2, 2, 2, 4 ),
 ( 0.000000000000000000, 0.0003520942986628443545, 0.0007041885973256887090, 0.001056282895988533118, 0.001408377194651377418 ),
 .UNSPECIFIED. ) ;
#25247=ORIENTED_EDGE ( 'NONE', *, *, #7884, .T. ) ;
#25249=ORIENTED_EDGE ( 'NONE', *, *, #27783, .T. ) ;
#25263=AXIS2_PLACEMENT_3D ( 'NONE', #21524, #4712, #30695 ) ;
#25268=CARTESIAN_POINT ( 'NONE',  ( 51.70000000000003126, -4.020776289669855785, 2.234582293948397691 ) ) ;
#25274=EDGE_CURVE ( 'NONE', #12883, #6647, #5012, .T. ) ;
#25277=CARTESIAN_POINT ( 'NONE',  ( 54.40373534908291475, 5.983016908836285452, 1.963089969304594895 ) ) ;
#25279=CARTESIAN_POINT ( 'NONE',  ( 50.80000000000002558, -3.937842575352406005, 1.145831896685643558 ) ) ;
#25314=CARTESIAN_POINT ( 'NONE',  ( 24.20708092330206185, 5.694650688851918829, 2.049999999999915001 ) ) ;
#25333=MANIFOLD_SOLID_BREP ( 'Stock-MAS-683-1', #18576 ) ;
#25334=ADVANCED_FACE ( 'NONE', ( #16214 ), #9395, .T. ) ;
#25339=CARTESIAN_POINT ( 'NONE',  ( 52.38400031671233137, 8.538946093000230775, -1.943109374214847973 ) ) ;
#25346=CARTESIAN_POINT ( 'NONE',  ( 47.06312566212015724, 8.366466760780054912, -2.050000000000163691 ) ) ;
#25357=CARTESIAN_POINT ( 'NONE',  ( 53.60445531103938777, 4.614871059762980288, 2.049999999999812861 ) ) ;
#25361=B_SPLINE_CURVE_WITH_KNOTS ( 'NONE', 3,
 ( #3997, #20948, #8890, #21427 ),
 .UNSPECIFIED., .F., .F.,
 ( 4, 4 ),
 ( 0.000000000000000000, 1.000000000000000000 ),
 .UNSPECIFIED. ) ;
#25366=CARTESIAN_POINT ( 'NONE',  ( 24.69162372611912204, 5.424666981099267815, 1.949999999999913580 ) ) ;
#25378=CARTESIAN_POINT ( 'NONE',  ( 26.18134456910377850, 5.211034382732834480, -1.425000000000091083 ) ) ;
#25380=B_SPLINE_CURVE_WITH_KNOTS ( 'NONE', 3,
 ( #1576, #7595, #22009, #16794, #26438, #4899, #9972, #17253, #26893, #24516, #9523, #29283, #28968, #12323, #19182, #7276, #17113, #11871, #26759, #2828, #20231, #26285, #19331, #19477, #2685, #21716, #12482, #5060, #29122, #16945, #7440, #29861 ),
 .UNSPECIFIED., .F., .F.,
 ( 4, 2, 2, 2, 2, 2, 2, 2, 2, 2, 2, 2, 2, 2, 2, 4 ),
 ( 1.010318202610065295E-16, 0.0009241660915624322521, 0.001848332183124763457, 0.002772498274687094661, 0.003696664366249425866, 0.004620830457811756636, 0.005544996549374087841, 0.006469162640936418178, 0.006931245686717583780, 0.007393328732498750250, 0.009241660915623431741, 0.01016582700718577509, 0.01108999309874812017, 0.01201415919031047566, 0.01293832528187282768, 0.01478665746499753693 ),
 .UNSPECIFIED. ) ;
#25383=DIRECTION ( 'NONE',  ( 3.491481338843133750E-15, 0.000000000000000000, 1.000000000000000000 ) ) ;
#25400=CARTESIAN_POINT ( 'NONE',  ( 51.80000000000000426, -4.020776289669849568, -2.234582293948755183 ) ) ;
#25403=CARTESIAN_POINT ( 'NONE',  ( 22.72181155690797638, 6.520914527883283185, -2.050000000000079758 ) ) ;
#25407=VERTEX_POINT ( 'NONE', #19068 ) ;
#25414=CARTESIAN_POINT ( 'NONE',  ( 47.49584747294277065, -3.900546889229666636, 1.266936454265243039 ) ) ;
#25417=CARTESIAN_POINT ( 'NONE',  ( 53.81457038983117513, 5.799118250651475570, -1.689328355159275041 ) ) ;
#25426=CARTESIAN_POINT ( 'NONE',  ( 54.29903447189319365, 6.002870899074444822, -2.050000000000188116 ) ) ;
#25429=CARTESIAN_POINT ( 'NONE',  ( 51.77457724156050034, -3.759243154119239261, 1.865745259404142598 ) ) ;
#25431=CARTESIAN_POINT ( 'NONE',  ( 53.71202192472757275, 7.447163568589272309, 1.837855077339518362 ) ) ;
#25434=DIRECTION ( 'NONE',  ( 0.000000000000000000, -0.8660422822663634834, 0.4999707644721521627 ) ) ;
#25436=CARTESIAN_POINT ( 'NONE',  ( 31.86627779902472568, 7.736385160319314558, -2.050000000000110845 ) ) ;
#25441=CYLINDRICAL_SURFACE ( 'NONE', #8891, 1.000000000000000000 ) ;
#25445=EDGE_CURVE ( 'NONE', #9698, #30783, #25008, .T. ) ;
#25446=CARTESIAN_POINT ( 'NONE',  ( 51.80000048712027905, 3.919471135816211316, 2.045252759501752227 ) ) ;
#25458=DIRECTION ( 'NONE',  ( 3.489354422748178582E-15, -1.218509414717996338E-16, 1.000000000000000000 ) ) ;
#25459=CARTESIAN_POINT ( 'NONE',  ( 22.49281023664668311, 6.945812178203861542, 2.049999999999921663 ) ) ;
#25461=DIRECTION ( 'NONE',  ( -3.491481338843133355E-15, 0.000000000000000000, -1.000000000000000000 ) ) ;
#25468=ORIENTED_EDGE ( 'NONE', *, *, #7486, .T. ) ;
#25483=CARTESIAN_POINT ( 'NONE',  ( 53.94136487687669046, 6.599443998687474000, -2.050000000000187228 ) ) ;
#25487=DIRECTION ( 'NONE',  ( 3.491481338843133355E-15, -0.000000000000000000, 1.000000000000000000 ) ) ;
#25494=ORIENTED_EDGE ( 'NONE', *, *, #18892, .T. ) ;
#25503=CARTESIAN_POINT ( 'NONE',  ( 52.98236138753810565, 8.264679131573773319, 2.049999999999815525 ) ) ;
#25504=PLANE ( 'NONE',  #19929 ) ;
#25507=EDGE_CURVE ( 'NONE', #17544, #8932, #17454, .T. ) ;
#25538=SURFACE_SIDE_STYLE ('',( #23341 ) ) ;
#25548=CARTESIAN_POINT ( 'NONE',  ( 51.67599084732030690, -4.149782173365514026, -1.728795876848868485 ) ) ;
#25549=ORIENTED_EDGE ( 'NONE', *, *, #29957, .F. ) ;
#25555=VECTOR ( 'NONE', #25487, 1000.000000000000000 ) ;
#25563=CARTESIAN_POINT ( 'NONE',  ( 47.10000001504278089, -3.608564799421224656, 1.949774616186315424 ) ) ;
#25568=CARTESIAN_POINT ( 'NONE',  ( 51.67746714285173226, -4.134031523355556459, 2.020495556749221322 ) ) ;
#25575=CARTESIAN_POINT ( 'NONE',  ( 54.19698791822510486, 6.698472055538887915, -2.050000000000188116 ) ) ;
#25580=CARTESIAN_POINT ( 'NONE',  ( 51.25597219945275640, -3.873145847240234030, 1.345634385052566051 ) ) ;
#25582=CIRCLE ( 'NONE', #22090, 0.1000000000000002554 ) ;
#25583=CARTESIAN_POINT ( 'NONE',  ( 51.74540690333468262, 3.818766532315405193, 2.049999999999813305 ) ) ;
#25589=CARTESIAN_POINT ( 'NONE',  ( 25.69839743624499917, 5.334032503031479244, -2.050000000000089084 ) ) ;
#25605=AXIS2_PLACEMENT_3D ( 'NONE', #17903, #27543, #23288 ) ;
#25607=AXIS2_PLACEMENT_3D ( 'NONE', #7482, #22211, #19221 ) ;
#25610=B_SPLINE_CURVE_WITH_KNOTS ( 'NONE', 3,
 ( #7284, #2836, #29428, #24523, #27050, #12330, #5366, #10128, #12490, #29129, #15027, #22177, #14401, #9979, #2548, #29288, #7602, #17258, #2386, #22017, #464, #26598, #308, #12049, #4909, #14572, #26900, #163 ),
 .UNSPECIFIED., .F., .F.,
 ( 4, 2, 2, 2, 2, 2, 2, 2, 2, 2, 2, 2, 2, 4 ),
 ( 0.003059686050519383211, 0.004393787003443079715, 0.005060837479904928618, 0.005727887956366777521, 0.007061988909290467520, 0.007729039385752312086, 0.008396089862214158386, 0.009063140338676002952, 0.009730190815137849253, 0.01106429176806154879, 0.01239839272098524833, 0.01306544319744709463, 0.01339896843567802039, 0.01373249367390894267 ),
 .UNSPECIFIED. ) ;
#25619=ADVANCED_FACE ( 'NONE', ( #14766 ), #17162, .T. ) ;
#25623=DIRECTION ( 'NONE',  ( 4.275831445896958607E-31, 1.000000000000000000, 1.224646799147353207E-16 ) ) ;
#25625=CARTESIAN_POINT ( 'NONE',  ( 47.10000000000002274, 2.428612866367529932E-14, -1.644487710595116631E-13 ) ) ;
#25640=CARTESIAN_POINT ( 'NONE',  ( 53.30088642852334146, 4.970682635617305500, -1.612336972319552642 ) ) ;
#25656=VECTOR ( 'NONE', #4424, 1000.000000000000114 ) ;
#25658=DIRECTION ( 'NONE',  ( 0.000000000000000000, 0.000000000000000000, -1.000000000000000000 ) ) ;
#25667=DIRECTION ( 'NONE',  ( 3.491481338843133355E-15, -0.000000000000000000, 1.000000000000000000 ) ) ;
#25671=CARTESIAN_POINT ( 'NONE',  ( 52.02275531408258047, 3.834498708141866441, 2.049999999999818190 ) ) ;
#25682=CARTESIAN_POINT ( 'NONE',  ( 22.16344984338963897, 7.321836226319897278, 1.949999999999922462 ) ) ;
#25691=CARTESIAN_POINT ( 'NONE',  ( 27.79265796670793875, 5.432811198890464155, -1.425000000000097300 ) ) ;
#25693=EDGE_CURVE ( 'NONE', #15927, #15558, #25582, .T. ) ;
#25708=FILL_AREA_STYLE ('',( #30599 ) ) ;
#25711=DIRECTION ( 'NONE',  ( 1.000000000000000000, 0.000000000000000000, -3.469446951953543191E-15 ) ) ;
#25721=CARTESIAN_POINT ( 'NONE',  ( 54.04962709127927667, 6.684747557764788795, -2.023090456647256730 ) ) ;
#25723=CARTESIAN_POINT ( 'NONE',  ( 22.07280086217094706, 8.086143481909150665, -2.050000000000076206 ) ) ;
#25742=CARTESIAN_POINT ( 'NONE',  ( 50.80000000000001847, -4.031600731908413948, -1.173113608511851869 ) ) ;
#25743=CIRCLE ( 'NONE', #14095, 0.1000000000000021150 ) ;
#25745=CARTESIAN_POINT ( 'NONE',  ( 50.35762544161294585, 8.151359338959887069, -2.008578643762865656 ) ) ;
#25748=CARTESIAN_POINT ( 'NONE',  ( 51.06335740850991556, -4.023874009802445251, 1.198297772468548406 ) ) ;
#25750=CARTESIAN_POINT ( 'NONE',  ( 52.38400031671219637, 8.538946093000150839, 2.049999999999817302 ) ) ;
#25755=ORIENTED_EDGE ( 'NONE', *, *, #19713, .F. ) ;
#25763=CARTESIAN_POINT ( 'NONE',  ( 51.87582967299545800, 8.646477722258159915, -2.039222690361161661 ) ) ;
#25765=CARTESIAN_POINT ( 'NONE',  ( 53.91574522235882228, 6.672251602522421443, 1.774295301432037286 ) ) ;
#25777=CARTESIAN_POINT ( 'NONE',  ( 54.31409749668478071, 6.709390224138188863, -2.050000000000189004 ) ) ;
#25778=CARTESIAN_POINT ( 'NONE',  ( 53.29715246084701619, 4.966963424194753784, 1.611982351028472760 ) ) ;
#25785=DIRECTION ( 'NONE',  ( 0.000000000000000000, -1.224646799147285661E-16, 1.000000000000000000 ) ) ;
#25796=CARTESIAN_POINT ( 'NONE',  ( 50.35762544161296006, 8.151359338959887069, 2.008578643762515714 ) ) ;
#25808=CARTESIAN_POINT ( 'NONE',  ( 50.80000000000002558, -4.291790910095608425, 1.352971095042303507 ) ) ;
#25817=CARTESIAN_POINT ( 'NONE',  ( 47.00000000000003553, 2.428612866367529932E-14, 4.199999999999828759 ) ) ;
#25836=ORIENTED_EDGE ( 'NONE', *, *, #27126, .F. ) ;
#25858=DIRECTION ( 'NONE',  ( 0.7313537016191670181, 0.6819983600625022513, -2.468850131082252327E-15 ) ) ;
#25862=VECTOR ( 'NONE', #28744, 1000.000000000000000 ) ;
#25883=CARTESIAN_POINT ( 'NONE',  ( 51.88812122917401837, 8.998461838226445408, 1.949999999999818767 ) ) ;
#25885=CARTESIAN_POINT ( 'NONE',  ( 51.70000000000002416, 2.428612866367529932E-14, -1.805095852181900386E-13 ) ) ;
#25895=CARTESIAN_POINT ( 'NONE',  ( 41.48619405471883681, -151.3359592902622239, -1.950000000000163380 ) ) ;
#25900=CARTESIAN_POINT ( 'NONE',  ( 53.87654288987801721, 4.973000991543902849, 2.049999999999811973 ) ) ;
#25922=EDGE_CURVE ( 'NONE', #11599, #23041, #22601, .T. ) ;
#25936=FACE_OUTER_BOUND ( 'NONE', #25218, .T. ) ;
#25940=EDGE_CURVE ( 'NONE', #107, #24006, #12475, .T. ) ;
#25945=FACE_OUTER_BOUND ( 'NONE', #4145, .T. ) ;
#25951=SHAPE_DEFINITION_REPRESENTATION ( #2990, #549 ) ;
#25954=VERTEX_POINT ( 'NONE', #29661 ) ;
#25967=DIRECTION ( 'NONE',  ( 3.304235192336781034E-15, 0.000000000000000000, 1.000000000000000000 ) ) ;
#25970=DIRECTION ( 'NONE',  ( 3.016910393003118404E-15, 0.000000000000000000, 1.000000000000000000 ) ) ;
#25976=CARTESIAN_POINT ( 'NONE',  ( 47.10000000000000853, -3.637377585518695611, -2.099877210783201331 ) ) ;
#25984=ORIENTED_EDGE ( 'NONE', *, *, #2655, .F. ) ;
#25987=CARTESIAN_POINT ( 'NONE',  ( 0.000000000000000000, 0.000000000000000000, 0.000000000000000000 ) ) ;
#26001=CARTESIAN_POINT ( 'NONE',  ( 51.80000000000001137, -4.003661535119149129, -1.269131321892099207 ) ) ;
#26008=CARTESIAN_POINT ( 'NONE',  ( 54.15673930838963912, 5.684321142249388892, 2.049999999999811529 ) ) ;
#26011=ADVANCED_FACE ( 'NONE', ( #10668 ), #23183, .F. ) ;
#26019=EDGE_LOOP ( 'NONE', ( #9806, #2154, #11001, #19282, #7292, #8457, #14184, #18453 ) ) ;
#26028=VERTEX_POINT ( 'NONE', #10522 ) ;
#26047=LINE ( 'NONE', #11314, #29946 ) ;
#26048=ORIENTED_EDGE ( 'NONE', *, *, #11056, .F. ) ;
#26056=CARTESIAN_POINT ( 'NONE',  ( 52.41206581543988108, 8.644163850305695007, 2.049999999999817302 ) ) ;
#26059=CARTESIAN_POINT ( 'NONE',  ( 51.06382050520482352, -3.930543434675132008, -1.171429914303246056 ) ) ;
#26079=AXIS2_PLACEMENT_3D ( 'NONE', #25808, #19014, #28018 ) ;
#26089=ORIENTED_EDGE ( 'NONE', *, *, #646, .F. ) ;
#26105=DIRECTION ( 'NONE',  ( -0.9993908270190957621, 0.03489949670250097613, 3.491481338843133355E-15 ) ) ;
#26109=CARTESIAN_POINT ( 'NONE',  ( 50.87477060347374902, 8.633605004118187765, 1.549999999999822631 ) ) ;
#26122=EDGE_CURVE ( 'NONE', #4199, #21532, #13647, .T. ) ;
#26127=VECTOR ( 'NONE', #9202, 1000.000000000000000 ) ;
#26130=CARTESIAN_POINT ( 'NONE',  ( 47.19756905715325956, -4.191177329985519506, -1.624749424009585885 ) ) ;
#26132=CARTESIAN_POINT ( 'NONE',  ( 54.28867365409859502, 5.640057820322912363, -2.050000000000189004 ) ) ;
#26134=ORIENTED_EDGE ( 'NONE', *, *, #10851, .T. ) ;
#26142=ORIENTED_EDGE ( 'NONE', *, *, #24476, .F. ) ;
#26143=VERTEX_POINT ( 'NONE', #29170 ) ;
#26150=ORIENTED_EDGE ( 'NONE', *, *, #21867, .F. ) ;
#26154=AXIS2_PLACEMENT_3D ( 'NONE', #12457, #12768, #10571 ) ;
#26155=CARTESIAN_POINT ( 'NONE',  ( 51.67599336825460199, -3.859587729118648447, -1.644141655455117368 ) ) ;
#26156=ORIENTED_EDGE ( 'NONE', *, *, #111, .T. ) ;
#26160=VERTEX_POINT ( 'NONE', #17148 ) ;
#26165=LINE ( 'NONE', #17144, #29312 ) ;
#26168=EDGE_CURVE ( 'NONE', #18665, #20522, #15011, .T. ) ;
#26170=DIRECTION ( 'NONE',  ( 1.000000000000000000, 0.000000000000000000, -3.491481338843133355E-15 ) ) ;
#26175=DIRECTION ( 'NONE',  ( -0.9993908270190956511, 0.03489949670250089980, 3.491481338843132961E-15 ) ) ;
#26180=CARTESIAN_POINT ( 'NONE',  ( 53.86842434078439368, 7.562405067244617918, 2.049999999999813305 ) ) ;
#26186=EDGE_CURVE ( 'NONE', #6647, #14732, #9564, .T. ) ;
#26189=CARTESIAN_POINT ( 'NONE',  ( 30.51261366513614703, 7.487866468533194819, 1.424999999999893907 ) ) ;
#26191=EDGE_LOOP ( 'NONE', ( #25494, #16101, #15318, #5744, #19808, #15862 ) ) ;
#26200=CARTESIAN_POINT ( 'NONE',  ( 31.50816695980749671, 7.454773700472920872, 2.049999999999889244 ) ) ;
#26204=DIRECTION ( 'NONE',  ( 0.9993908270191184107, -0.03489949670185085034, -3.491481338843133355E-15 ) ) ;
#26215=CARTESIAN_POINT ( 'NONE',  ( 48.00000000000002132, -3.908336260473453727, 1.238913909465751972 ) ) ;
#26220=ADVANCED_FACE ( 'NONE', ( #22051 ), #4891, .T. ) ;
#26222=ORIENTED_EDGE ( 'NONE', *, *, #28181, .F. ) ;
#26228=ORIENTED_EDGE ( 'NONE', *, *, #12353, .F. ) ;
#26232=ORIENTED_EDGE ( 'NONE', *, *, #6908, .T. ) ;
#26245=CARTESIAN_POINT ( 'NONE',  ( 22.04321716858595082, 7.679566743993206934, 1.549999999999923217 ) ) ;
#26247=CARTESIAN_POINT ( 'NONE',  ( 54.41366571437519895, 6.718673005292168376, -2.050000000000189448 ) ) ;
#26254=CARTESIAN_POINT ( 'NONE',  ( 52.98657663771353299, 4.708191849549097086, 1.586975497715994221 ) ) ;
#26255=CARTESIAN_POINT ( 'NONE',  ( 53.94320358904982271, 6.378589075886260673, -0.8960560664367792638 ) ) ;
#26261=CARTESIAN_POINT ( 'NONE',  ( 51.70000000000001705, -4.079459090034584179, -2.128991905554068254 ) ) ;
#26268=CARTESIAN_POINT ( 'NONE',  ( 51.80000000000001137, -3.908336260473453727, -1.238913909466101027 ) ) ;
#26276=CARTESIAN_POINT ( 'NONE',  ( 47.00000000000003553, 6.982261990806648555E-14, 4.499999999999873879 ) ) ;
#26285=CARTESIAN_POINT ( 'NONE',  ( 29.88389444396583627, 6.456032137337936128, -1.950000000000103428 ) ) ;
#26294=CARTESIAN_POINT ( 'NONE',  ( 48.00000000000002132, -4.003661535119149129, 1.269131321891750375 ) ) ;
#26314=CARTESIAN_POINT ( 'NONE',  ( 51.80000000000001847, -3.701035844659721352, -1.983438066290037494 ) ) ;
#26318=EDGE_LOOP ( 'NONE', ( #5123, #13308, #22928, #29421, #20129 ) ) ;
#26334=CARTESIAN_POINT ( 'NONE',  ( 54.05511024441276646, 7.179753009059693269, 2.049999999999811529 ) ) ;
#26337=CARTESIAN_POINT ( 'NONE',  ( 54.28771311682444178, 6.706930398806282945, -2.050000000000190781 ) ) ;
#26342=CARTESIAN_POINT ( 'NONE',  ( 50.80000000000002558, -4.319730106884873244, 1.256953381662059277 ) ) ;
#26353=CARTESIAN_POINT ( 'NONE',  ( 22.07280086217093285, 8.086143481909154218, -1.950000000000076339 ) ) ;
#26355=CARTESIAN_POINT ( 'NONE',  ( 33.98208436257321097, 8.188484708538934953, 1.949999999999879385 ) ) ;
#26363=ADVANCED_FACE ( 'NONE', ( #3508 ), #8244, .T. ) ;
#26373=ORIENTED_EDGE ( 'NONE', *, *, #5551, .T. ) ;
#26384=ORIENTED_EDGE ( 'NONE', *, *, #24665, .F. ) ;
#26398=AXIS2_PLACEMENT_3D ( 'NONE', #8085, #17752, #15352 ) ;
#26404=ORIENTED_EDGE ( 'NONE', *, *, #30575, .F. ) ;
#26409=CARTESIAN_POINT ( 'NONE',  ( 54.02156981857547891, 6.375678713436270684, 1.975347020395713526 ) ) ;
#26419=DIRECTION ( 'NONE',  ( -1.000000000000000000, -0.000000000000000000, 3.491481338843133355E-15 ) ) ;
#26426=EDGE_CURVE ( 'NONE', #29340, #9758, #24950, .T. ) ;
#26438=CARTESIAN_POINT ( 'NONE',  ( 22.56915537023571261, 6.668482724649285487, -1.950000000000079226 ) ) ;
#26486=CARTESIAN_POINT ( 'NONE',  ( 54.38834443889974324, 6.716312293568780234, -2.020139939762307879 ) ) ;
#26497=CARTESIAN_POINT ( 'NONE',  ( 50.35762544161294585, 8.151359338959888845, -1.950000000000174927 ) ) ;
#26524=EDGE_LOOP ( 'NONE', ( #16710, #11629, #18152, #24426 ) ) ;
#26530=CARTESIAN_POINT ( 'NONE',  ( 22.08713154258123978, 7.931348155120199195, -2.050000000000076650 ) ) ;
#26533=CARTESIAN_POINT ( 'NONE',  ( 51.70000000000000995, 4.174380580618773706, -1.932497546739578631 ) ) ;
#26556=CARTESIAN_POINT ( 'NONE',  ( 53.81464057712624793, 5.799094425976102585, -1.402257306246839752 ) ) ;
#26579=LINE ( 'NONE', #29278, #4074 ) ;
#26585=CARTESIAN_POINT ( 'NONE',  ( 47.27788309694084745, -3.792101016927676316, -1.560991511224512740 ) ) ;
#26588=DIRECTION ( 'NONE',  ( 0.000000000000000000, 0.8740818021021506956, -0.4857787595540346559 ) ) ;
#26594=CARTESIAN_POINT ( 'NONE',  ( 53.32367365360940425, 7.956671815864365449, -1.890488970402769198 ) ) ;
#26595=AXIS2_PLACEMENT_3D ( 'NONE', #29087, #23881, #29250 ) ;
#26597=CARTESIAN_POINT ( 'NONE',  ( 51.88812122917230596, 8.998461838226505805, 2.049999999999819522 ) ) ;
#26598=CARTESIAN_POINT ( 'NONE',  ( 22.58884618656104593, 6.655783678991567420, 1.424999999999921663 ) ) ;
#26601=VECTOR ( 'NONE', #17488, 1000.000000000000114 ) ;
#26613=VERTEX_POINT ( 'NONE', #16161 ) ;
#26615=CARTESIAN_POINT ( 'NONE',  ( 47.12445916330874951, -4.150097527438618705, 1.728039211944948139 ) ) ;
#26620=CARTESIAN_POINT ( 'NONE',  ( 51.60223906999866728, -3.901712759401290143, -1.540267080488221030 ) ) ;
#26628=EDGE_LOOP ( 'NONE', ( #3985, #18809, #2939, #2932 ) ) ;
#26632=CARTESIAN_POINT ( 'NONE',  ( 53.25573957143294734, 8.250120694359615925, -2.050000000000185452 ) ) ;
#26643=ADVANCED_FACE ( 'NONE', ( #4734 ), #11, .F. ) ;
#26649=LINE ( 'NONE', #9717, #14433 ) ;
#26650=CARTESIAN_POINT ( 'NONE',  ( 47.38241355479843264, -4.256399122627302134, -1.449625929767729193 ) ) ;
#26656=CARTESIAN_POINT ( 'NONE',  ( 51.26902472369699382, -3.881932310064108549, -1.329369065055225452 ) ) ;
#26664=VERTEX_POINT ( 'NONE', #6986 ) ;
#26678=CARTESIAN_POINT ( 'NONE',  ( 31.50816695936848433, 7.454773701384803886, 1.949999999999889377 ) ) ;
#26695=CARTESIAN_POINT ( 'NONE',  ( 51.97945110550962511, 4.337541896208987779, 2.049999999999818190 ) ) ;
#26704=PLANE ( 'NONE',  #23104 ) ;
#26711=CARTESIAN_POINT ( 'NONE',  ( 23.93113343277027738, 5.410774079442639106, 1.949999999999916023 ) ) ;
#26716=ORIENTED_EDGE ( 'NONE', *, *, #8809, .T. ) ;
#26717=CARTESIAN_POINT ( 'NONE',  ( 47.10000000000002274, 2.428612866367529932E-14, -1.644487710595116631E-13 ) ) ;
#26724=CARTESIAN_POINT ( 'NONE',  ( 51.39453088482484588, 4.389042235173731932, -1.550000000000179012 ) ) ;
#26725=CARTESIAN_POINT ( 'NONE',  ( 22.32336313483207135, 6.618105965108083133, 1.549999999999922107 ) ) ;
#26731=CARTESIAN_POINT ( 'NONE',  ( 51.80000000000002558, 6.475000000000061817, 2.049999999999819522 ) ) ;
#26734=DIRECTION ( 'NONE',  ( -0.09218405009745890555, 0.9957419851084061690, 4.429949212628659047E-16 ) ) ;
#26759=CARTESIAN_POINT ( 'NONE',  ( 27.87224558658655482, 5.458855767854803531, -1.950000000000095435 ) ) ;
#26766=VERTEX_POINT ( 'NONE', #10705 ) ;
#26786=ORIENTED_EDGE ( 'NONE', *, *, #357, .F. ) ;
#26788=VECTOR ( 'NONE', #23911, 1000.000000000000114 ) ;
#26805=VERTEX_POINT ( 'NONE', #25742 ) ;
#26815=DIRECTION ( 'NONE',  ( 0.9993908270190956511, -0.03489949670250202390, -3.491481338843132961E-15 ) ) ;
#26818=EDGE_LOOP ( 'NONE', ( #18477, #21958, #3990, #30974 ) ) ;
#26823=CARTESIAN_POINT ( 'NONE',  ( 32.57869118458520319, 7.908463456459324803, 1.949999999999884936 ) ) ;
#26827=CARTESIAN_POINT ( 'NONE',  ( 51.29845177546386026, 3.894758067259835421, -2.050000000000178790 ) ) ;
#26837=CARTESIAN_POINT ( 'NONE',  ( 52.54946733419066618, 4.465216787881845839, 1.565330858589529806 ) ) ;
#26839=ADVANCED_FACE ( 'NONE', ( #29863 ), #27811, .T. ) ;
#26847=CARTESIAN_POINT ( 'NONE',  ( 27.27214205000342062, 5.011961650406415281, -1.950000000000094769 ) ) ;
#26858=CARTESIAN_POINT ( 'NONE',  ( 53.75952070206891875, 7.747157889885662563, -2.050000000000187228 ) ) ;
#26868=CARTESIAN_POINT ( 'NONE',  ( 54.11548317488421134, 5.698162681109456784, 2.049999999999810640 ) ) ;
#26876=CARTESIAN_POINT ( 'NONE',  ( 22.07280086217093640, 8.086143481909152442, -1.950000000000076339 ) ) ;
#26880=CARTESIAN_POINT ( 'NONE',  ( 53.43503425481907954, 4.477923827963745218, 2.048707174794345942 ) ) ;
#26887=AXIS2_PLACEMENT_3D ( 'NONE', #27977, #28138, #1387 ) ;
#26890=CARTESIAN_POINT ( 'NONE',  ( 51.89161117884413699, 9.098400920926795976, -2.050000000000180123 ) ) ;
#26893=CARTESIAN_POINT ( 'NONE',  ( 24.09848814319705568, 5.630607826402612481, -1.950000000000083666 ) ) ;
#26900=CARTESIAN_POINT ( 'NONE',  ( 22.07284336892448096, 7.567314370317718364, 1.424999999999923439 ) ) ;
#26943=CARTESIAN_POINT ( 'NONE',  ( 51.80000000000002558, 3.850000000000016520, 1.678541033159270279 ) ) ;
#26950=DIRECTION ( 'NONE',  ( 0.9993908270190956511, -0.03489949670250202390, -3.491481338843132961E-15 ) ) ;
#26953=CARTESIAN_POINT ( 'NONE',  ( 47.06312566212017146, 8.366466760780054912, 1.949999999999836087 ) ) ;
#26963=CARTESIAN_POINT ( 'NONE',  ( 25.08803375996945917, 5.428914793826548291, 2.049999999999911893 ) ) ;
#26987=DIRECTION ( 'NONE',  ( 0.9993908270190956511, -0.03489949670250202390, -3.491481338843132961E-15 ) ) ;
#26990=CARTESIAN_POINT ( 'NONE',  ( 54.18129837870574050, 6.362043366690858903, -2.050000000000185008 ) ) ;
#26996=CARTESIAN_POINT ( 'NONE',  ( 29.93605863095885056, 6.616288078318222077, -2.050000000000103295 ) ) ;
#27002=CARTESIAN_POINT ( 'NONE',  ( 52.48717296556561251, 8.620750214766545128, -2.050000000000182343 ) ) ;
#27005=TOROIDAL_SURFACE ( 'NONE', #19951, 2.525000000001608846, 0.1000000000000000056 ) ;
#27014=CARTESIAN_POINT ( 'NONE',  ( 54.33851379069789544, 5.996232874381098199, 2.046523307115193369 ) ) ;
#27025=CARTESIAN_POINT ( 'NONE',  ( 51.80000000000001847, 2.428612866367529932E-14, -1.808587333520743709E-13 ) ) ;
#27050=CARTESIAN_POINT ( 'NONE',  ( 30.02700392305997212, 6.560679691584609508, 1.424999999999895239 ) ) ;
#27059=AXIS2_PLACEMENT_3D ( 'NONE', #1768, #26170, #21433 ) ;
#27094=ORIENTED_EDGE ( 'NONE', *, *, #19121, .T. ) ;
#27099=DIRECTION ( 'NONE',  ( 3.016910393003118404E-15, 0.000000000000000000, 1.000000000000000000 ) ) ;
#27100=CARTESIAN_POINT ( 'NONE',  ( 52.79530352569713614, 4.045408597361428882, 0.6880653358388769680 ) ) ;
#27101=CARTESIAN_POINT ( 'NONE',  ( 47.00000000000002842, -3.994701997234459068, 2.069753729861246061 ) ) ;
#27115=CARTESIAN_POINT ( 'NONE',  ( 48.00000000000002842, -4.387164041431067751, 1.383037119376590685 ) ) ;
#27123=CARTESIAN_POINT ( 'NONE',  ( 25.69798005929094131, 5.334073409755834660, 2.049999999999910116 ) ) ;
#27124=ORIENTED_EDGE ( 'NONE', *, *, #28923, .F. ) ;
#27126=EDGE_CURVE ( 'NONE', #14388, #9993, #22256, .T. ) ;
#27129=CARTESIAN_POINT ( 'NONE',  ( 53.05250010753324830, 4.165967808473761913, -2.050000000000185008 ) ) ;
#27135=CIRCLE ( 'NONE', #1345, 4.199999999999993072 ) ;
#27136=B_SPLINE_CURVE_WITH_KNOTS ( 'NONE', 3,
 ( #9316, #6948, #20883, #6472, #16612, #8999, #26254, #28150, #4562, #14209, #31154, #3934, #25778, #13574, #23412, #23262, #11209, #15267, #16764, #1026, #128, #16910 ),
 .UNSPECIFIED., .F., .F.,
 ( 4, 2, 2, 2, 2, 1, 2, 2, 1, 2, 2, 4 ),
 ( 0.000000000000000000, 0.1038980121052294342, 0.1558470181578441305, 0.2077960242104588684, 0.2337705272367660847, 0.2467577787499208308, 0.2483811851890659617, 0.2500045916282110925, 0.2532514045065013542, 0.2597450302630850971, 0.3116940363157674199, 0.4155920484211318988 ),
 .UNSPECIFIED. ) ;
#27141=CARTESIAN_POINT ( 'NONE',  ( 51.87416143049283335, 8.598705507415685290, -1.950000000000180256 ) ) ;
#27144=VERTEX_POINT ( 'NONE', #10349 ) ;
#27158=CARTESIAN_POINT ( 'NONE',  ( 51.52173077008821167, -4.267091652301652438, -1.720255306494824055 ) ) ;
#27159=ORIENTED_EDGE ( 'NONE', *, *, #2975, .T. ) ;
#27162=CARTESIAN_POINT ( 'NONE',  ( 33.40812713680993085, 8.122903765861718028, -2.049999999999987832 ) ) ;
#27171=CARTESIAN_POINT ( 'NONE',  ( 53.31611809544273939, 8.197428291949847790, -2.050000000000185452 ) ) ;
#27186=CARTESIAN_POINT ( 'NONE',  ( 54.40373534988020765, 5.983016911212706290, -1.963089969304966820 ) ) ;
#27187=ORIENTED_EDGE ( 'NONE', *, *, #15658, .T. ) ;
#27192=CARTESIAN_POINT ( 'NONE',  ( 53.53640187423193453, 5.215699251213354870, 1.635615235160198466 ) ) ;
#27203=CARTESIAN_POINT ( 'NONE',  ( 51.80000048029783244, 4.021162535479849254, 2.019963026417355589 ) ) ;
#27210=EDGE_CURVE ( 'NONE', #12796, #13195, #14489, .T. ) ;
#27217=CARTESIAN_POINT ( 'NONE',  ( 53.88560433715219489, 6.996395185205533274, -1.802990336641044244 ) ) ;
#27220=CARTESIAN_POINT ( 'NONE',  ( 28.65063797331448825, 5.832638074306361275, 2.049999999999899902 ) ) ;
#27244=ORIENTED_EDGE ( 'NONE', *, *, #19445, .T. ) ;
#27246=CARTESIAN_POINT ( 'NONE',  ( 52.98658227084825256, 8.418175601153722099, -2.050000000000184563 ) ) ;
#27249=CARTESIAN_POINT ( 'NONE',  ( 51.67583320948680381, -3.859603212985638354, 1.644059474114338615 ) ) ;
#27265=CARTESIAN_POINT ( 'NONE',  ( 47.88166157169970916, -4.387164033828454102, 1.383037143493017984 ) ) ;
#27285=CARTESIAN_POINT ( 'NONE',  ( 24.17629218419978798, 5.599093920765381149, 1.949999999999914468 ) ) ;
#27288=DIRECTION ( 'NONE',  ( -0.7313537016191670181, -0.6819983600625022513, 2.468850131082252327E-15 ) ) ;
#27297=CIRCLE ( 'NONE', #17707, 0.1000000000000001443 ) ;
#27298=CARTESIAN_POINT ( 'NONE',  ( 51.87416143049283335, 8.598705507415687066, -1.976179938780094680 ) ) ;
#27313=ORIENTED_EDGE ( 'NONE', *, *, #3436, .F. ) ;
#27315=CARTESIAN_POINT ( 'NONE',  ( 53.92227517398921322, 6.075005530725110958, -1.819853284099130386 ) ) ;
#27319=CARTESIAN_POINT ( 'NONE',  ( 32.30803788440152857, 7.816246120666627384, -2.049999999999984723 ) ) ;
#27321=CARTESIAN_POINT ( 'NONE',  ( 48.00000000000002132, -3.908336260473453727, 1.238913909465751972 ) ) ;
#27325=CARTESIAN_POINT ( 'NONE',  ( 53.60047708782973075, 7.640852521089409599, -2.050000000000185896 ) ) ;
#27327=CIRCLE ( 'NONE', #542, 0.1000000000000000472 ) ;
#27331=PRODUCT_DEFINITION ( 'UNKNOWN', '', #22751, #1238 ) ;
#27334=( BOUNDED_SURFACE ( )  B_SPLINE_SURFACE ( 2, 3, ( 
 ( #1204, #20552, #30183, #586, #10245, #19917, #27192, #5501, #15154, #24809, #6441, #25431, #23232, #28284, #8644, #14015, #6596, #23072 ),
 ( #4366, #23706, #13700, #4057, #28596, #30968, #11662, #15782, #3733, #30339, #1665, #8960, #30484, #30816, #13375, #25750, #18950, #23533 ),
 ( #1368, #1833, #8787, #11034, #13550, #1996, #25900, #6743, #21340, #18640, #1521, #16254, #16404, #11182, #11324, #6275, #21185, #20709 ),
 ( #28118, #4206, #13844, #30648, #11506, #20856, #21009, #18478, #18324, #23382, #27961, #9133, #18797, #16102, #28439, #26056, #9287, #15921 ),
 ( #3901, #25583, #24317, #7370, #4677, #16578, #14333, #14497, #2147, #19584, #24003, #2304, #12416, #16735, #29222, #28762, #7220, #12130 ) ),
 .UNSPECIFIED., .F., .F., .F. ) 
 B_SPLINE_SURFACE_WITH_KNOTS ( ( 3, 2, 3 ),
 ( 4, 2, 2, 2, 2, 2, 2, 2, 4 ),
 ( 0.000000000000000000, 1.000000000000000000, 1.010000000000000009 ),
 ( 1.413716694115406902, 1.826050729899067360, 2.238384765682727817, 2.650718801466387831, 3.063052837250048288, 3.475386873033708746, 3.887720908817368759, 4.300054944601029661, 4.712388980384689674 ),
 .UNSPECIFIED. ) 
 GEOMETRIC_REPRESENTATION_ITEM ( )  RATIONAL_B_SPLINE_SURFACE ( (
 ( 1.000000000000000000, 1.000000000000000000, 1.000000000000000000, 1.000000000000000000, 1.000000000000000000, 1.000000000000000000, 1.000000000000000000, 1.000000000000000000, 1.000000000000000000, 1.000000000000000000, 1.000000000000000000, 1.000000000000000000, 1.000000000000000000, 1.000000000000000000, 1.000000000000000000, 1.000000000000000000, 1.000000000000000000, 1.000000000000000000),
 ( 0.7071067811865476838, 0.7071067811865476838, 0.7071067811865473507, 0.7071067811865473507, 0.7071067811865476838, 0.7071067811865476838, 0.7071067811865476838, 0.7071067811865476838, 0.7071067811865473507, 0.7071067811865473507, 0.7071067811865476838, 0.7071067811865476838, 0.7071067811865480168, 0.7071067811865480168, 0.7071067811865450192, 0.7071067811865450192, 0.7071067811865467956, 0.7071067811865467956),
 ( 1.000000000000000000, 1.000000000000000000, 1.000000000000000000, 1.000000000000000000, 1.000000000000000000, 1.000000000000000000, 1.000000000000000000, 1.000000000000000000, 1.000000000000000000, 1.000000000000000000, 1.000000000000000000, 1.000000000000000000, 1.000000000000000000, 1.000000000000000000, 1.000000000000000000, 1.000000000000000000, 1.000000000000000000, 1.000000000000000000),
 ( 1.000000000000000000, 1.000000000000000000, 1.000000000000000000, 1.000000000000000000, 1.000000000000000000, 1.000000000000000000, 1.000000000000000000, 1.000000000000000000, 1.000000000000000000, 1.000000000000000000, 1.000000000000000000, 1.000000000000000000, 1.000000000000000000, 1.000000000000000000, 1.000000000000000000, 1.000000000000000000, 1.000000000000000000, 1.000000000000000000),
 ( 1.000000000000000000, 1.000000000000000000, 1.000000000000000000, 1.000000000000000000, 1.000000000000000000, 1.000000000000000000, 1.000000000000000000, 1.000000000000000000, 1.000000000000000000, 1.000000000000000000, 1.000000000000000000, 1.000000000000000000, 1.000000000000000000, 1.000000000000000000, 1.000000000000000000, 1.000000000000000000, 1.000000000000000000, 1.000000000000000000) ) ) 
 REPRESENTATION_ITEM ( '' )  SURFACE ( )  );
#27338=CARTESIAN_POINT ( 'NONE',  ( 54.27669070682345165, 6.362024491156814676, 2.049999999999809308 ) ) ;
#27343=ADVANCED_FACE ( 'NONE', ( #1616 ), #24101, .T. ) ;
#27344=CARTESIAN_POINT ( 'NONE',  ( 51.70000000000002416, 4.174380580618757719, 1.932497546739255556 ) ) ;
#27348=CARTESIAN_POINT ( 'NONE',  ( 51.77061368361890459, -3.672971185000162730, -1.825899123715961414 ) ) ;
#27354=CARTESIAN_POINT ( 'NONE',  ( 52.94611566430813809, 4.198287402864775864, 2.047134521670517682 ) ) ;
#27366=AXIS2_PLACEMENT_3D ( 'NONE', #11064, #25623, #25785 ) ;
#27387=CARTESIAN_POINT ( 'NONE',  ( 31.20024169076945242, 7.859880411735725048, -1.425000000000108402 ) ) ;
#27398=CARTESIAN_POINT ( 'NONE',  ( 51.80000000000001137, 8.600000000000106226, -2.050000000000179678 ) ) ;
#27405=CARTESIAN_POINT ( 'NONE',  ( 30.51261366513613993, 7.487866468533194819, -1.425000000000106404 ) ) ;
#27408=CARTESIAN_POINT ( 'NONE',  ( 52.42865501881644263, 4.000228981067450285, -2.045760679945879623 ) ) ;
#27422=CARTESIAN_POINT ( 'NONE',  ( 31.30720621464601905, 7.411182539856417506, -1.550000000000108624 ) ) ;
#27425=ORIENTED_EDGE ( 'NONE', *, *, #13596, .F. ) ;
#27429=ORIENTED_EDGE ( 'NONE', *, *, #31055, .F. ) ;
#27433=ORIENTED_EDGE ( 'NONE', *, *, #11867, .F. ) ;
#27436=CARTESIAN_POINT ( 'NONE',  ( 22.49391462655620444, 6.944224163294628660, 2.049999999999920774 ) ) ;
#27451=CARTESIAN_POINT ( 'NONE',  ( 53.81456880582373259, 5.799118505022251568, 1.784642093723081357 ) ) ;
#27456=DIRECTION ( 'NONE',  ( 1.000000000000000000, 0.000000000000000000, -3.469446951951483476E-15 ) ) ;
#27462=CARTESIAN_POINT ( 'NONE',  ( 51.06312929986522420, -4.312041630646782586, -1.282098934413016700 ) ) ;
#27466=CARTESIAN_POINT ( 'NONE',  ( 22.49391462655623997, 6.944224163294429708, -2.050000000000078426 ) ) ;
#27467=CARTESIAN_POINT ( 'NONE',  ( 50.80000000000001137, -4.387164041431065975, -1.383037119376935742 ) ) ;
#27479=CARTESIAN_POINT ( 'NONE',  ( 51.42173091724420431, -4.356630359622029047, 1.481809601934319209 ) ) ;
#27486=CARTESIAN_POINT ( 'NONE',  ( 54.44737856558258926, 6.357064942762717052, -1.856154119295183591E-13 ) ) ;
#27500=DIRECTION ( 'NONE',  ( 0.000000000000000000, 0.000000000000000000, 1.000000000000000000 ) ) ;
#27504=CARTESIAN_POINT ( 'NONE',  ( 51.80000000000002558, 3.850000000000016520, 1.678541033159270279 ) ) ;
#27506=CARTESIAN_POINT ( 'NONE',  ( 22.04321716858595082, 7.679566743993206934, 1.549999999999923217 ) ) ;
#27514=VECTOR ( 'NONE', #2185, 1000.000000000000000 ) ;
#27534=AXIS2_PLACEMENT_3D ( 'NONE', #25075, #20206, #3411 ) ;
#27543=DIRECTION ( 'NONE',  ( -0.9993908270190957621, 0.03489949670250202390, 3.491481338843133355E-15 ) ) ;
#27544=TOROIDAL_SURFACE ( 'NONE', #14911, 160.5997717543497743, 0.1000000000000000056 ) ;
#27545=CARTESIAN_POINT ( 'NONE',  ( 52.80702527127468926, 4.040723488129245311, -2.050000000000183675 ) ) ;
#27563=PLANE ( 'NONE',  #22730 ) ;
#27565=VERTEX_POINT ( 'NONE', #18241 ) ;
#27566=CARTESIAN_POINT ( 'NONE',  ( 53.60047708782973785, 7.640852521089409599, 2.049999999999813305 ) ) ;
#27567=CARTESIAN_POINT ( 'NONE',  ( 29.25706191173315673, 5.994885333997870269, -1.550000000000101741 ) ) ;
#27574=DIRECTION ( 'NONE',  ( -1.000000000000000000, -0.000000000000000000, 3.491481338843133355E-15 ) ) ;
#27577=CARTESIAN_POINT ( 'NONE',  ( 34.27001433279279752, 8.197396758520717697, 1.949999999999880274 ) ) ;
#27585=CARTESIAN_POINT ( 'NONE',  ( 22.09542497983118281, 7.445411299649673964, 2.050000000000058886 ) ) ;
#27595=DIRECTION ( 'NONE',  ( -0.9993908270190956511, 0.03489949670250202390, 3.491481338843132961E-15 ) ) ;
#27598=DIRECTION ( 'NONE',  ( 3.491481338843133355E-15, -0.000000000000000000, 1.000000000000000000 ) ) ;
#27602=CARTESIAN_POINT ( 'NONE',  ( 51.65293807187808994, 3.825852911387368493, -2.050000000000177902 ) ) ;
#27606=CARTESIAN_POINT ( 'NONE',  ( 53.56882961073743843, 7.945105661027664468, -2.050000000000185896 ) ) ;
#27611=AXIS2_PLACEMENT_3D ( 'NONE', #8737, #17952, #25383 ) ;
#27612=VERTEX_POINT ( 'NONE', #811 ) ;
#27644=CARTESIAN_POINT ( 'NONE',  ( 50.93211418564875004, -4.319730106544481529, 1.256953381563011618 ) ) ;
#27646=CIRCLE ( 'NONE', #3889, 4.500000000000037303 ) ;
#27654=CARTESIAN_POINT ( 'NONE',  ( 54.44724579895265748, 6.358489013468038742, 1.963089969304595783 ) ) ;
#27664=CARTESIAN_POINT ( 'NONE',  ( 51.87416143049283335, 8.598705507415685290, -1.950000000000180256 ) ) ;
#27669=ORIENTED_EDGE ( 'NONE', *, *, #15906, .T. ) ;
#27689=CARTESIAN_POINT ( 'NONE',  ( 50.31971926781695004, 8.252744006147214151, 2.049999999999824407 ) ) ;
#27694=VECTOR ( 'NONE', #16743, 999.9999999999998863 ) ;
#27699=DIRECTION ( 'NONE',  ( -3.489354422748178582E-15, 1.218509414717996338E-16, -1.000000000000000000 ) ) ;
#27714=CARTESIAN_POINT ( 'NONE',  ( 53.30599709427681177, 4.975793220244357329, -1.612824162456762300 ) ) ;
#27716=( BOUNDED_CURVE ( )  B_SPLINE_CURVE ( 3, ( #18846, #25796, #28653, #1712 ),
 .UNSPECIFIED., .F., .T. ) 
 B_SPLINE_CURVE_WITH_KNOTS ( ( 4, 4 ),
 ( 1.011983630320553299E-14, 1.570796326794897890 ),
 .UNSPECIFIED. ) 
 CURVE ( )  GEOMETRIC_REPRESENTATION_ITEM ( )  RATIONAL_B_SPLINE_CURVE ( ( 1.000000000000000000, 0.8047378541243670469, 0.8047378541243670469, 1.000000000000000000 ) ) 
 REPRESENTATION_ITEM ( '' )  );
#27720=CARTESIAN_POINT ( 'NONE',  ( 53.34494210428217542, 4.987020249080358347, -1.614082030464848438 ) ) ;
#27725=CARTESIAN_POINT ( 'NONE',  ( 41.48619405471883681, -151.3359592902621955, -1.950000000000163380 ) ) ;
#27726=AXIS2_PLACEMENT_3D ( 'NONE', #16657, #28681, #25970 ) ;
#27731=CARTESIAN_POINT ( 'NONE',  ( 51.73328143279135105, 4.175271471638106746, -1.930573136446366300 ) ) ;
#27739=CARTESIAN_POINT ( 'NONE',  ( 54.23625105546378933, 6.534957249981562022, 2.049999999999810640 ) ) ;
#27741=EDGE_CURVE ( 'NONE', #19028, #28904, #15997, .T. ) ;
#27747=B_SPLINE_CURVE_WITH_KNOTS ( 'NONE', 3,
 ( #18185, #27827, #6135, #15787, #13556, #25436, #18330, #3739, #6601, #20717, #13381, #30344, #23078, #1374, #11187, #8651, #27967, #6280, #15928, #30489, #25589, #6447, #3908, #23239, #16108, #23712, #31292, #17057, #4372, #9910, #28601, #11817, #6919, #24009, #26530, #2631 ),
 .UNSPECIFIED., .F., .F.,
 ( 4, 2, 2, 2, 2, 2, 2, 2, 2, 2, 2, 2, 2, 2, 2, 2, 2, 4 ),
 ( 0.000000000000000000, 0.001741378360725073316, 0.002612067541087599674, 0.003047412131268863178, 0.003482756721450126249, 0.004353445901812643716, 0.005224135082175161184, 0.006965513442900206527, 0.007836202623262724862, 0.008706891803625242329, 0.009577580983987759797, 0.01044827016435027900, 0.01131895934471279647, 0.01218964852507531393, 0.01262499311525657093, 0.01306033770543782620, 0.01349568229561908320, 0.01393102688580033846 ),
 .UNSPECIFIED. ) ;
#27752=EDGE_LOOP ( 'NONE', ( #11331, #18145, #24010, #23006 ) ) ;
#27772=PRESENTATION_STYLE_ASSIGNMENT (( #10990 ) ) ;
#27774=ORIENTED_EDGE ( 'NONE', *, *, #19750, .T. ) ;
#27783=EDGE_CURVE ( 'NONE', #9283, #23396, #23112, .T. ) ;
#27795=VECTOR ( 'NONE', #4417, 1000.000000000000000 ) ;
#27799=CARTESIAN_POINT ( 'NONE',  ( 47.00000000000002842, -3.700146292169669948, 1.985065161562699299 ) ) ;
#27802=CIRCLE ( 'NONE', #25263, 159.6997717543496833 ) ;
#27805=CARTESIAN_POINT ( 'NONE',  ( 53.97784470437120774, 5.744339954850582686, -2.010804190376556555 ) ) ;
#27807=CARTESIAN_POINT ( 'NONE',  ( 51.80000000000003268, -4.020776289669856673, 2.234582293948397691 ) ) ;
#27809=TOROIDAL_SURFACE ( 'NONE', #497, 4.500000000000037303, 0.1000000000000000056 ) ;
#27811=CYLINDRICAL_SURFACE ( 'NONE', #897, 160.6997717543497686 ) ;
#27814=CARTESIAN_POINT ( 'NONE',  ( 54.31535763113295445, 6.000143968236459457, -2.050000000000189004 ) ) ;
#27827=CARTESIAN_POINT ( 'NONE',  ( 33.97286272917381922, 8.288178785419178851, -2.050000000000117506 ) ) ;
#27851=CARTESIAN_POINT ( 'NONE',  ( 29.17657462828753268, 6.106387485306473906, 2.049999999999898570 ) ) ;
#27857=DIRECTION ( 'NONE',  ( -3.023770467182126270E-15, -0.4999707644721522182, -0.8660422822663637055 ) ) ;
#27865=DIRECTION ( 'NONE',  ( -9.754918421198722508E-16, 0.9601771338024398528, -0.2793919678926571337 ) ) ;
#27869=CARTESIAN_POINT ( 'NONE',  ( 52.41186875581714588, 8.643425072357743488, -2.050000000000182343 ) ) ;
#27877=CARTESIAN_POINT ( 'NONE',  ( 53.02518193390453405, 4.240975178678276336, -2.047385601739696082 ) ) ;
#27880=VERTEX_POINT ( 'NONE', #2690 ) ;
#27888=CARTESIAN_POINT ( 'NONE',  ( 54.24037840390755605, 6.535103219670295616, 2.049999999999810640 ) ) ;
#27897=DIRECTION ( 'NONE',  ( 0.000000000000000000, -1.224646799146977512E-16, 1.000000000000000000 ) ) ;
#27912=EDGE_CURVE ( 'NONE', #16106, #13475, #22612, .T. ) ;
#27914=DIRECTION ( 'NONE',  ( -1.000000000000000000, -0.000000000000000000, 3.491481338843133355E-15 ) ) ;
#27917=CARTESIAN_POINT ( 'NONE',  ( 54.19028661868582475, 6.697846887293304796, 2.049999999999810640 ) ) ;
#27935=CARTESIAN_POINT ( 'NONE',  ( 22.32354329814768334, 7.018810584857617663, -1.950000000000043698 ) ) ;
#27941=DIRECTION ( 'NONE',  ( -0.9993908270190956511, 0.03489949670250089980, 3.469446951951485842E-15 ) ) ;
#27943=CARTESIAN_POINT ( 'NONE',  ( 52.98236138753792801, 8.264679131573696935, -1.919164453910518375 ) ) ;
#27961=CARTESIAN_POINT ( 'NONE',  ( 54.16371155698127637, 6.950779743548840983, 2.049999999999811973 ) ) ;
#27963=LINE ( 'NONE', #28120, #23634 ) ;
#27966=ORIENTED_EDGE ( 'NONE', *, *, #1930, .F. ) ;
#27967=CARTESIAN_POINT ( 'NONE',  ( 27.52372483455771857, 5.460843285065334562, -2.050000000000095746 ) ) ;
#27970=DIRECTION ( 'NONE',  ( -3.489354422748178188E-15, 1.218509414717996091E-16, -1.000000000000000000 ) ) ;
#27975=EDGE_CURVE ( 'NONE', #29651, #15816, #21723, .T. ) ;
#27977=CARTESIAN_POINT ( 'NONE',  ( 51.80000000000001137, 6.475000000000062705, -2.050000000000180123 ) ) ;
#27987=DIRECTION ( 'NONE',  ( -3.489354422748178582E-15, 1.218509414717996338E-16, -1.000000000000000000 ) ) ;
#27991=EDGE_CURVE ( 'NONE', #25173, #737, #1445, .T. ) ;
#28000=CARTESIAN_POINT ( 'NONE',  ( 53.91582462592158720, 6.672259099522137582, -2.142504121165067499E-08 ) ) ;
#28001=CARTESIAN_POINT ( 'NONE',  ( 30.89639353480223960, 7.705332860780324644, -1.425000000000107514 ) ) ;
#28002=CARTESIAN_POINT ( 'NONE',  ( 51.77425608051891004, -4.052343190076493684, -1.949685991417844155 ) ) ;
#28018=DIRECTION ( 'NONE',  ( 0.000000000000000000, 0.000000000000000000, -1.000000000000000000 ) ) ;
#28029=CARTESIAN_POINT ( 'NONE',  ( 47.00000000000001421, -3.637377585518695611, -2.099877210783201331 ) ) ;
#28033=CARTESIAN_POINT ( 'NONE',  ( 52.72145679358934700, 4.007061708474140005, 2.049999999999815969 ) ) ;
#28041=CARTESIAN_POINT ( 'NONE',  ( 47.10000000000000853, -4.079448311123454296, -2.129011300494398018 ) ) ;
#28045=CARTESIAN_POINT ( 'NONE',  ( 22.10406324885627782, 7.468725723506255854, 1.949999999999923128 ) ) ;
#28051=VERTEX_POINT ( 'NONE', #11542 ) ;
#28057=AXIS2_PLACEMENT_3D ( 'NONE', #1467, #27914, #16039 ) ;
#28074=CARTESIAN_POINT ( 'NONE',  ( 51.80000000000001137, 6.475000000000062705, -2.050000000000180123 ) ) ;
#28085=CARTESIAN_POINT ( 'NONE',  ( 51.80000000000001847, 2.428612866367529932E-14, -1.808587333520743709E-13 ) ) ;
#28087=CARTESIAN_POINT ( 'NONE',  ( 22.72181155399563224, 6.520914524688375735, -1.950000000000079670 ) ) ;
#28108=DIRECTION ( 'NONE',  ( 3.489354422748178582E-15, -1.218509414717996338E-16, 1.000000000000000000 ) ) ;
#28118=CARTESIAN_POINT ( 'NONE',  ( 51.38880644991420610, 3.878826100321112413, 2.049999999999820410 ) ) ;
#28120=CARTESIAN_POINT ( 'NONE',  ( 22.04321716858593661, 7.679566743993218481, -2.050000000000076650 ) ) ;
#28121=CARTESIAN_POINT ( 'NONE',  ( 51.41512632536708338, -3.877460150898793145, -1.337636034594305245 ) ) ;
#28127=VECTOR ( 'NONE', #6159, 1000.000000000000000 ) ;
#28138=DIRECTION ( 'NONE',  ( 3.489354422748178582E-15, -1.218509414717996338E-16, 1.000000000000000000 ) ) ;
#28150=CARTESIAN_POINT ( 'NONE',  ( 53.12794425116820207, 4.814976926303064175, 1.597382792423633902 ) ) ;
#28160=ORIENTED_EDGE ( 'NONE', *, *, #11356, .T. ) ;
#28169=ORIENTED_EDGE ( 'NONE', *, *, #16041, .T. ) ;
#28175=CARTESIAN_POINT ( 'NONE',  ( 53.61897490378053277, 5.359699723822127559, -1.649481177327357662 ) ) ;
#28181=EDGE_CURVE ( 'NONE', #21603, #17195, #14537, .T. ) ;
#28187=DIRECTION ( 'NONE',  ( 9.754918421198724481E-16, -0.9601771338024399638, 0.2793919678926571892 ) ) ;
#28195=CARTESIAN_POINT ( 'NONE',  ( 46.99711047134479713, -4.086537470741383515, -2.116255473935157561 ) ) ;
#28200=B_SPLINE_CURVE_WITH_KNOTS ( 'NONE', 3,
 ( #18063, #1247, #8539, #3946, #18224, #16301, #21229, #28002, #1887, #13418 ),
 .UNSPECIFIED., .F., .F.,
 ( 4, 2, 2, 2, 4 ),
 ( 0.000000000000000000, 0.0003923015305839677226, 0.0007846030611679354451, 0.001176904591751903222, 0.001569206122335870890 ),
 .UNSPECIFIED. ) ;
#28207=CARTESIAN_POINT ( 'NONE',  ( 53.31680359303815919, 8.198234760421843959, 2.049999999999814193 ) ) ;
#28210=ADVANCED_FACE ( 'NONE', ( #5027 ), #9377, .T. ) ;
#28227=CARTESIAN_POINT ( 'NONE',  ( 29.64923672893718276, 6.300449151053643781, -1.425000000000103739 ) ) ;
#28232=DIRECTION ( 'NONE',  ( 0.7313537016191670181, 0.6819983600625022513, -2.468850131082252327E-15 ) ) ;
#28240=EDGE_CURVE ( 'NONE', #26143, #5179, #9765, .T. ) ;
#28252=STYLED_ITEM ( 'NONE', ( #24255 ), #2132 ) ;
#28255=VECTOR ( 'NONE', #23964, 1000.000000000000000 ) ;
#28261=ORIENTED_EDGE ( 'NONE', *, *, #4272, .F. ) ;
#28284=CARTESIAN_POINT ( 'NONE',  ( 53.16217804548193016, 8.131925109091586279, 1.902110155464532104 ) ) ;
#28287=SPHERICAL_SURFACE ( 'NONE', #1375, 0.1000000000000000056 ) ;
#28293=ADVANCED_FACE ( 'NONE', ( #22065 ), #23594, .T. ) ;
#28296=ORIENTED_EDGE ( 'NONE', *, *, #14247, .T. ) ;
#28310=DIRECTION ( 'NONE',  ( 3.489354422748178582E-15, -1.218509414717996338E-16, 1.000000000000000000 ) ) ;
#28320=VERTEX_POINT ( 'NONE', #21921 ) ;
#28324=DIRECTION ( 'NONE',  ( -1.000000000000000000, -0.000000000000000000, 3.491481338843133355E-15 ) ) ;
#28331=FACE_OUTER_BOUND ( 'NONE', #21105, .T. ) ;
#28336=DIRECTION ( 'NONE',  ( -0.9993908270190958731, 0.03489949670250085123, 3.435095992031088928E-15 ) ) ;
#28366=EDGE_CURVE ( 'NONE', #20869, #9056, #5426, .T. ) ;
#28370=VERTEX_POINT ( 'NONE', #15379 ) ;
#28380=CARTESIAN_POINT ( 'NONE',  ( 22.07284336892448096, 7.567314370317723693, -1.425000000000076428 ) ) ;
#28383=CARTESIAN_POINT ( 'NONE',  ( 22.07280086217095061, 8.086143481909148889, 1.949999999999923128 ) ) ;
#28426=DIRECTION ( 'NONE',  ( 9.754918421198724481E-16, 0.9601771338024399638, 0.2793919678926571892 ) ) ;
#28439=CARTESIAN_POINT ( 'NONE',  ( 52.98705886115022423, 8.418976914897422503, 2.049999999999815081 ) ) ;
#28457=CARTESIAN_POINT ( 'NONE',  ( 47.10000000000001563, -4.079459090034584179, 2.128991905553722308 ) ) ;
#28482=CARTESIAN_POINT ( 'NONE',  ( 22.06071280439820015, 8.185410187602871090, -1.425000000000076650 ) ) ;
#28506=FACE_OUTER_BOUND ( 'NONE', #16259, .T. ) ;
#28521=EDGE_LOOP ( 'NONE', ( #27966, #1583, #28160, #5090, #7071, #8011, #9378, #17234 ) ) ;
#28529=EDGE_LOOP ( 'NONE', ( #22026, #22732, #24897, #21166 ) ) ;
#28532=CARTESIAN_POINT ( 'NONE',  ( 29.45665666413593087, 6.177494273110403000, -1.425000000000101963 ) ) ;
#28541=DIRECTION ( 'NONE',  ( 0.000000000000000000, 0.000000000000000000, 1.000000000000000000 ) ) ;
#28546=CARTESIAN_POINT ( 'NONE',  ( 51.87765138016309407, 8.698644590117595499, 2.049999999999819522 ) ) ;
#28551=CARTESIAN_POINT ( 'NONE',  ( 54.29335997410981207, 6.002961067146851626, -2.050000000000190781 ) ) ;
#28553=ORIENTED_EDGE ( 'NONE', *, *, #26122, .T. ) ;
#28554=CARTESIAN_POINT ( 'NONE',  ( 22.58314801556728568, 7.622751244490449274, -1.425000000000078426 ) ) ;
#28560=ORIENTED_EDGE ( 'NONE', *, *, #13848, .T. ) ;
#28570=CARTESIAN_POINT ( 'NONE',  ( 33.98208436309214164, 8.188484713949170768, 2.049999999999878586 ) ) ;
#28571=VERTEX_POINT ( 'NONE', #7610 ) ;
#28580=DIRECTION ( 'NONE',  ( 0.000000000000000000, -1.000000000000000000, 0.000000000000000000 ) ) ;
#28590=CIRCLE ( 'NONE', #27059, 4.099999999999992539 ) ;
#28596=CARTESIAN_POINT ( 'NONE',  ( 52.88620718028473533, 4.625382794676503373, 2.049999999999815081 ) ) ;
#28601=CARTESIAN_POINT ( 'NONE',  ( 22.40895431619513900, 7.071232237904418128, -2.050000000000078870 ) ) ;
#28604=DIRECTION ( 'NONE',  ( -0.9993908270190957621, 0.03489949670250098307, 3.491481338843133355E-15 ) ) ;
#28619=VECTOR ( 'NONE', #12187, 1000.000000000000000 ) ;
#28620=CARTESIAN_POINT ( 'NONE',  ( 29.25706191173316739, 5.994885333997870269, 1.549999999999897904 ) ) ;
#28626=ORIENTED_EDGE ( 'NONE', *, *, #2294, .F. ) ;
#28653=CARTESIAN_POINT ( 'NONE',  ( 50.34192419032898158, 8.193354243125561709, 2.049999999999823963 ) ) ;
#28656=DIRECTION ( 'NONE',  ( -0.9956821769042226711, -0.09282781153979745292, 3.494196887668849000E-15 ) ) ;
#28657=CARTESIAN_POINT ( 'NONE',  ( 54.15673930838963912, 5.684321142249388892, 2.049999999999811529 ) ) ;
#28662=AXIS2_PLACEMENT_3D ( 'NONE', #16738, #2307, #11974 ) ;
#28672=CIRCLE ( 'NONE', #21619, 4.600000000000036948 ) ;
#28673=CARTESIAN_POINT ( 'NONE',  ( 47.00000000000000711, -4.020776289669854897, -2.234582293948742304 ) ) ;
#28674=AXIS2_PLACEMENT_3D ( 'NONE', #20305, #15535, #1427 ) ;
#28681=DIRECTION ( 'NONE',  ( -1.000000000000000000, 0.000000000000000000, 3.491481338843133355E-15 ) ) ;
#28688=ORIENTED_EDGE ( 'NONE', *, *, #15293, .F. ) ;
#28696=ADVANCED_FACE ( 'NONE', ( #2845 ), #17413, .T. ) ;
#28698=ORIENTED_EDGE ( 'NONE', *, *, #2186, .T. ) ;
#28725=CARTESIAN_POINT ( 'NONE',  ( 51.51923570830314247, -3.793498434807317743, -1.557570148623113937 ) ) ;
#28726=AXIS2_PLACEMENT_3D ( 'NONE', #4538, #18959, #28604 ) ;
#28729=CARTESIAN_POINT ( 'NONE',  ( 51.30583474879431094, -4.280467579807392120, 1.378329539256710312 ) ) ;
#28744=DIRECTION ( 'NONE',  ( 3.491481338843133355E-15, -0.000000000000000000, 1.000000000000000000 ) ) ;
#28762=CARTESIAN_POINT ( 'NONE',  ( 52.41226287506260917, 8.644902628253648302, 2.049999999999817302 ) ) ;
#28765=CARTESIAN_POINT ( 'NONE',  ( 51.30671737785521458, -3.991926107141777980, -1.294864543654180133 ) ) ;
#28776=CARTESIAN_POINT ( 'NONE',  ( 47.12246479398822885, -4.133513435957373083, 2.021478398489655159 ) ) ;
#28785=EDGE_CURVE ( 'NONE', #2006, #30563, #4698, .T. ) ;
#28787=EDGE_CURVE ( 'NONE', #3208, #29340, #390, .T. ) ;
#28793=CARTESIAN_POINT ( 'NONE',  ( 53.94287803706861695, 6.382080985259960038, -1.484311132272649436 ) ) ;
#28828=CARTESIAN_POINT ( 'NONE',  ( 47.10000000000000853, -4.020776289669854009, -2.234582293948742748 ) ) ;
#28838=ORIENTED_EDGE ( 'NONE', *, *, #25445, .F. ) ;
#28857=CARTESIAN_POINT ( 'NONE',  ( 53.87894805006523313, 4.971284855691957993, -2.050000000000188116 ) ) ;
#28858=DIRECTION ( 'NONE',  ( 0.000000000000000000, -0.8660422822663634834, -0.4999707644721521627 ) ) ;
#28874=CARTESIAN_POINT ( 'NONE',  ( 54.35699767715569664, 6.713389823568764569, -2.043118470513792140 ) ) ;
#28878=DIRECTION ( 'NONE',  ( -3.491481338843133355E-15, 0.000000000000000000, -1.000000000000000000 ) ) ;
#28889=FACE_OUTER_BOUND ( 'NONE', #31279, .T. ) ;
#28890=ORIENTED_EDGE ( 'NONE', *, *, #23612, .T. ) ;
#28904=VERTEX_POINT ( 'NONE', #29084 ) ;
#28905=ORIENTED_EDGE ( 'NONE', *, *, #4390, .F. ) ;
#28923=EDGE_CURVE ( 'NONE', #3746, #15927, #8993, .T. ) ;
#28939=ORIENTED_EDGE ( 'NONE', *, *, #27912, .T. ) ;
#28944=CARTESIAN_POINT ( 'NONE',  ( 47.28118949446516694, -3.793704335752947632, -1.557065711441589562 ) ) ;
#28950=CARTESIAN_POINT ( 'NONE',  ( 47.10000000000002274, 2.428612866367529932E-14, -1.644487710595116631E-13 ) ) ;
#28968=CARTESIAN_POINT ( 'NONE',  ( 25.89592582029650103, 5.217927461809758860, -1.950000000000090328 ) ) ;
#28972=CARTESIAN_POINT ( 'NONE',  ( 53.06648468529573393, 8.205141401880769791, -1.913421085928479259 ) ) ;
#28973=DIRECTION ( 'NONE',  ( -0.9993908270191184107, 0.03489949670185085034, 3.491481338843133355E-15 ) ) ;
#28985=CARTESIAN_POINT ( 'NONE',  ( 22.07280086217093640, 8.086143481909148889, -2.050000000000076650 ) ) ;
#29014=EDGE_LOOP ( 'NONE', ( #30698, #3416, #2440, #5262, #15082, #17890 ) ) ;
#29017=CARTESIAN_POINT ( 'NONE',  ( 51.72415272413284271, 3.851081239263533629, 1.414169555378673504 ) ) ;
#29025=ORIENTED_EDGE ( 'NONE', *, *, #27912, .F. ) ;
#29028=CARTESIAN_POINT ( 'NONE',  ( 51.60188271988062070, -4.191430714671220414, 1.624095931900496836 ) ) ;
#29039=CARTESIAN_POINT ( 'NONE',  ( 30.98482657347519975, 7.184130539199036214, 1.949999999999890710 ) ) ;
#29043=CARTESIAN_POINT ( 'NONE',  ( 54.21707933481621922, 5.861459378068796688, -2.050000000000189004 ) ) ;
#29071=CARTESIAN_POINT ( 'NONE',  ( 31.30720621464603326, 7.411182539856416618, 1.949999999999890488 ) ) ;
#29075=VECTOR ( 'NONE', #20557, 1000.000000000000000 ) ;
#29076=CARTESIAN_POINT ( 'NONE',  ( 53.91574522235882228, 6.672251602522421443, 1.774295301432037286 ) ) ;
#29082=CARTESIAN_POINT ( 'NONE',  ( 52.45567523936517773, 8.517307475678894235, -2.050000000000181899 ) ) ;
#29084=CARTESIAN_POINT ( 'NONE',  ( 54.28867365409859502, 5.640057820322912363, -1.950000000000180256 ) ) ;
#29087=CARTESIAN_POINT ( 'NONE',  ( 51.80000000000001137, 6.475000000000062705, -1.950000000000180256 ) ) ;
#29089=DIRECTION ( 'NONE',  ( 0.09218405009836744268, -0.9957419851083220141, -9.170184867090491304E-13 ) ) ;
#29092=CARTESIAN_POINT ( 'NONE',  ( 54.02708675723533105, 5.727819401067892890, 2.034055266290029085 ) ) ;
#29102=PLANE ( 'NONE',  #30831 ) ;
#29107=CARTESIAN_POINT ( 'NONE',  ( 47.10000000000002984, -4.020776289669855785, 2.234582293948414122 ) ) ;
#29108=ORIENTED_EDGE ( 'NONE', *, *, #13112, .T. ) ;
#29110=DIRECTION ( 'NONE',  ( -1.000000000000000000, -0.000000000000000000, 3.491481338843133355E-15 ) ) ;
#29118=VECTOR ( 'NONE', #20845, 1000.000000000000000 ) ;
#29122=CARTESIAN_POINT ( 'NONE',  ( 32.51063813751913045, 7.887597498970548848, -1.950000000000113864 ) ) ;
#29126=AXIS2_PLACEMENT_3D ( 'NONE', #24272, #14899, #7777 ) ;
#29128=CARTESIAN_POINT ( 'NONE',  ( 51.67649652704533736, -3.663955391962993247, 1.843087722223471392 ) ) ;
#29129=CARTESIAN_POINT ( 'NONE',  ( 27.79265796670792099, 5.432811198890458826, 1.424999999999903011 ) ) ;
#29132=EDGE_CURVE ( 'NONE', #7829, #11599, #21837, .T. ) ;
#29135=ADVANCED_FACE ( 'NONE', ( #16053 ), #7493, .T. ) ;
#29137=DIRECTION ( 'NONE',  ( 9.754918421198722508E-16, -0.9601771338024398528, 0.2793919678926571337 ) ) ;
#29154=FILL_AREA_STYLE_COLOUR ( '', #29275 ) ;
#29165=CIRCLE ( 'NONE', #15511, 4.600000000000036948 ) ;
#29170=CARTESIAN_POINT ( 'NONE',  ( 53.96125931204732495, 5.169815675097246377, -2.050000000000188116 ) ) ;
#29183=CARTESIAN_POINT ( 'NONE',  ( 47.12400915267975421, -4.149782173365510474, 1.728795876848494339 ) ) ;
#29189=CARTESIAN_POINT ( 'NONE',  ( 51.80000000000001847, -3.995252422878564857, 2.068710474281524991 ) ) ;
#29191=ORIENTED_EDGE ( 'NONE', *, *, #11354, .T. ) ;
#29202=CARTESIAN_POINT ( 'NONE',  ( 30.73039768916305192, 7.037486599914624108, 1.949999999999957989 ) ) ;
#29205=CARTESIAN_POINT ( 'NONE',  ( 52.18343291569983222, 8.689381540779887558, -2.050000000000181455 ) ) ;
#29221=ORIENTED_EDGE ( 'NONE', *, *, #111, .F. ) ;
#29222=CARTESIAN_POINT ( 'NONE',  ( 52.98753545145217458, 8.419778228641124684, 2.049999999999815081 ) ) ;
#29236=CARTESIAN_POINT ( 'NONE',  ( 30.73039768916300218, 7.037486599914601015, -1.950000000000105871 ) ) ;
#29242=CARTESIAN_POINT ( 'NONE',  ( 52.48739568812349177, 8.621481665389278959, -2.050000000000182343 ) ) ;
#29247=CARTESIAN_POINT ( 'NONE',  ( 51.70000000000002416, 2.428612866367529932E-14, -1.805095852181900386E-13 ) ) ;
#29250=DIRECTION ( 'NONE',  ( -1.000000000000000000, 0.000000000000000000, 3.491481338843132961E-15 ) ) ;
#29254=CARTESIAN_POINT ( 'NONE',  ( 54.10831690868383959, 6.369227351352716227, 2.033314590869161442 ) ) ;
#29264=ORIENTED_EDGE ( 'NONE', *, *, #25507, .F. ) ;
#29266=B_SPLINE_CURVE_WITH_KNOTS ( 'NONE', 3,
 ( #3774, #13415, #11373, #28000, #6481, #6315, #2036 ),
 .UNSPECIFIED., .F., .F.,
 ( 4, 1, 1, 1, 4 ),
 ( 0.000000000000000000, 0.2499733219912199933, 0.4999822146608134954, 0.7499911073304068587, 1.000000000000000000 ),
 .UNSPECIFIED. ) ;
#29275=COLOUR_RGB ( '', 0.31764706, 0.68627451, 0.89019608) ;
#29278=CARTESIAN_POINT ( 'NONE',  ( 31.58270314793946909, 7.514175884156569118, -1.425000000000109956 ) ) ;
#29281=EDGE_CURVE ( 'NONE', #3677, #4799, #11457, .T. ) ;
#29283=CARTESIAN_POINT ( 'NONE',  ( 25.58670780871698369, 5.245615029320309652, -1.950000000000087885 ) ) ;
#29287=CARTESIAN_POINT ( 'NONE',  ( 51.70000000000001705, -3.609867133138429551, 1.947518732152937027 ) ) ;
#29288=CARTESIAN_POINT ( 'NONE',  ( 25.71580480958625969, 5.235626398479815258, 1.424999999999910560 ) ) ;
#29312=VECTOR ( 'NONE', #14429, 999.9999999999998863 ) ;
#29330=CARTESIAN_POINT ( 'NONE',  ( 52.50319102799119264, 3.945003566797451899, -1.118186572507700038 ) ) ;
#29340=VERTEX_POINT ( 'NONE', #6513 ) ;
#29351=ADVANCED_FACE ( 'NONE', ( #1918 ), #30090, .T. ) ;
#29362=EDGE_LOOP ( 'NONE', ( #3520, #9751, #23264, #24524 ) ) ;
#29363=ORIENTED_EDGE ( 'NONE', *, *, #21915, .T. ) ;
#29364=ORIENTED_EDGE ( 'NONE', *, *, #18097, .F. ) ;
#29369=CARTESIAN_POINT ( 'NONE',  ( 47.05963571244990362, 8.266527678078146479, -2.050000000000163691 ) ) ;
#29370=ORIENTED_EDGE ( 'NONE', *, *, #10477, .T. ) ;
#29373=CARTESIAN_POINT ( 'NONE',  ( 53.90826771765248537, 6.078164526406591328, -1.689602626210267466 ) ) ;
#29374=ORIENTED_EDGE ( 'NONE', *, *, #7778, .F. ) ;
#29378=CARTESIAN_POINT ( 'NONE',  ( 33.98208436257626630, 8.188484708539069956, -1.950000000000503775 ) ) ;
#29385=CARTESIAN_POINT ( 'NONE',  ( 51.29912638713658168, 3.898228643449899167, -2.050000000000178790 ) ) ;
#29393=CARTESIAN_POINT ( 'NONE',  ( 53.81457038983117513, 5.799118250651475570, -1.689328355159275041 ) ) ;
#29396=EDGE_LOOP ( 'NONE', ( #59, #19315, #20505, #4576, #17621, #8429 ) ) ;
#29398=( BOUNDED_CURVE ( )  B_SPLINE_CURVE ( 3, ( #21552, #3959, #13602, #18544 ),
 .UNSPECIFIED., .F., .T. ) 
 B_SPLINE_CURVE_WITH_KNOTS ( ( 4, 4 ),
 ( 4.712388980384687898, 6.283185307179586232 ),
 .UNSPECIFIED. ) 
 CURVE ( )  GEOMETRIC_REPRESENTATION_ITEM ( )  RATIONAL_B_SPLINE_CURVE ( ( 1.000000000000000000, 0.8047378541243646044, 0.8047378541243646044, 1.000000000000000000 ) ) 
 REPRESENTATION_ITEM ( '' )  );
#29404=ORIENTED_EDGE ( 'NONE', *, *, #23887, .T. ) ;
#29421=ORIENTED_EDGE ( 'NONE', *, *, #2433, .F. ) ;
#29425=CARTESIAN_POINT ( 'NONE',  ( 51.80000000000001847, 2.428612866367529932E-14, -1.808587333520743709E-13 ) ) ;
#29427=CARTESIAN_POINT ( 'NONE',  ( 51.51881050553487995, -3.793704335752947632, 1.557065711441241840 ) ) ;
#29428=CARTESIAN_POINT ( 'NONE',  ( 30.78427835929706191, 7.077770142316436974, 1.424999999999892353 ) ) ;
#29444=AXIS2_PLACEMENT_3D ( 'NONE', #11706, #27574, #16018 ) ;
#29465=CARTESIAN_POINT ( 'NONE',  ( 51.74870924761699342, 3.850494199885640345, 1.444083690939125697 ) ) ;
#29467=CARTESIAN_POINT ( 'NONE',  ( 52.06031971197555919, 3.858116234519211929, -1.389650576489513956 ) ) ;
#29468=CARTESIAN_POINT ( 'NONE',  ( 47.86851286004601036, -4.319730106380312407, 1.256953381515252044 ) ) ;
#29478=CARTESIAN_POINT ( 'NONE',  ( 33.10182602044763200, 8.045524457602619250, 1.949999999999884714 ) ) ;
#29500=CARTESIAN_POINT ( 'NONE',  ( 53.29207122288458720, 4.934008984266801789, 1.614082030464476292 ) ) ;
#29514=CARTESIAN_POINT ( 'NONE',  ( 51.42113644652349080, -4.356776102639509318, -1.481376528584163577 ) ) ;
#29518=CARTESIAN_POINT ( 'NONE',  ( 26.61920844898535776, 5.219578738934656847, -1.950000000000091438 ) ) ;
#29521=CARTESIAN_POINT ( 'NONE',  ( 47.28076429169690442, -3.793498434807316855, 1.557570148622769546 ) ) ;
#29526=CARTESIAN_POINT ( 'NONE',  ( 54.21235476094169314, 5.862613896911505584, -2.050000000000189004 ) ) ;
#29541=CARTESIAN_POINT ( 'NONE',  ( 54.17607972459842358, 5.677832729363556652, 2.049999999999814637 ) ) ;
#29549=CARTESIAN_POINT ( 'NONE',  ( 51.04089638944252272, -4.379721596991722699, 1.407221449367199506 ) ) ;
#29574=( BOUNDED_SURFACE ( )  B_SPLINE_SURFACE ( 3, 2, ( 
 ( #25268, #27807, #23056 ),
 ( #20842, #8174, #6264 ),
 ( #25568, #16087, #8775 ),
 ( #15911, #13690, #23371 ),
 ( #1651, #1354, #17842 ),
 ( #25105, #27479, #5796 ),
 ( #15451, #3435, #8322 ),
 ( #17991, #15770, #22759 ),
 ( #1052, #10703, #27644 ),
 ( #6119, #11023, #30170 ) ),
 .UNSPECIFIED., .F., .F., .F. ) 
 B_SPLINE_SURFACE_WITH_KNOTS ( ( 4, 2, 2, 2, 4 ),
 ( 3, 3 ),
 ( -5.421010862427522170E-20, 0.0003534648051082245031, 0.0007069296102164490062, 0.001060394415324673618, 0.001413859220432898012 ),
 ( 0.000000000000000000, 1.000000000000000000 ),
 .UNSPECIFIED. ) 
 GEOMETRIC_REPRESENTATION_ITEM ( )  RATIONAL_B_SPLINE_SURFACE ( (
 ( 1.000000000000000000, 0.7071067811865467956, 1.000000000000000000),
 ( 1.000000000000000000, 0.6969521241106181320, 1.000000000000000000),
 ( 1.000000000000000000, 0.6903264600367975401, 1.000000000000000000),
 ( 1.000000000000000000, 0.6841066566212652411, 1.000000000000000000),
 ( 1.000000000000000000, 0.6845305055633155167, 1.000000000000000000),
 ( 1.000000000000000000, 0.6885489555143140539, 1.000000000000000000),
 ( 1.000000000000000000, 0.6920376555006676478, 1.000000000000000000),
 ( 1.000000000000000000, 0.6973723772399861298, 1.000000000000000000),
 ( 1.000000000000000000, 0.6992679762642822761, 1.000000000000000000),
 ( 1.000000000000000000, 0.6992058987801010872, 1.000000000000000000) ) ) 
 REPRESENTATION_ITEM ( '' )  SURFACE ( )  );
#29580=CARTESIAN_POINT ( 'NONE',  ( 26.90437805175149677, 5.347594907239942685, 2.049999999999904787 ) ) ;
#29591=TOROIDAL_SURFACE ( 'NONE', #20011, 4.500000000000037303, 0.1000000000000000056 ) ;
#29603=ORIENTED_EDGE ( 'NONE', *, *, #28923, .T. ) ;
#29605=CARTESIAN_POINT ( 'NONE',  ( 52.09213388422776347, 8.599999999993013233, -2.050000000000181011 ) ) ;
#29610=CARTESIAN_POINT ( 'NONE',  ( 51.41735323613823994, -3.967853068034125741, 1.365472663300960177 ) ) ;
#29643=CARTESIAN_POINT ( 'NONE',  ( 28.61151848776741602, 5.704727522705969278, 1.949999999999900924 ) ) ;
#29647=CARTESIAN_POINT ( 'NONE',  ( 47.00000000000002132, 2.428612866367529932E-14, -1.640996229256273308E-13 ) ) ;
#29650=CARTESIAN_POINT ( 'NONE',  ( 25.06719628359775953, 5.330953183167972398, 2.049999999999911005 ) ) ;
#29651=VERTEX_POINT ( 'NONE', #11697 ) ;
#29656=CARTESIAN_POINT ( 'NONE',  ( 52.72388909184999761, 4.000582417204456398, -2.050000000000183675 ) ) ;
#29660=EDGE_CURVE ( 'NONE', #21368, #26143, #31224, .T. ) ;
#29661=CARTESIAN_POINT ( 'NONE',  ( 51.80000000000001137, -3.637377585518695611, -2.099877210783217318 ) ) ;
#29662=CARTESIAN_POINT ( 'NONE',  ( 47.00000000000001421, -3.657334280697314810, -2.105684202162497520 ) ) ;
#29686=CARTESIAN_POINT ( 'NONE',  ( 54.11548297085168713, 5.698162749561729079, -2.050000000000191225 ) ) ;
#29688=CARTESIAN_POINT ( 'NONE',  ( 51.70000000000001705, 3.851905453475298113, -1.404572667215154835 ) ) ;
#29690=CARTESIAN_POINT ( 'NONE',  ( 28.70703846264934000, 5.747922415052726386, -2.049999999999577938 ) ) ;
#29697=CARTESIAN_POINT ( 'NONE',  ( 53.93792434297149185, 7.473468098462470621, -2.050000000000187672 ) ) ;
#29698=CARTESIAN_POINT ( 'NONE',  ( 47.49593195540760604, -3.900599430603016060, -1.266782962024618708 ) ) ;
#29709=DIRECTION ( 'NONE',  ( 0.7313537016191670181, 0.6819983600625022513, -2.468850131082252327E-15 ) ) ;
#29715=CARTESIAN_POINT ( 'NONE',  ( 54.41366571437519895, 6.718673005292167488, -1.625000000000181188 ) ) ;
#29717=EDGE_CURVE ( 'NONE', #9056, #7143, #24093, .T. ) ;
#29721=CARTESIAN_POINT ( 'NONE',  ( 51.76844985144015254, 4.130398687517124579, 1.964667065638868726 ) ) ;
#29730=DIRECTION ( 'NONE',  ( 3.489354422748178582E-15, -1.218509414717996338E-16, 1.000000000000000000 ) ) ;
#29763=CARTESIAN_POINT ( 'NONE',  ( 28.63101374161908907, 6.274379892050022001, 1.424999999999899458 ) ) ;
#29764=ORIENTED_EDGE ( 'NONE', *, *, #18892, .F. ) ;
#29771=EDGE_CURVE ( 'NONE', #14732, #16720, #30872, .T. ) ;
#29774=CARTESIAN_POINT ( 'NONE',  ( 53.71202192472753012, 7.447163568589559191, -2.050000000000249401 ) ) ;
#29781=CARTESIAN_POINT ( 'NONE',  ( 30.08242191457676995, 7.215531071606934965, -1.425000000000104849 ) ) ;
#29788=ORIENTED_EDGE ( 'NONE', *, *, #27741, .F. ) ;
#29801=VERTEX_POINT ( 'NONE', #2973 ) ;
#29809=CARTESIAN_POINT ( 'NONE',  ( 51.96434559586250401, 4.380380852615003207, -1.404523007340313212 ) ) ;
#29810=VECTOR ( 'NONE', #25667, 1000.000000000000000 ) ;
#29815=CARTESIAN_POINT ( 'NONE',  ( 22.61091062455514589, 6.637672123835637983, 1.949999999999954214 ) ) ;
#29820=CARTESIAN_POINT ( 'NONE',  ( 54.41366571437520605, 6.718673005292168376, -1.950000000000180256 ) ) ;
#29831=LINE ( 'NONE', #22874, #12955 ) ;
#29846=CARTESIAN_POINT ( 'NONE',  ( 51.79999999999973426, 3.849999999998453770, -1.627286622740575339 ) ) ;
#29848=CARTESIAN_POINT ( 'NONE',  ( 27.81683722849682638, 5.540920426342174743, -2.050000000000097078 ) ) ;
#29854=CARTESIAN_POINT ( 'NONE',  ( 47.38141046868508965, -3.967542327744154829, 1.366354831956431370 ) ) ;
#29855=CARTESIAN_POINT ( 'NONE',  ( 47.21128518863328338, -3.753741921856249331, -1.652517360674314206 ) ) ;
#29861=CARTESIAN_POINT ( 'NONE',  ( 34.56702326949724835, 8.213851659285209550, -1.950000000000119860 ) ) ;
#29863=FACE_OUTER_BOUND ( 'NONE', #11699, .T. ) ;
#29868=EDGE_CURVE ( 'NONE', #29651, #12157, #20089, .T. ) ;
#29870=CARTESIAN_POINT ( 'NONE',  ( 54.41366571437519895, 6.718673005292166600, -1.856154119295183591E-13 ) ) ;
#29871=EDGE_LOOP ( 'NONE', ( #7762, #9129, #9543, #19211 ) ) ;
#29885=CARTESIAN_POINT ( 'NONE',  ( 51.94586206790092575, 3.919599533071086661, 2.045267139815340585 ) ) ;
#29910=CARTESIAN_POINT ( 'NONE',  ( 47.10000000000002984, -3.637377585518695611, 2.099877210782872261 ) ) ;
#29912=VERTEX_POINT ( 'NONE', #3596 ) ;
#29921=ADVANCED_FACE ( 'NONE', ( #5813 ), #3453, .F. ) ;
#29930=CARTESIAN_POINT ( 'NONE',  ( 53.89553379148919277, 6.017104844469294278, -2.050000000000187228 ) ) ;
#29935=DIRECTION ( 'NONE',  ( 0.000000000000000000, 0.000000000000000000, 1.000000000000000000 ) ) ;
#29946=VECTOR ( 'NONE', #14009, 1000.000000000000114 ) ;
#29951=CARTESIAN_POINT ( 'NONE',  ( 52.02336772807330334, 3.827384603151627207, 2.049999999999818190 ) ) ;
#29957=EDGE_CURVE ( 'NONE', #16445, #3208, #27963, .T. ) ;
#29966=CARTESIAN_POINT ( 'NONE',  ( 23.88937650878824925, 5.720041404659278683, 2.049999999999714717 ) ) ;
#29971=CARTESIAN_POINT ( 'NONE',  ( 47.06312566212015724, 8.366466760780054912, -2.050000000000163691 ) ) ;
#29976=ADVANCED_FACE ( 'NONE', ( #11813 ), #28287, .T. ) ;
#29994=DIRECTION ( 'NONE',  ( -1.000000000000000000, -0.000000000000000000, 3.491481338843133355E-15 ) ) ;
#30001=CARTESIAN_POINT ( 'NONE',  ( 47.86779985288954009, -4.031600731540144977, 1.173113608404348529 ) ) ;
#30002=LINE ( 'NONE', #13070, #2501 ) ;
#30014=CARTESIAN_POINT ( 'NONE',  ( 54.39855553801235288, 5.984306564616975521, 1.990863471608376845 ) ) ;
#30016=CARTESIAN_POINT ( 'NONE',  ( 50.80000000000002558, -3.908336260473454615, 1.238913909465742424 ) ) ;
#30037=CIRCLE ( 'NONE', #1223, 0.09999999999999867328 ) ;
#30043=CARTESIAN_POINT ( 'NONE',  ( 53.54945414537598936, 7.685533664402775855, -1.865296808329178102 ) ) ;
#30049=CARTESIAN_POINT ( 'NONE',  ( 31.44395763972472579, 7.534587386684770571, 2.049999999999888800 ) ) ;
#30071=ORIENTED_EDGE ( 'NONE', *, *, #7831, .F. ) ;
#30074=CARTESIAN_POINT ( 'NONE',  ( 52.38400031671216794, 8.538946093000149062, -2.050000000000181899 ) ) ;
#30078=EDGE_CURVE ( 'NONE', #22071, #26766, #7401, .T. ) ;
#30081=ADVANCED_FACE ( 'NONE', ( #21660 ), #7441, .T. ) ;
#30090=PLANE ( 'NONE',  #31193 ) ;
#30093=CARTESIAN_POINT ( 'NONE',  ( 52.48717296556563383, 8.620750214766543351, 2.049999999999817302 ) ) ;
#30103=EDGE_LOOP ( 'NONE', ( #16458, #10867, #21745, #26404, #16889 ) ) ;
#30104=CARTESIAN_POINT ( 'NONE',  ( 52.08333333333334991, 4.368973594129894167, -1.439468559502902645 ) ) ;
#30106=ORIENTED_EDGE ( 'NONE', *, *, #11955, .T. ) ;
#30111=CIRCLE ( 'NONE', #24554, 160.6997717543497686 ) ;
#30151=CARTESIAN_POINT ( 'NONE',  ( 23.07431837327370161, 6.199584068344814902, -2.050000000000079758 ) ) ;
#30159=EDGE_CURVE ( 'NONE', #363, #18295, #20111, .T. ) ;
#30162=CARTESIAN_POINT ( 'NONE',  ( 47.20240392245177219, -3.813771782910507557, 1.508835477669279168 ) ) ;
#30168=DIRECTION ( 'NONE',  ( -0.9993908270190957621, 0.03489949670250106634, 3.490838185622846777E-15 ) ) ;
#30170=CARTESIAN_POINT ( 'NONE',  ( 50.80000000000002558, -4.319730106884872356, 1.256953381662059055 ) ) ;
#30179=CARTESIAN_POINT ( 'NONE',  ( 54.40301487434273753, 5.980869423001016649, -0.9750000000001823874 ) ) ;
#30181=FACE_OUTER_BOUND ( 'NONE', #24174, .T. ) ;
#30183=CARTESIAN_POINT ( 'NONE',  ( 52.05393800078983446, 4.345106731198570493, 1.549654688285104331 ) ) ;
#30189=CARTESIAN_POINT ( 'NONE',  ( 47.05963571244990362, 8.266527678078146479, -2.050000000000163691 ) ) ;
#30193=ORIENTED_EDGE ( 'NONE', *, *, #24967, .F. ) ;
#30196=ORIENTED_EDGE ( 'NONE', *, *, #8696, .T. ) ;
#30211=AXIS2_PLACEMENT_3D ( 'NONE', #21993, #31007, #9328 ) ;
#30228=ORIENTED_EDGE ( 'NONE', *, *, #6537, .F. ) ;
#30230=CARTESIAN_POINT ( 'NONE',  ( 31.20024169076946308, 7.859880411735725048, 1.424999999999890798 ) ) ;
#30236=ADVANCED_FACE ( 'NONE', ( #2936 ), #24776, .T. ) ;
#30238=CARTESIAN_POINT ( 'NONE',  ( 53.19737178513464215, 4.872051914464355704, -1.602904050740938890 ) ) ;
#30242=DIRECTION ( 'NONE',  ( -0.9993908270190952070, 0.03489949670251432656, 3.492791461889839594E-15 ) ) ;
#30246=DIRECTION ( 'NONE',  ( -1.000000000000000000, -0.000000000000000000, 3.491481338843133355E-15 ) ) ;
#30248=CARTESIAN_POINT ( 'NONE',  ( 50.87826055314399554, 8.733544086820096197, 1.949999999999822320 ) ) ;
#30267=EDGE_LOOP ( 'NONE', ( #4992, #4754, #24745, #14014, #11033, #21813, #23743, #1927 ) ) ;
#30290=CARTESIAN_POINT ( 'NONE',  ( 54.04962709127944720, 6.684747557764787906, 2.023090456646976509 ) ) ;
#30298=AXIS2_PLACEMENT_3D ( 'NONE', #2070, #4747, #31209 ) ;
#30302=CARTESIAN_POINT ( 'NONE',  ( 47.02574391948114396, -4.052343190076495461, 1.949685991417499764 ) ) ;
#30305=CARTESIAN_POINT ( 'NONE',  ( 51.60192307426172675, -4.191416138886287612, -1.624134901684648913 ) ) ;
#30310=CARTESIAN_POINT ( 'NONE',  ( 22.18976255005414444, 7.481058471420858780, -2.050000000000077094 ) ) ;
#30319=CARTESIAN_POINT ( 'NONE',  ( 48.00000000000002132, -4.031600731908414836, 1.173113608511506367 ) ) ;
#30330=DIRECTION ( 'NONE',  ( 0.000000000000000000, 0.000000000000000000, 1.000000000000000000 ) ) ;
#30332=EDGE_CURVE ( 'NONE', #11640, #12796, #28200, .T. ) ;
#30338=ADVANCED_FACE ( 'NONE', ( #25945 ), #5453, .T. ) ;
#30339=CARTESIAN_POINT ( 'NONE',  ( 53.94136487687671178, 6.599443998687474000, 2.049999999999811529 ) ) ;
#30344=CARTESIAN_POINT ( 'NONE',  ( 30.17845427745894682, 6.795635868401290303, -2.050000000000105516 ) ) ;
#30348=DIRECTION ( 'NONE',  ( -0.9993908270191184107, 0.03489949670185085034, 3.491481338843133355E-15 ) ) ;
#30356=B_SPLINE_CURVE_WITH_KNOTS ( 'NONE', 3,
 ( #3497, #15978, #28175, #25180, #21069, #18071, #20606, #27714, #25640, #1568, #13745, #20902, #30238, #5865, #16148, #30532, #8838, #6180, #18533, #6034, #6490 ),
 .UNSPECIFIED., .F., .F.,
 ( 4, 2, 2, 1, 2, 2, 1, 1, 2, 2, 2, 4 ),
 ( 0.5844128917508384369, 0.6883096688131545848, 0.7402580573443117151, 0.7467516059107093263, 0.7499983801939079653, 0.7516217673355072293, 0.7532451544771066043, 0.7662322516098910574, 0.7922064458754600746, 0.8441548344065958887, 0.8961032229377317027, 1.000000000000000000 ),
 .UNSPECIFIED. ) ;
#30360=CARTESIAN_POINT ( 'NONE',  ( 41.48619405471883681, -151.3359592902621955, -1.550000000000163469 ) ) ;
#30403=B_SPLINE_CURVE_WITH_KNOTS ( 'NONE', 3,
 ( #10984, #11132, #8740, #30290, #15877, #27917 ),
 .UNSPECIFIED., .F., .F.,
 ( 4, 2, 4 ),
 ( 0.000000000000000000, 0.4999999999999995559, 1.000000000000000000 ),
 .UNSPECIFIED. ) ;
#30409=CARTESIAN_POINT ( 'NONE',  ( 53.31611809544275360, 8.197428291949846013, 2.049999999999814193 ) ) ;
#30410=FACE_OUTER_BOUND ( 'NONE', #8874, .T. ) ;
#30416=ORIENTED_EDGE ( 'NONE', *, *, #11359, .F. ) ;
#30417=CARTESIAN_POINT ( 'NONE',  ( 23.28297127712496106, 6.056087685919490760, 1.949999999999917577 ) ) ;
#30451=CARTESIAN_POINT ( 'NONE',  ( 51.70000000000000995, -4.020776289669855785, -2.234582293948758291 ) ) ;
#30457=CARTESIAN_POINT ( 'NONE',  ( 24.79111845547821247, 5.500805180497733815, -2.050000000000085976 ) ) ;
#30466=CARTESIAN_POINT ( 'NONE',  ( 53.60047708782985154, 7.640852521089521510, -1.861455469535500340 ) ) ;
#30468=CARTESIAN_POINT ( 'NONE',  ( 41.48619405471885102, -151.3359592902622239, 1.949999999999835865 ) ) ;
#30472=CARTESIAN_POINT ( 'NONE',  ( 22.04321716858593661, 7.679566743993218481, -2.050000000000076650 ) ) ;
#30480=CARTESIAN_POINT ( 'NONE',  ( 54.17609772354683884, 5.677826690772942442, -2.050000000000186784 ) ) ;
#30481=EDGE_LOOP ( 'NONE', ( #3704, #12786, #26089, #24342 ) ) ;
#30482=CARTESIAN_POINT ( 'NONE',  ( 51.58871481136676351, -3.753741921856246222, 1.652517360673975588 ) ) ;
#30483=ORIENTED_EDGE ( 'NONE', *, *, #30988, .F. ) ;
#30484=CARTESIAN_POINT ( 'NONE',  ( 53.55869261961972683, 7.702978059423483792, 2.049999999999813305 ) ) ;
#30489=CARTESIAN_POINT ( 'NONE',  ( 26.00383130008247079, 5.312289655708096525, -2.050000000000089972 ) ) ;
#30491=EDGE_CURVE ( 'NONE', #15816, #17715, #21131, .T. ) ;
#30506=EDGE_CURVE ( 'NONE', #5154, #16857, #11514, .T. ) ;
#30516=ORIENTED_EDGE ( 'NONE', *, *, #2655, .T. ) ;
#30529=CIRCLE ( 'NONE', #11319, 2.525000000001611511 ) ;
#30532=CARTESIAN_POINT ( 'NONE',  ( 52.88901726360196420, 4.646846922877157837, -1.580885370238881427 ) ) ;
#30543=CARTESIAN_POINT ( 'NONE',  ( 51.80000000000002558, -3.936726248589973221, 1.145507068359712388 ) ) ;
#30549=CARTESIAN_POINT ( 'NONE',  ( 47.49367672221800518, -4.280384112421974585, -1.378579207634685222 ) ) ;
#30552=VERTEX_POINT ( 'NONE', #12931 ) ;
#30554=( BOUNDED_SURFACE ( )  B_SPLINE_SURFACE ( 3, 2, ( 
 ( #19898, #24060, #15136 ),
 ( #24793, #3101, #10550 ),
 ( #22428, #8316, #13069 ),
 ( #7272, #29698, #571 ),
 ( #12902, #720, #20227 ),
 ( #26585, #894, #17987 ),
 ( #29855, #15290, #17684 ),
 ( #5638, #14389, #22284 ),
 ( #10379, #1047, #8169 ),
 ( #3430, #17838, #5792 ) ),
 .UNSPECIFIED., .F., .F., .F. ) 
 B_SPLINE_SURFACE_WITH_KNOTS ( ( 4, 2, 2, 2, 4 ),
 ( 3, 3 ),
 ( -5.421010862427522170E-20, 0.0003537438758377275429, 0.0007074877516754551942, 0.001061231627513182845, 0.001414975503350910388 ),
 ( 0.000000000000000000, 1.000000000000000000 ),
 .UNSPECIFIED. ) 
 GEOMETRIC_REPRESENTATION_ITEM ( )  RATIONAL_B_SPLINE_SURFACE ( (
 ( 1.000000000000000000, 0.7154752000627009334, 1.000000000000000000),
 ( 1.000000000000000000, 0.7154106121887914282, 1.000000000000000000),
 ( 1.000000000000000000, 0.7173719856081617330, 1.000000000000000000),
 ( 1.000000000000000000, 0.7229186815313275449, 1.000000000000000000),
 ( 1.000000000000000000, 0.7264660769266189089, 1.000000000000000000),
 ( 1.000000000000000000, 0.7305267549325924481, 1.000000000000000000),
 ( 1.000000000000000000, 0.7309418327394059389, 1.000000000000000000),
 ( 1.000000000000000000, 0.7246992783962609153, 1.000000000000000000),
 ( 1.000000000000000000, 0.7179850693091097691, 1.000000000000000000),
 ( 1.000000000000000000, 0.7071067811865482389, 1.000000000000000000) ) ) 
 REPRESENTATION_ITEM ( '' )  SURFACE ( )  );
#30561=CARTESIAN_POINT ( 'NONE',  ( 53.60227722476025747, 4.617096236911464757, 2.049999999999812861 ) ) ;
#30563=VERTEX_POINT ( 'NONE', #20253 ) ;
#30568=ORIENTED_EDGE ( 'NONE', *, *, #10429, .T. ) ;
#30575=EDGE_CURVE ( 'NONE', #25126, #11599, #12746, .T. ) ;
#30581=CARTESIAN_POINT ( 'NONE',  ( 22.58884618656103882, 6.655783678991572749, -1.425000000000078648 ) ) ;
#30583=AXIS2_PLACEMENT_3D ( 'NONE', #13792, #1948, #28232 ) ;
#30593=CARTESIAN_POINT ( 'NONE',  ( 47.00000000000000711, 7.037983420167852921E-14, -4.500000000000199840 ) ) ;
#30594=CIRCLE ( 'NONE', #19509, 0.1000000000000000472 ) ;
#30599=FILL_AREA_STYLE_COLOUR ( '', #23071 ) ;
#30600=VERTEX_POINT ( 'NONE', #12465 ) ;
#30611=CARTESIAN_POINT ( 'NONE',  ( 48.00000000000002842, -4.291790910095608425, 1.352971095042313499 ) ) ;
#30613=CARTESIAN_POINT ( 'NONE',  ( 22.10122560051033602, 7.779108733371300488, -2.050000000000076206 ) ) ;
#30620=CARTESIAN_POINT ( 'NONE',  ( 51.80000000000002558, -4.319730106884873244, 1.256953381662055724 ) ) ;
#30621=VECTOR ( 'NONE', #28656, 1000.000000000000114 ) ;
#30632=CIRCLE ( 'NONE', #26079, 0.1000000000000000472 ) ;
#30634=ADVANCED_FACE ( 'NONE', ( #17863 ), #3132, .F. ) ;
#30637=FACE_OUTER_BOUND ( 'NONE', #4054, .T. ) ;
#30638=CIRCLE ( 'NONE', #13422, 160.1997717543138720 ) ;
#30645=CARTESIAN_POINT ( 'NONE',  ( 51.41454121074928452, -3.877603133525080903, 1.337216932410616010 ) ) ;
#30648=CARTESIAN_POINT ( 'NONE',  ( 52.80835374156199435, 4.037528258991556207, 2.049999999999815969 ) ) ;
#30693=CARTESIAN_POINT ( 'NONE',  ( 22.07280086217093640, 8.086143481909154218, -1.425000000000076650 ) ) ;
#30695=DIRECTION ( 'NONE',  ( -0.9993908270190953180, 0.03489949670251430575, 3.490905158897711881E-15 ) ) ;
#30698=ORIENTED_EDGE ( 'NONE', *, *, #9940, .T. ) ;
#30705=AXIS2_PLACEMENT_3D ( 'NONE', #4474, #21430, #7316 ) ;
#30715=CIRCLE ( 'NONE', #20628, 160.5997717543497743 ) ;
#30717=ORIENTED_EDGE ( 'NONE', *, *, #5661, .T. ) ;
#30718=AXIS2_PLACEMENT_3D ( 'NONE', #13892, #1412, #11072 ) ;
#30725=TOROIDAL_SURFACE ( 'NONE', #28726, 159.7997717543496776, 0.1000000000000000056 ) ;
#30729=CARTESIAN_POINT ( 'NONE',  ( 51.80000000000001137, -4.031600731908413948, -1.173113608511855421 ) ) ;
#30732=ORIENTED_EDGE ( 'NONE', *, *, #28181, .T. ) ;
#30733=PLANE ( 'NONE',  #15094 ) ;
#30755=ORIENTED_EDGE ( 'NONE', *, *, #3383, .F. ) ;
#30770=ORIENTED_EDGE ( 'NONE', *, *, #12811, .T. ) ;
#30781=ORIENTED_EDGE ( 'NONE', *, *, #10687, .T. ) ;
#30782=LINE ( 'NONE', #16539, #16968 ) ;
#30783=VERTEX_POINT ( 'NONE', #31132 ) ;
#30786=CARTESIAN_POINT ( 'NONE',  ( 50.35762544161294585, 8.151359338959888845, -2.050000000000174794 ) ) ;
#30792=ORIENTED_EDGE ( 'NONE', *, *, #17751, .F. ) ;
#30816=CARTESIAN_POINT ( 'NONE',  ( 53.16217804548205805, 8.131925109091699966, 2.049999999999814637 ) ) ;
#30827=CARTESIAN_POINT ( 'NONE',  ( 50.83686442967773900, 8.734989671305513070, 2.049999999999822631 ) ) ;
#30829=CARTESIAN_POINT ( 'NONE',  ( 53.06647667635083820, 8.205144683163286601, 1.913422281012191029 ) ) ;
#30831=AXIS2_PLACEMENT_3D ( 'NONE', #2974, #19920, #21849 ) ;
#30838=VECTOR ( 'NONE', #24291, 999.9999999999998863 ) ;
#30839=B_SPLINE_CURVE_WITH_KNOTS ( 'NONE', 3,
 ( #15554, #10322, #27422, #15382, #27567, #19991, #8569, #5896, #18099 ),
 .UNSPECIFIED., .F., .F.,
 ( 4, 1, 1, 1, 1, 1, 4 ),
 ( 0.000000000000000000, 0.08990530927501938496, 0.2069505209790863942, 0.2957249676700259844, 0.5865340158044511920, 0.7553074047937105018, 0.9685669348269276835 ),
 .UNSPECIFIED. ) ;
#30852=VERTEX_POINT ( 'NONE', #23544 ) ;
#30853=DIRECTION ( 'NONE',  ( 3.489354422748178582E-15, -1.218509414717996338E-16, 1.000000000000000000 ) ) ;
#30861=DIRECTION ( 'NONE',  ( 0.9993908270190958731, -0.03489949670250092062, -3.492262959426260213E-15 ) ) ;
#30869=DIRECTION ( 'NONE',  ( 0.000000000000000000, 0.000000000000000000, 1.000000000000000000 ) ) ;
#30872=B_SPLINE_CURVE_WITH_KNOTS ( 'NONE', 3,
 ( #24352, #22151, #29549, #588, #3279, #5329, #742, #10101, #2665, #15310 ),
 .UNSPECIFIED., .F., .F.,
 ( 4, 2, 2, 2, 4 ),
 ( 0.000000000000000000, 0.0003600849014046860722, 0.0007201698028093721443, 0.001080254704214058271, 0.001440339605618744289 ),
 .UNSPECIFIED. ) ;
#30882=DIRECTION ( 'NONE',  ( 3.489354422748178582E-15, -1.218509414717996338E-16, 1.000000000000000000 ) ) ;
#30883=CARTESIAN_POINT ( 'NONE',  ( 47.86788581435126844, -4.319730106544175108, -1.256953381563268524 ) ) ;
#30887=ADVANCED_FACE ( 'NONE', ( #2636 ), #11660, .T. ) ;
#30913=CARTESIAN_POINT ( 'NONE',  ( 23.49584529083620765, 5.910990189302484765, -1.425000000000082201 ) ) ;
#30926=CARTESIAN_POINT ( 'NONE',  ( 53.25905939444253789, 8.220207195185320614, 2.049999999999814637 ) ) ;
#30937=VERTEX_POINT ( 'NONE', #19085 ) ;
#30942=AXIS2_PLACEMENT_3D ( 'NONE', #17213, #24636, #5162 ) ;
#30943=CARTESIAN_POINT ( 'NONE',  ( 51.80000000000001137, -4.003661535119149129, -1.169131321892099340 ) ) ;
#30949=ORIENTED_EDGE ( 'NONE', *, *, #14425, .F. ) ;
#30958=DIRECTION ( 'NONE',  ( -3.489354422748178582E-15, 1.218509414717996338E-16, -1.000000000000000000 ) ) ;
#30965=ORIENTED_EDGE ( 'NONE', *, *, #7778, .T. ) ;
#30968=CARTESIAN_POINT ( 'NONE',  ( 53.34494210428216832, 4.987020249080381440, 2.049999999999814193 ) ) ;
#30969=AXIS2_PLACEMENT_3D ( 'NONE', #9124, #23700, #1089 ) ;
#30974=ORIENTED_EDGE ( 'NONE', *, *, #16016, .F. ) ;
#30981=CARTESIAN_POINT ( 'NONE',  ( 51.87416143049284756, 8.598705507415683513, 1.949999999999818767 ) ) ;
#30988=EDGE_CURVE ( 'NONE', #363, #17715, #7050, .T. ) ;
#30993=DIRECTION ( 'NONE',  ( 3.016910393003118404E-15, 0.000000000000000000, 1.000000000000000000 ) ) ;
#30998=ORIENTED_EDGE ( 'NONE', *, *, #2830, .T. ) ;
#31006=DIRECTION ( 'NONE',  ( 3.489354422748178582E-15, -1.218509414717996338E-16, 1.000000000000000000 ) ) ;
#31007=DIRECTION ( 'NONE',  ( -0.9990609829735203062, -0.04332611568077059105, 3.480798531547777782E-15 ) ) ;
#31018=CARTESIAN_POINT ( 'NONE',  ( 48.00000000000001421, -4.291790910095608425, -1.352971095042649008 ) ) ;
#31023=CARTESIAN_POINT ( 'NONE',  ( 47.10000000000002984, -3.933368109459640660, 2.186004417993010485 ) ) ;
#31024=PLANE ( 'NONE',  #293 ) ;
#31030=CARTESIAN_POINT ( 'NONE',  ( 47.27781215386389846, -4.266866293145928246, -1.720819027622056518 ) ) ;
#31035=FACE_OUTER_BOUND ( 'NONE', #10462, .T. ) ;
#31055=EDGE_CURVE ( 'NONE', #30852, #21603, #19640, .T. ) ;
#31064=DIRECTION ( 'NONE',  ( 3.016910393003118404E-15, 0.000000000000000000, 1.000000000000000000 ) ) ;
#31071=CARTESIAN_POINT ( 'NONE',  ( 54.12923718489511060, 6.977553454647814846, 2.049999999999811973 ) ) ;
#31075=CARTESIAN_POINT ( 'NONE',  ( 54.39855551779084664, 5.984306579698073669, -1.990863909997389714 ) ) ;
#31080=CARTESIAN_POINT ( 'NONE',  ( 51.41758644520160715, -4.256399122627303022, 1.449625929767385246 ) ) ;
#31089=EDGE_LOOP ( 'NONE', ( #16972, #22422, #4495, #14023 ) ) ;
#31093=CARTESIAN_POINT ( 'NONE',  ( 27.84544208489372252, 5.444976783748807669, 1.949999999999901368 ) ) ;
#31095=ORIENTED_EDGE ( 'NONE', *, *, #29771, .F. ) ;
#31113=EDGE_LOOP ( 'NONE', ( #516, #12853, #7965, #17154 ) ) ;
#31125=EDGE_CURVE ( 'NONE', #3631, #18665, #10046, .T. ) ;
#31132=CARTESIAN_POINT ( 'NONE',  ( 51.70000000000000995, -3.550773357292059007, -2.049880134336001802 ) ) ;
#31136=ORIENTED_EDGE ( 'NONE', *, *, #18116, .T. ) ;
#31154=CARTESIAN_POINT ( 'NONE',  ( 53.26701594926968397, 4.937284862446969846, 1.609150370324200718 ) ) ;
#31155=CARTESIAN_POINT ( 'NONE',  ( 53.90434097516060774, 5.769000224701694712, 1.948881089517881859 ) ) ;
#31169=CARTESIAN_POINT ( 'NONE',  ( 22.07280086217095061, 8.086143481909152442, 1.949999999999922906 ) ) ;
#31171=DIRECTION ( 'NONE',  ( 0.000000000000000000, 0.000000000000000000, 1.000000000000000000 ) ) ;
#31174=ORIENTED_EDGE ( 'NONE', *, *, #25090, .F. ) ;
#31193=AXIS2_PLACEMENT_3D ( 'NONE', #10941, #1438, #20629 ) ;
#31201=CARTESIAN_POINT ( 'NONE',  ( 51.03418148659205400, -3.901693722832460409, 1.260438308020271903 ) ) ;
#31205=AXIS2_PLACEMENT_3D ( 'NONE', #1466, #3547, #24905 ) ;
#31207=CARTESIAN_POINT ( 'NONE',  ( 50.87477060347373481, 8.633605004118187765, -2.050000000000176570 ) ) ;
#31209=DIRECTION ( 'NONE',  ( 3.384826294588897856E-15, 0.000000000000000000, 1.000000000000000000 ) ) ;
#31211=ORIENTED_EDGE ( 'NONE', *, *, #6697, .T. ) ;
#31217=EDGE_CURVE ( 'NONE', #25954, #12796, #12392, .T. ) ;
#31224=CIRCLE ( 'NONE', #17569, 2.525000000001609290 ) ;
#31240=LINE ( 'NONE', #9566, #9960 ) ;
#31260=CARTESIAN_POINT ( 'NONE',  ( 51.94556111432137868, 4.388904740222429268, -1.377811342933043859 ) ) ;
#31264=CARTESIAN_POINT ( 'NONE',  ( 29.99460040655817394, 6.535150012679998177, 1.949999999999896261 ) ) ;
#31268=( BOUNDED_SURFACE ( )  B_SPLINE_SURFACE ( 2, 3, ( 
 ( #14490, #9749, #24161, #26837, #24451, #29500, #11964, #24610, #5284, #17042, #5140, #14941, #24311, #19410, #14793, #2762, #2928, #7363 ),
 ( #12570, #7816, #26695, #21650, #31278, #21803, #4991, #2620, #9609, #19267, #7213, #16876, #27566, #18560, #25503, #8416, #6518, #3360 ),
 ( #18098, #13012, #25671, #28033, #6350, #23158, #3977, #13617, #1590, #27739, #991, #22846, #10787, #30409, #20929, #30093, #6202, #16008 ),
 ( #1442, #1279, #11251, #11102, #23307, #30561, #8869, #25030, #22696, #8260, #22990, #10643, #3814, #28207, #6058, #3521, #15710, #20781 ),
 ( #20321, #8568, #29951, #17926, #5895, #25357, #15553, #25205, #13160, #27888, #1136, #15849, #13460, #8713, #20472, #10945, #18397, #3663 ) ),
 .UNSPECIFIED., .F., .F., .F. ) 
 B_SPLINE_SURFACE_WITH_KNOTS ( ( 3, 2, 3 ),
 ( 4, 2, 2, 2, 2, 2, 2, 2, 4 ),
 ( 0.000000000000000000, 1.000000000000000000, 1.010000000000000009 ),
 ( 1.413716694115406902, 1.826050729899067360, 2.238384765682727817, 2.650718801466387831, 3.063052837250048288, 3.475386873033708746, 3.887720908817368759, 4.300054944601029661, 4.712388980384689674 ),
 .UNSPECIFIED. ) 
 GEOMETRIC_REPRESENTATION_ITEM ( )  RATIONAL_B_SPLINE_SURFACE ( (
 ( 1.000000000000000000, 1.000000000000000000, 1.000000000000000000, 1.000000000000000000, 1.000000000000000000, 1.000000000000000000, 1.000000000000000000, 1.000000000000000000, 1.000000000000000000, 1.000000000000000000, 1.000000000000000000, 1.000000000000000000, 1.000000000000000000, 1.000000000000000000, 1.000000000000000000, 1.000000000000000000, 1.000000000000000000, 1.000000000000000000),
 ( 0.7071067811865476838, 0.7071067811865476838, 0.7071067811865473507, 0.7071067811865473507, 0.7071067811865476838, 0.7071067811865476838, 0.7071067811865476838, 0.7071067811865476838, 0.7071067811865473507, 0.7071067811865473507, 0.7071067811865476838, 0.7071067811865476838, 0.7071067811865480168, 0.7071067811865480168, 0.7071067811865450192, 0.7071067811865450192, 0.7071067811865467956, 0.7071067811865467956),
 ( 1.000000000000000000, 1.000000000000000000, 1.000000000000000000, 1.000000000000000000, 1.000000000000000000, 1.000000000000000000, 1.000000000000000000, 1.000000000000000000, 1.000000000000000000, 1.000000000000000000, 1.000000000000000000, 1.000000000000000000, 1.000000000000000000, 1.000000000000000000, 1.000000000000000000, 1.000000000000000000, 1.000000000000000000, 1.000000000000000000),
 ( 1.000000000000000000, 1.000000000000000000, 1.000000000000000000, 1.000000000000000000, 1.000000000000000000, 1.000000000000000000, 1.000000000000000000, 1.000000000000000000, 1.000000000000000000, 1.000000000000000000, 1.000000000000000000, 1.000000000000000000, 1.000000000000000000, 1.000000000000000000, 1.000000000000000000, 1.000000000000000000, 1.000000000000000000, 1.000000000000000000),
 ( 1.000000000000000000, 1.000000000000000000, 1.000000000000000000, 1.000000000000000000, 1.000000000000000000, 1.000000000000000000, 1.000000000000000000, 1.000000000000000000, 1.000000000000000000, 1.000000000000000000, 1.000000000000000000, 1.000000000000000000, 1.000000000000000000, 1.000000000000000000, 1.000000000000000000, 1.000000000000000000, 1.000000000000000000, 1.000000000000000000) ) ) 
 REPRESENTATION_ITEM ( '' )  SURFACE ( )  );
#31270=CARTESIAN_POINT ( 'NONE',  ( 52.08333333333334991, 4.368973594129894167, -1.439468559502902645 ) ) ;
#31274=CARTESIAN_POINT ( 'NONE',  ( 48.00000000000002132, -4.031600731908413948, 1.173113608511506367 ) ) ;
#31278=CARTESIAN_POINT ( 'NONE',  ( 52.82099478266075465, 4.588601447596422744, 2.049999999999815081 ) ) ;
#31279=EDGE_LOOP ( 'NONE', ( #15590, #15085, #660, #23775 ) ) ;
#31284=ORIENTED_EDGE ( 'NONE', *, *, #25445, .T. ) ;
#31292=CARTESIAN_POINT ( 'NONE',  ( 23.13503935330941275, 6.279616010019203998, -2.050000000000080647 ) ) ;
#31294=CARTESIAN_POINT ( 'NONE',  ( 34.56702326949724835, 8.213851659285209550, -1.950000000000119860 ) ) ;
#31298=CARTESIAN_POINT ( 'NONE',  ( 52.08333333333335702, 4.368973594129894167, 1.439468559502539824 ) ) ;
#31323=ORIENTED_EDGE ( 'NONE', *, *, #23079, .T. ) ;
ENDSEC;
END-ISO-10303-21;
